ISO-10303-21;
HEADER;
/* Generated by software containing ST-Developer
 * from STEP Tools, Inc. (www.steptools.com) 
 */

FILE_DESCRIPTION(
/* description */ ('', 'CAx-IF Rec.Pracs.---Representation and Presentation of Product Manufa
cturing Information (PMI)---4.0---2014-10-13'),
/* implementation_level */ '2;1');

FILE_NAME(
/* name */ 'Countersunk Screw 2.5x12.step',
/* time_stamp */ '2026-10-28T14:45:12+01:00',
/* author */ (''),
/* organization */ (''),
/* preprocessor_version */ 'ST-DEVELOPER v20.2',
/* originating_system */ 'Autodesk Translation Framework v15.17.0.0',
/* authorisation */ '');

FILE_SCHEMA (('AP242_MANAGED_MODEL_BASED_3D_ENGINEERING_MIM_LF { 1 0 10303 442 2 1 4 }'));
ENDSEC;

DATA;
#10=MECHANICAL_DESIGN_GEOMETRIC_PRESENTATION_REPRESENTATION('',(#264),#52164);
#92=ELLIPSE('',#9924,0.251906298612587,0.25);
#93=ELLIPSE('',#9925,0.251906298612587,0.25);
#94=ELLIPSE('',#9926,0.251906298612587,0.25);
#95=ELLIPSE('',#9927,0.251906298612587,0.25);
#96=ELLIPSE('',#9928,0.251906298612587,0.25);
#97=ELLIPSE('',#9929,0.251906298612587,0.25);
#98=ELLIPSE('',#9930,0.251906298612587,0.25);
#99=ELLIPSE('',#9931,0.251906298612587,0.25);
#100=ELLIPSE('',#9932,0.251906298612587,0.25);
#101=ELLIPSE('',#9933,0.251906298612587,0.25);
#102=ELLIPSE('',#9934,0.251906298612587,0.25);
#103=ELLIPSE('',#9935,0.251906298612587,0.25);
#104=ELLIPSE('',#9951,0.251906298612587,0.25);
#105=ELLIPSE('',#9954,0.251906298612587,0.25);
#106=ELLIPSE('',#9955,0.251906298612587,0.25);
#107=ELLIPSE('',#9956,0.251906298612587,0.25);
#108=ELLIPSE('',#9957,0.251906298612587,0.25);
#109=ELLIPSE('',#9958,0.251906298612587,0.25);
#110=ELLIPSE('',#9959,0.251906298612587,0.25);
#111=ELLIPSE('',#9960,0.251906298612587,0.25);
#112=ELLIPSE('',#9961,0.251906298612587,0.25);
#113=ELLIPSE('',#9962,0.251906298612587,0.25);
#114=ELLIPSE('',#9963,0.251906298612587,0.25);
#115=ELLIPSE('',#9964,0.251906298612587,0.25);
#205=CONICAL_SURFACE('',#9938,1.725,0.785398163397448);
#206=CONICAL_SURFACE('',#9944,1.175,0.785398163397448);
#219=TOROIDAL_SURFACE('',#9940,1.594974746831,0.7);
#238=SHAPE_REPRESENTATION_RELATIONSHIP('SRR','None',#52217,#251);
#251=ADVANCED_BREP_SHAPE_REPRESENTATION('',(#277),#52157);
#264=STYLED_ITEM('',(#52325),#277);
#277=MANIFOLD_SOLID_BREP('Body1',#9124);
#303=FACE_BOUND('',#1425,.T.);
#370=B_SPLINE_SURFACE_WITH_KNOTS('',3,3,((#34681,#34682,#34683,#34684,#34685,
#34686,#34687,#34688,#34689,#34690,#34691,#34692,#34693,#34694,#34695,#34696,
#34697,#34698,#34699,#34700,#34701,#34702,#34703,#34704,#34705,#34706,#34707,
#34708,#34709,#34710,#34711,#34712,#34713,#34714,#34715),(#34716,#34717,
#34718,#34719,#34720,#34721,#34722,#34723,#34724,#34725,#34726,#34727,#34728,
#34729,#34730,#34731,#34732,#34733,#34734,#34735,#34736,#34737,#34738,#34739,
#34740,#34741,#34742,#34743,#34744,#34745,#34746,#34747,#34748,#34749,#34750),
(#34751,#34752,#34753,#34754,#34755,#34756,#34757,#34758,#34759,#34760,
#34761,#34762,#34763,#34764,#34765,#34766,#34767,#34768,#34769,#34770,#34771,
#34772,#34773,#34774,#34775,#34776,#34777,#34778,#34779,#34780,#34781,#34782,
#34783,#34784,#34785),(#34786,#34787,#34788,#34789,#34790,#34791,#34792,
#34793,#34794,#34795,#34796,#34797,#34798,#34799,#34800,#34801,#34802,#34803,
#34804,#34805,#34806,#34807,#34808,#34809,#34810,#34811,#34812,#34813,#34814,
#34815,#34816,#34817,#34818,#34819,#34820)),.UNSPECIFIED.,.F.,.F.,.F.,(4,
4),(4,1,1,1,1,1,1,1,1,1,1,1,1,1,1,1,1,1,1,1,1,1,1,1,1,1,1,1,1,1,1,1,4),
(-0.05164332951995,1.05164332952),(-0.02,0.0125,0.045,0.0775,0.11,0.1425,
0.175,0.2075,0.24,0.2725,0.305,0.3375,0.37,0.4025,0.435,0.4675,0.5,0.5325,
0.565,0.5975,0.63,0.6625,0.695,0.7275,0.76,0.7925,0.825,0.8575,0.89,0.9225,
0.955,0.9875,1.02),.UNSPECIFIED.);
#371=B_SPLINE_SURFACE_WITH_KNOTS('',3,3,((#35063,#35064,#35065,#35066,#35067,
#35068,#35069,#35070,#35071,#35072,#35073,#35074,#35075,#35076,#35077,#35078,
#35079,#35080,#35081,#35082,#35083,#35084,#35085,#35086,#35087,#35088,#35089,
#35090,#35091,#35092,#35093,#35094,#35095,#35096,#35097),(#35098,#35099,
#35100,#35101,#35102,#35103,#35104,#35105,#35106,#35107,#35108,#35109,#35110,
#35111,#35112,#35113,#35114,#35115,#35116,#35117,#35118,#35119,#35120,#35121,
#35122,#35123,#35124,#35125,#35126,#35127,#35128,#35129,#35130,#35131,#35132),
(#35133,#35134,#35135,#35136,#35137,#35138,#35139,#35140,#35141,#35142,
#35143,#35144,#35145,#35146,#35147,#35148,#35149,#35150,#35151,#35152,#35153,
#35154,#35155,#35156,#35157,#35158,#35159,#35160,#35161,#35162,#35163,#35164,
#35165,#35166,#35167),(#35168,#35169,#35170,#35171,#35172,#35173,#35174,
#35175,#35176,#35177,#35178,#35179,#35180,#35181,#35182,#35183,#35184,#35185,
#35186,#35187,#35188,#35189,#35190,#35191,#35192,#35193,#35194,#35195,#35196,
#35197,#35198,#35199,#35200,#35201,#35202)),.UNSPECIFIED.,.F.,.F.,.F.,(4,
4),(4,1,1,1,1,1,1,1,1,1,1,1,1,1,1,1,1,1,1,1,1,1,1,1,1,1,1,1,1,1,1,1,4),
(-0.05164332951996,1.05164332952),(-0.02,0.0125,0.045,0.0775,0.11,0.1425,
0.175,0.2075,0.24,0.2725,0.305,0.3375,0.37,0.4025,0.435,0.4675,0.5,0.5325,
0.565,0.5975,0.63,0.6625,0.695,0.7275,0.76,0.7925,0.825,0.8575,0.89,0.9225,
0.955,0.9875,1.02),.UNSPECIFIED.);
#372=B_SPLINE_SURFACE_WITH_KNOTS('',3,3,((#35371,#35372,#35373,#35374,#35375,
#35376,#35377,#35378,#35379,#35380,#35381,#35382,#35383,#35384,#35385,#35386,
#35387,#35388,#35389,#35390,#35391,#35392,#35393,#35394,#35395,#35396,#35397,
#35398,#35399,#35400,#35401,#35402,#35403,#35404,#35405),(#35406,#35407,
#35408,#35409,#35410,#35411,#35412,#35413,#35414,#35415,#35416,#35417,#35418,
#35419,#35420,#35421,#35422,#35423,#35424,#35425,#35426,#35427,#35428,#35429,
#35430,#35431,#35432,#35433,#35434,#35435,#35436,#35437,#35438,#35439,#35440),
(#35441,#35442,#35443,#35444,#35445,#35446,#35447,#35448,#35449,#35450,
#35451,#35452,#35453,#35454,#35455,#35456,#35457,#35458,#35459,#35460,#35461,
#35462,#35463,#35464,#35465,#35466,#35467,#35468,#35469,#35470,#35471,#35472,
#35473,#35474,#35475),(#35476,#35477,#35478,#35479,#35480,#35481,#35482,
#35483,#35484,#35485,#35486,#35487,#35488,#35489,#35490,#35491,#35492,#35493,
#35494,#35495,#35496,#35497,#35498,#35499,#35500,#35501,#35502,#35503,#35504,
#35505,#35506,#35507,#35508,#35509,#35510)),.UNSPECIFIED.,.F.,.F.,.F.,(4,
4),(4,1,1,1,1,1,1,1,1,1,1,1,1,1,1,1,1,1,1,1,1,1,1,1,1,1,1,1,1,1,1,1,4),
(-0.05164332951995,1.05164332952),(-0.02,0.0125,0.045,0.0775,0.11,0.1425,
0.175,0.2075,0.24,0.2725,0.305,0.3375,0.37,0.4025,0.435,0.4675,0.5,0.5325,
0.565,0.5975,0.63,0.6625,0.695,0.7275,0.76,0.7925,0.825,0.8575,0.89,0.9225,
0.955,0.9875,1.02),.UNSPECIFIED.);
#373=B_SPLINE_SURFACE_WITH_KNOTS('',3,3,((#35746,#35747,#35748,#35749,#35750,
#35751,#35752,#35753,#35754,#35755,#35756,#35757,#35758,#35759,#35760,#35761,
#35762,#35763,#35764,#35765,#35766,#35767,#35768,#35769,#35770,#35771,#35772,
#35773,#35774,#35775,#35776,#35777,#35778,#35779,#35780),(#35781,#35782,
#35783,#35784,#35785,#35786,#35787,#35788,#35789,#35790,#35791,#35792,#35793,
#35794,#35795,#35796,#35797,#35798,#35799,#35800,#35801,#35802,#35803,#35804,
#35805,#35806,#35807,#35808,#35809,#35810,#35811,#35812,#35813,#35814,#35815),
(#35816,#35817,#35818,#35819,#35820,#35821,#35822,#35823,#35824,#35825,
#35826,#35827,#35828,#35829,#35830,#35831,#35832,#35833,#35834,#35835,#35836,
#35837,#35838,#35839,#35840,#35841,#35842,#35843,#35844,#35845,#35846,#35847,
#35848,#35849,#35850),(#35851,#35852,#35853,#35854,#35855,#35856,#35857,
#35858,#35859,#35860,#35861,#35862,#35863,#35864,#35865,#35866,#35867,#35868,
#35869,#35870,#35871,#35872,#35873,#35874,#35875,#35876,#35877,#35878,#35879,
#35880,#35881,#35882,#35883,#35884,#35885)),.UNSPECIFIED.,.F.,.F.,.F.,(4,
4),(4,1,1,1,1,1,1,1,1,1,1,1,1,1,1,1,1,1,1,1,1,1,1,1,1,1,1,1,1,1,1,1,4),
(-0.05164332951996,1.05164332952),(-0.02,0.0125,0.045,0.0775,0.11,0.1425,
0.175,0.2075,0.24,0.2725,0.305,0.3375,0.37,0.4025,0.435,0.4675,0.5,0.5325,
0.565,0.5975,0.63,0.6625,0.695,0.7275,0.76,0.7925,0.825,0.8575,0.89,0.9225,
0.955,0.9875,1.02),.UNSPECIFIED.);
#374=B_SPLINE_SURFACE_WITH_KNOTS('',3,3,((#36047,#36048,#36049,#36050,#36051,
#36052,#36053,#36054,#36055,#36056,#36057,#36058,#36059,#36060,#36061,#36062,
#36063,#36064,#36065,#36066,#36067,#36068,#36069,#36070,#36071,#36072,#36073,
#36074,#36075,#36076,#36077,#36078,#36079,#36080,#36081),(#36082,#36083,
#36084,#36085,#36086,#36087,#36088,#36089,#36090,#36091,#36092,#36093,#36094,
#36095,#36096,#36097,#36098,#36099,#36100,#36101,#36102,#36103,#36104,#36105,
#36106,#36107,#36108,#36109,#36110,#36111,#36112,#36113,#36114,#36115,#36116),
(#36117,#36118,#36119,#36120,#36121,#36122,#36123,#36124,#36125,#36126,
#36127,#36128,#36129,#36130,#36131,#36132,#36133,#36134,#36135,#36136,#36137,
#36138,#36139,#36140,#36141,#36142,#36143,#36144,#36145,#36146,#36147,#36148,
#36149,#36150,#36151),(#36152,#36153,#36154,#36155,#36156,#36157,#36158,
#36159,#36160,#36161,#36162,#36163,#36164,#36165,#36166,#36167,#36168,#36169,
#36170,#36171,#36172,#36173,#36174,#36175,#36176,#36177,#36178,#36179,#36180,
#36181,#36182,#36183,#36184,#36185,#36186)),.UNSPECIFIED.,.F.,.F.,.F.,(4,
4),(4,1,1,1,1,1,1,1,1,1,1,1,1,1,1,1,1,1,1,1,1,1,1,1,1,1,1,1,1,1,1,1,4),
(-0.05164332951995,1.05164332952),(-0.02,0.0125,0.045,0.0775,0.11,0.1425,
0.175,0.2075,0.24,0.2725,0.305,0.3375,0.37,0.4025,0.435,0.4675,0.5,0.5325,
0.565,0.5975,0.63,0.6625,0.695,0.7275,0.76,0.7925,0.825,0.8575,0.89,0.9225,
0.955,0.9875,1.02),.UNSPECIFIED.);
#375=B_SPLINE_SURFACE_WITH_KNOTS('',3,3,((#36420,#36421,#36422,#36423,#36424,
#36425,#36426,#36427,#36428,#36429,#36430,#36431,#36432,#36433,#36434,#36435,
#36436,#36437,#36438,#36439,#36440,#36441,#36442,#36443,#36444,#36445,#36446,
#36447,#36448,#36449,#36450,#36451,#36452,#36453,#36454),(#36455,#36456,
#36457,#36458,#36459,#36460,#36461,#36462,#36463,#36464,#36465,#36466,#36467,
#36468,#36469,#36470,#36471,#36472,#36473,#36474,#36475,#36476,#36477,#36478,
#36479,#36480,#36481,#36482,#36483,#36484,#36485,#36486,#36487,#36488,#36489),
(#36490,#36491,#36492,#36493,#36494,#36495,#36496,#36497,#36498,#36499,
#36500,#36501,#36502,#36503,#36504,#36505,#36506,#36507,#36508,#36509,#36510,
#36511,#36512,#36513,#36514,#36515,#36516,#36517,#36518,#36519,#36520,#36521,
#36522,#36523,#36524),(#36525,#36526,#36527,#36528,#36529,#36530,#36531,
#36532,#36533,#36534,#36535,#36536,#36537,#36538,#36539,#36540,#36541,#36542,
#36543,#36544,#36545,#36546,#36547,#36548,#36549,#36550,#36551,#36552,#36553,
#36554,#36555,#36556,#36557,#36558,#36559)),.UNSPECIFIED.,.F.,.F.,.F.,(4,
4),(4,1,1,1,1,1,1,1,1,1,1,1,1,1,1,1,1,1,1,1,1,1,1,1,1,1,1,1,1,1,1,1,4),
(-0.05164332951996,1.05164332952),(-0.02,0.0125,0.045,0.0775,0.11,0.1425,
0.175,0.2075,0.24,0.2725,0.305,0.3375,0.37,0.4025,0.435,0.4675,0.5,0.5325,
0.565,0.5975,0.63,0.6625,0.695,0.7275,0.76,0.7925,0.825,0.8575,0.89,0.9225,
0.955,0.9875,1.02),.UNSPECIFIED.);
#376=B_SPLINE_SURFACE_WITH_KNOTS('',3,3,((#36721,#36722,#36723,#36724,#36725,
#36726,#36727,#36728,#36729,#36730,#36731,#36732,#36733,#36734,#36735,#36736,
#36737,#36738,#36739,#36740,#36741,#36742,#36743,#36744,#36745,#36746,#36747,
#36748,#36749,#36750,#36751,#36752,#36753,#36754,#36755),(#36756,#36757,
#36758,#36759,#36760,#36761,#36762,#36763,#36764,#36765,#36766,#36767,#36768,
#36769,#36770,#36771,#36772,#36773,#36774,#36775,#36776,#36777,#36778,#36779,
#36780,#36781,#36782,#36783,#36784,#36785,#36786,#36787,#36788,#36789,#36790),
(#36791,#36792,#36793,#36794,#36795,#36796,#36797,#36798,#36799,#36800,
#36801,#36802,#36803,#36804,#36805,#36806,#36807,#36808,#36809,#36810,#36811,
#36812,#36813,#36814,#36815,#36816,#36817,#36818,#36819,#36820,#36821,#36822,
#36823,#36824,#36825),(#36826,#36827,#36828,#36829,#36830,#36831,#36832,
#36833,#36834,#36835,#36836,#36837,#36838,#36839,#36840,#36841,#36842,#36843,
#36844,#36845,#36846,#36847,#36848,#36849,#36850,#36851,#36852,#36853,#36854,
#36855,#36856,#36857,#36858,#36859,#36860)),.UNSPECIFIED.,.F.,.F.,.F.,(4,
4),(4,1,1,1,1,1,1,1,1,1,1,1,1,1,1,1,1,1,1,1,1,1,1,1,1,1,1,1,1,1,1,1,4),
(-0.05164332951995,1.05164332952),(-0.02,0.0125,0.045,0.0775,0.11,0.1425,
0.175,0.2075,0.24,0.2725,0.305,0.3375,0.37,0.4025,0.435,0.4675,0.5,0.5325,
0.565,0.5975,0.63,0.6625,0.695,0.7275,0.76,0.7925,0.825,0.8575,0.89,0.9225,
0.955,0.9875,1.02),.UNSPECIFIED.);
#377=B_SPLINE_SURFACE_WITH_KNOTS('',3,3,((#37098,#37099,#37100,#37101,#37102,
#37103,#37104,#37105,#37106,#37107,#37108,#37109,#37110,#37111,#37112,#37113,
#37114,#37115,#37116,#37117,#37118,#37119,#37120,#37121,#37122,#37123,#37124,
#37125,#37126,#37127,#37128,#37129,#37130,#37131,#37132),(#37133,#37134,
#37135,#37136,#37137,#37138,#37139,#37140,#37141,#37142,#37143,#37144,#37145,
#37146,#37147,#37148,#37149,#37150,#37151,#37152,#37153,#37154,#37155,#37156,
#37157,#37158,#37159,#37160,#37161,#37162,#37163,#37164,#37165,#37166,#37167),
(#37168,#37169,#37170,#37171,#37172,#37173,#37174,#37175,#37176,#37177,
#37178,#37179,#37180,#37181,#37182,#37183,#37184,#37185,#37186,#37187,#37188,
#37189,#37190,#37191,#37192,#37193,#37194,#37195,#37196,#37197,#37198,#37199,
#37200,#37201,#37202),(#37203,#37204,#37205,#37206,#37207,#37208,#37209,
#37210,#37211,#37212,#37213,#37214,#37215,#37216,#37217,#37218,#37219,#37220,
#37221,#37222,#37223,#37224,#37225,#37226,#37227,#37228,#37229,#37230,#37231,
#37232,#37233,#37234,#37235,#37236,#37237)),.UNSPECIFIED.,.F.,.F.,.F.,(4,
4),(4,1,1,1,1,1,1,1,1,1,1,1,1,1,1,1,1,1,1,1,1,1,1,1,1,1,1,1,1,1,1,1,4),
(-0.05164332951996,1.05164332952),(-0.02,0.0125,0.045,0.0775,0.11,0.1425,
0.175,0.2075,0.24,0.2725,0.305,0.3375,0.37,0.4025,0.435,0.4675,0.5,0.5325,
0.565,0.5975,0.63,0.6625,0.695,0.7275,0.76,0.7925,0.825,0.8575,0.89,0.9225,
0.955,0.9875,1.02),.UNSPECIFIED.);
#378=B_SPLINE_SURFACE_WITH_KNOTS('',3,3,((#37401,#37402,#37403,#37404,#37405,
#37406,#37407,#37408,#37409,#37410,#37411,#37412,#37413,#37414,#37415,#37416,
#37417,#37418,#37419,#37420,#37421,#37422,#37423,#37424,#37425,#37426,#37427,
#37428,#37429,#37430,#37431,#37432,#37433,#37434,#37435),(#37436,#37437,
#37438,#37439,#37440,#37441,#37442,#37443,#37444,#37445,#37446,#37447,#37448,
#37449,#37450,#37451,#37452,#37453,#37454,#37455,#37456,#37457,#37458,#37459,
#37460,#37461,#37462,#37463,#37464,#37465,#37466,#37467,#37468,#37469,#37470),
(#37471,#37472,#37473,#37474,#37475,#37476,#37477,#37478,#37479,#37480,
#37481,#37482,#37483,#37484,#37485,#37486,#37487,#37488,#37489,#37490,#37491,
#37492,#37493,#37494,#37495,#37496,#37497,#37498,#37499,#37500,#37501,#37502,
#37503,#37504,#37505),(#37506,#37507,#37508,#37509,#37510,#37511,#37512,
#37513,#37514,#37515,#37516,#37517,#37518,#37519,#37520,#37521,#37522,#37523,
#37524,#37525,#37526,#37527,#37528,#37529,#37530,#37531,#37532,#37533,#37534,
#37535,#37536,#37537,#37538,#37539,#37540)),.UNSPECIFIED.,.F.,.F.,.F.,(4,
4),(4,1,1,1,1,1,1,1,1,1,1,1,1,1,1,1,1,1,1,1,1,1,1,1,1,1,1,1,1,1,1,1,4),
(-0.05164332951995,1.05164332952),(-0.02,0.0125,0.045,0.0775,0.11,0.1425,
0.175,0.2075,0.24,0.2725,0.305,0.3375,0.37,0.4025,0.435,0.4675,0.5,0.5325,
0.565,0.5975,0.63,0.6625,0.695,0.7275,0.76,0.7925,0.825,0.8575,0.89,0.9225,
0.955,0.9875,1.02),.UNSPECIFIED.);
#379=B_SPLINE_SURFACE_WITH_KNOTS('',3,3,((#37772,#37773,#37774,#37775,#37776,
#37777,#37778,#37779,#37780,#37781,#37782,#37783,#37784,#37785,#37786,#37787,
#37788,#37789,#37790,#37791,#37792,#37793,#37794,#37795,#37796,#37797,#37798,
#37799,#37800,#37801,#37802,#37803,#37804,#37805,#37806),(#37807,#37808,
#37809,#37810,#37811,#37812,#37813,#37814,#37815,#37816,#37817,#37818,#37819,
#37820,#37821,#37822,#37823,#37824,#37825,#37826,#37827,#37828,#37829,#37830,
#37831,#37832,#37833,#37834,#37835,#37836,#37837,#37838,#37839,#37840,#37841),
(#37842,#37843,#37844,#37845,#37846,#37847,#37848,#37849,#37850,#37851,
#37852,#37853,#37854,#37855,#37856,#37857,#37858,#37859,#37860,#37861,#37862,
#37863,#37864,#37865,#37866,#37867,#37868,#37869,#37870,#37871,#37872,#37873,
#37874,#37875,#37876),(#37877,#37878,#37879,#37880,#37881,#37882,#37883,
#37884,#37885,#37886,#37887,#37888,#37889,#37890,#37891,#37892,#37893,#37894,
#37895,#37896,#37897,#37898,#37899,#37900,#37901,#37902,#37903,#37904,#37905,
#37906,#37907,#37908,#37909,#37910,#37911)),.UNSPECIFIED.,.F.,.F.,.F.,(4,
4),(4,1,1,1,1,1,1,1,1,1,1,1,1,1,1,1,1,1,1,1,1,1,1,1,1,1,1,1,1,1,1,1,4),
(-0.05164332951996,1.05164332952),(-0.02,0.0125,0.045,0.0775,0.11,0.1425,
0.175,0.2075,0.24,0.2725,0.305,0.3375,0.37,0.4025,0.435,0.4675,0.5,0.5325,
0.565,0.5975,0.63,0.6625,0.695,0.7275,0.76,0.7925,0.825,0.8575,0.89,0.9225,
0.955,0.9875,1.02),.UNSPECIFIED.);
#380=B_SPLINE_SURFACE_WITH_KNOTS('',3,3,((#38073,#38074,#38075,#38076,#38077,
#38078,#38079,#38080,#38081,#38082,#38083,#38084,#38085,#38086,#38087,#38088,
#38089,#38090,#38091,#38092,#38093,#38094,#38095,#38096,#38097,#38098,#38099,
#38100,#38101,#38102,#38103,#38104,#38105,#38106,#38107),(#38108,#38109,
#38110,#38111,#38112,#38113,#38114,#38115,#38116,#38117,#38118,#38119,#38120,
#38121,#38122,#38123,#38124,#38125,#38126,#38127,#38128,#38129,#38130,#38131,
#38132,#38133,#38134,#38135,#38136,#38137,#38138,#38139,#38140,#38141,#38142),
(#38143,#38144,#38145,#38146,#38147,#38148,#38149,#38150,#38151,#38152,
#38153,#38154,#38155,#38156,#38157,#38158,#38159,#38160,#38161,#38162,#38163,
#38164,#38165,#38166,#38167,#38168,#38169,#38170,#38171,#38172,#38173,#38174,
#38175,#38176,#38177),(#38178,#38179,#38180,#38181,#38182,#38183,#38184,
#38185,#38186,#38187,#38188,#38189,#38190,#38191,#38192,#38193,#38194,#38195,
#38196,#38197,#38198,#38199,#38200,#38201,#38202,#38203,#38204,#38205,#38206,
#38207,#38208,#38209,#38210,#38211,#38212)),.UNSPECIFIED.,.F.,.F.,.F.,(4,
4),(4,1,1,1,1,1,1,1,1,1,1,1,1,1,1,1,1,1,1,1,1,1,1,1,1,1,1,1,1,1,1,1,4),
(-0.05164332951995,1.05164332952),(-0.02,0.0125,0.045,0.0775,0.11,0.1425,
0.175,0.2075,0.24,0.2725,0.305,0.3375,0.37,0.4025,0.435,0.4675,0.5,0.5325,
0.565,0.5975,0.63,0.6625,0.695,0.7275,0.76,0.7925,0.825,0.8575,0.89,0.9225,
0.955,0.9875,1.02),.UNSPECIFIED.);
#381=B_SPLINE_SURFACE_WITH_KNOTS('',3,3,((#38552,#38553,#38554,#38555,#38556,
#38557,#38558,#38559,#38560,#38561,#38562,#38563,#38564,#38565,#38566,#38567,
#38568,#38569,#38570,#38571,#38572,#38573,#38574,#38575,#38576,#38577,#38578,
#38579,#38580,#38581,#38582,#38583,#38584,#38585,#38586),(#38587,#38588,
#38589,#38590,#38591,#38592,#38593,#38594,#38595,#38596,#38597,#38598,#38599,
#38600,#38601,#38602,#38603,#38604,#38605,#38606,#38607,#38608,#38609,#38610,
#38611,#38612,#38613,#38614,#38615,#38616,#38617,#38618,#38619,#38620,#38621),
(#38622,#38623,#38624,#38625,#38626,#38627,#38628,#38629,#38630,#38631,
#38632,#38633,#38634,#38635,#38636,#38637,#38638,#38639,#38640,#38641,#38642,
#38643,#38644,#38645,#38646,#38647,#38648,#38649,#38650,#38651,#38652,#38653,
#38654,#38655,#38656),(#38657,#38658,#38659,#38660,#38661,#38662,#38663,
#38664,#38665,#38666,#38667,#38668,#38669,#38670,#38671,#38672,#38673,#38674,
#38675,#38676,#38677,#38678,#38679,#38680,#38681,#38682,#38683,#38684,#38685,
#38686,#38687,#38688,#38689,#38690,#38691)),.UNSPECIFIED.,.F.,.F.,.F.,(4,
4),(4,1,1,1,1,1,1,1,1,1,1,1,1,1,1,1,1,1,1,1,1,1,1,1,1,1,1,1,1,1,1,1,4),
(-0.05164332951995,1.05164332952),(0.1685302411052,0.1950231500896,0.221516059074,
0.2480089680584,0.2745018770427,0.3009947860271,0.3274876950115,0.3539806039959,
0.3804735129803,0.4069664219647,0.4334593309491,0.4599522399335,0.4864451489179,
0.5129380579023,0.5394309668867,0.5659238758711,0.5924167848555,0.6189096938399,
0.6454026028243,0.6718955118087,0.6983884207931,0.7248813297774,0.7513742387618,
0.7778671477462,0.8043600567306,0.830852965715,0.8573458746994,0.8838387836838,
0.9103316926682,0.9368246016526,0.963317510637,0.9898104196214,1.016303328606),
 .UNSPECIFIED.);
#382=B_SPLINE_SURFACE_WITH_KNOTS('',3,3,((#38949,#38950,#38951,#38952,#38953,
#38954,#38955,#38956,#38957,#38958,#38959,#38960,#38961,#38962,#38963,#38964,
#38965,#38966,#38967,#38968,#38969,#38970,#38971,#38972,#38973,#38974,#38975,
#38976,#38977,#38978,#38979,#38980,#38981,#38982,#38983),(#38984,#38985,
#38986,#38987,#38988,#38989,#38990,#38991,#38992,#38993,#38994,#38995,#38996,
#38997,#38998,#38999,#39000,#39001,#39002,#39003,#39004,#39005,#39006,#39007,
#39008,#39009,#39010,#39011,#39012,#39013,#39014,#39015,#39016,#39017,#39018),
(#39019,#39020,#39021,#39022,#39023,#39024,#39025,#39026,#39027,#39028,
#39029,#39030,#39031,#39032,#39033,#39034,#39035,#39036,#39037,#39038,#39039,
#39040,#39041,#39042,#39043,#39044,#39045,#39046,#39047,#39048,#39049,#39050,
#39051,#39052,#39053),(#39054,#39055,#39056,#39057,#39058,#39059,#39060,
#39061,#39062,#39063,#39064,#39065,#39066,#39067,#39068,#39069,#39070,#39071,
#39072,#39073,#39074,#39075,#39076,#39077,#39078,#39079,#39080,#39081,#39082,
#39083,#39084,#39085,#39086,#39087,#39088)),.UNSPECIFIED.,.F.,.F.,.F.,(4,
4),(4,1,1,1,1,1,1,1,1,1,1,1,1,1,1,1,1,1,1,1,1,1,1,1,1,1,1,1,1,1,1,1,4),
(-0.1318015091147,1.131801509115),(0.08569894047188,0.1148310820745,0.1439632236771,
0.1730953652797,0.2022275068823,0.2313596484849,0.2604917900876,0.2896239316902,
0.3187560732928,0.3478882148954,0.377020356498,0.4061524981006,0.4352846397032,
0.4644167813058,0.4935489229084,0.5226810645111,0.5518132061137,0.5809453477163,
0.6100774893189,0.6392096309215,0.6683417725241,0.6974739141267,0.7266060557293,
0.7557381973319,0.7848703389346,0.8140024805372,0.8431346221398,0.8722667637424,
0.901398905345,0.9305310469476,0.9596631885502,0.9887953301528,1.017927471755),
 .UNSPECIFIED.);
#383=B_SPLINE_SURFACE_WITH_KNOTS('',3,3,((#39090,#39091,#39092,#39093,#39094,
#39095,#39096,#39097,#39098,#39099,#39100,#39101,#39102,#39103,#39104,#39105,
#39106,#39107,#39108,#39109,#39110,#39111,#39112,#39113,#39114,#39115,#39116,
#39117,#39118,#39119,#39120,#39121,#39122,#39123,#39124),(#39125,#39126,
#39127,#39128,#39129,#39130,#39131,#39132,#39133,#39134,#39135,#39136,#39137,
#39138,#39139,#39140,#39141,#39142,#39143,#39144,#39145,#39146,#39147,#39148,
#39149,#39150,#39151,#39152,#39153,#39154,#39155,#39156,#39157,#39158,#39159),
(#39160,#39161,#39162,#39163,#39164,#39165,#39166,#39167,#39168,#39169,
#39170,#39171,#39172,#39173,#39174,#39175,#39176,#39177,#39178,#39179,#39180,
#39181,#39182,#39183,#39184,#39185,#39186,#39187,#39188,#39189,#39190,#39191,
#39192,#39193,#39194),(#39195,#39196,#39197,#39198,#39199,#39200,#39201,
#39202,#39203,#39204,#39205,#39206,#39207,#39208,#39209,#39210,#39211,#39212,
#39213,#39214,#39215,#39216,#39217,#39218,#39219,#39220,#39221,#39222,#39223,
#39224,#39225,#39226,#39227,#39228,#39229)),.UNSPECIFIED.,.F.,.F.,.F.,(4,
4),(4,1,1,1,1,1,1,1,1,1,1,1,1,1,1,1,1,1,1,1,1,1,1,1,1,1,1,1,1,1,1,1,4),
(-0.1318015091147,1.131801509115),(-0.02,0.0125,0.045,0.0775,0.11,0.1425,
0.175,0.2075,0.24,0.2725,0.305,0.3375,0.37,0.4025,0.435,0.4675,0.5,0.5325,
0.565,0.5975,0.63,0.6625,0.695,0.7275,0.76,0.7925,0.825,0.8575,0.89,0.9225,
0.955,0.9875,1.02),.UNSPECIFIED.);
#384=B_SPLINE_SURFACE_WITH_KNOTS('',3,3,((#39231,#39232,#39233,#39234,#39235,
#39236,#39237,#39238,#39239,#39240,#39241,#39242,#39243,#39244,#39245,#39246,
#39247,#39248,#39249,#39250,#39251,#39252,#39253,#39254,#39255,#39256,#39257,
#39258,#39259,#39260,#39261,#39262,#39263,#39264,#39265),(#39266,#39267,
#39268,#39269,#39270,#39271,#39272,#39273,#39274,#39275,#39276,#39277,#39278,
#39279,#39280,#39281,#39282,#39283,#39284,#39285,#39286,#39287,#39288,#39289,
#39290,#39291,#39292,#39293,#39294,#39295,#39296,#39297,#39298,#39299,#39300),
(#39301,#39302,#39303,#39304,#39305,#39306,#39307,#39308,#39309,#39310,
#39311,#39312,#39313,#39314,#39315,#39316,#39317,#39318,#39319,#39320,#39321,
#39322,#39323,#39324,#39325,#39326,#39327,#39328,#39329,#39330,#39331,#39332,
#39333,#39334,#39335),(#39336,#39337,#39338,#39339,#39340,#39341,#39342,
#39343,#39344,#39345,#39346,#39347,#39348,#39349,#39350,#39351,#39352,#39353,
#39354,#39355,#39356,#39357,#39358,#39359,#39360,#39361,#39362,#39363,#39364,
#39365,#39366,#39367,#39368,#39369,#39370)),.UNSPECIFIED.,.F.,.F.,.F.,(4,
4),(4,1,1,1,1,1,1,1,1,1,1,1,1,1,1,1,1,1,1,1,1,1,1,1,1,1,1,1,1,1,1,1,4),
(-0.1318015091147,1.131801509115),(-0.02,0.0125,0.045,0.0775,0.11,0.1425,
0.175,0.2075,0.24,0.2725,0.305,0.3375,0.37,0.4025,0.435,0.4675,0.5,0.5325,
0.565,0.5975,0.63,0.6625,0.695,0.7275,0.76,0.7925,0.825,0.8575,0.89,0.9225,
0.955,0.9875,1.02),.UNSPECIFIED.);
#385=B_SPLINE_SURFACE_WITH_KNOTS('',3,3,((#39372,#39373,#39374,#39375,#39376,
#39377,#39378,#39379,#39380,#39381,#39382,#39383,#39384,#39385,#39386,#39387,
#39388,#39389,#39390,#39391,#39392,#39393,#39394,#39395,#39396,#39397,#39398,
#39399,#39400,#39401,#39402,#39403,#39404,#39405,#39406),(#39407,#39408,
#39409,#39410,#39411,#39412,#39413,#39414,#39415,#39416,#39417,#39418,#39419,
#39420,#39421,#39422,#39423,#39424,#39425,#39426,#39427,#39428,#39429,#39430,
#39431,#39432,#39433,#39434,#39435,#39436,#39437,#39438,#39439,#39440,#39441),
(#39442,#39443,#39444,#39445,#39446,#39447,#39448,#39449,#39450,#39451,
#39452,#39453,#39454,#39455,#39456,#39457,#39458,#39459,#39460,#39461,#39462,
#39463,#39464,#39465,#39466,#39467,#39468,#39469,#39470,#39471,#39472,#39473,
#39474,#39475,#39476),(#39477,#39478,#39479,#39480,#39481,#39482,#39483,
#39484,#39485,#39486,#39487,#39488,#39489,#39490,#39491,#39492,#39493,#39494,
#39495,#39496,#39497,#39498,#39499,#39500,#39501,#39502,#39503,#39504,#39505,
#39506,#39507,#39508,#39509,#39510,#39511)),.UNSPECIFIED.,.F.,.F.,.F.,(4,
4),(4,1,1,1,1,1,1,1,1,1,1,1,1,1,1,1,1,1,1,1,1,1,1,1,1,1,1,1,1,1,1,1,4),
(-0.1318015091147,1.131801509115),(-0.02,0.0125,0.045,0.0775,0.11,0.1425,
0.175,0.2075,0.24,0.2725,0.305,0.3375,0.37,0.4025,0.435,0.4675,0.5,0.5325,
0.565,0.5975,0.63,0.6625,0.695,0.7275,0.76,0.7925,0.825,0.8575,0.89,0.9225,
0.955,0.9875,1.02),.UNSPECIFIED.);
#386=B_SPLINE_SURFACE_WITH_KNOTS('',3,3,((#39513,#39514,#39515,#39516,#39517,
#39518,#39519,#39520,#39521,#39522,#39523,#39524,#39525,#39526,#39527,#39528,
#39529,#39530,#39531,#39532,#39533,#39534,#39535,#39536,#39537,#39538,#39539,
#39540,#39541,#39542,#39543,#39544,#39545,#39546,#39547),(#39548,#39549,
#39550,#39551,#39552,#39553,#39554,#39555,#39556,#39557,#39558,#39559,#39560,
#39561,#39562,#39563,#39564,#39565,#39566,#39567,#39568,#39569,#39570,#39571,
#39572,#39573,#39574,#39575,#39576,#39577,#39578,#39579,#39580,#39581,#39582),
(#39583,#39584,#39585,#39586,#39587,#39588,#39589,#39590,#39591,#39592,
#39593,#39594,#39595,#39596,#39597,#39598,#39599,#39600,#39601,#39602,#39603,
#39604,#39605,#39606,#39607,#39608,#39609,#39610,#39611,#39612,#39613,#39614,
#39615,#39616,#39617),(#39618,#39619,#39620,#39621,#39622,#39623,#39624,
#39625,#39626,#39627,#39628,#39629,#39630,#39631,#39632,#39633,#39634,#39635,
#39636,#39637,#39638,#39639,#39640,#39641,#39642,#39643,#39644,#39645,#39646,
#39647,#39648,#39649,#39650,#39651,#39652)),.UNSPECIFIED.,.F.,.F.,.F.,(4,
4),(4,1,1,1,1,1,1,1,1,1,1,1,1,1,1,1,1,1,1,1,1,1,1,1,1,1,1,1,1,1,1,1,4),
(-0.1318015091147,1.131801509115),(-0.02,0.0125,0.045,0.0775,0.11,0.1425,
0.175,0.2075,0.24,0.2725,0.305,0.3375,0.37,0.4025,0.435,0.4675,0.5,0.5325,
0.565,0.5975,0.63,0.6625,0.695,0.7275,0.76,0.7925,0.825,0.8575,0.89,0.9225,
0.955,0.9875,1.02),.UNSPECIFIED.);
#387=B_SPLINE_SURFACE_WITH_KNOTS('',3,3,((#39654,#39655,#39656,#39657,#39658,
#39659,#39660,#39661,#39662,#39663,#39664,#39665,#39666,#39667,#39668,#39669,
#39670,#39671,#39672,#39673,#39674,#39675,#39676,#39677,#39678,#39679,#39680,
#39681,#39682,#39683,#39684,#39685,#39686,#39687,#39688),(#39689,#39690,
#39691,#39692,#39693,#39694,#39695,#39696,#39697,#39698,#39699,#39700,#39701,
#39702,#39703,#39704,#39705,#39706,#39707,#39708,#39709,#39710,#39711,#39712,
#39713,#39714,#39715,#39716,#39717,#39718,#39719,#39720,#39721,#39722,#39723),
(#39724,#39725,#39726,#39727,#39728,#39729,#39730,#39731,#39732,#39733,
#39734,#39735,#39736,#39737,#39738,#39739,#39740,#39741,#39742,#39743,#39744,
#39745,#39746,#39747,#39748,#39749,#39750,#39751,#39752,#39753,#39754,#39755,
#39756,#39757,#39758),(#39759,#39760,#39761,#39762,#39763,#39764,#39765,
#39766,#39767,#39768,#39769,#39770,#39771,#39772,#39773,#39774,#39775,#39776,
#39777,#39778,#39779,#39780,#39781,#39782,#39783,#39784,#39785,#39786,#39787,
#39788,#39789,#39790,#39791,#39792,#39793)),.UNSPECIFIED.,.F.,.F.,.F.,(4,
4),(4,1,1,1,1,1,1,1,1,1,1,1,1,1,1,1,1,1,1,1,1,1,1,1,1,1,1,1,1,1,1,1,4),
(-0.1318015091147,1.131801509115),(-0.02,0.0125,0.045,0.0775,0.11,0.1425,
0.175,0.2075,0.24,0.2725,0.305,0.3375,0.37,0.4025,0.435,0.4675,0.5,0.5325,
0.565,0.5975,0.63,0.6625,0.695,0.7275,0.76,0.7925,0.825,0.8575,0.89,0.9225,
0.955,0.9875,1.02),.UNSPECIFIED.);
#468=PLANE('',#9922);
#469=PLANE('',#9948);
#470=PLANE('',#9949);
#471=PLANE('',#9952);
#472=PLANE('',#9953);
#473=PLANE('',#9965);
#474=PLANE('',#9967);
#475=PLANE('',#9969);
#476=PLANE('',#9971);
#477=PLANE('',#9973);
#478=PLANE('',#9975);
#479=PLANE('',#9977);
#480=PLANE('',#9979);
#481=PLANE('',#9981);
#482=PLANE('',#9984);
#483=PLANE('',#9986);
#872=FACE_OUTER_BOUND('',#1424,.T.);
#873=FACE_OUTER_BOUND('',#1426,.T.);
#874=FACE_OUTER_BOUND('',#1427,.T.);
#875=FACE_OUTER_BOUND('',#1428,.T.);
#876=FACE_OUTER_BOUND('',#1429,.T.);
#877=FACE_OUTER_BOUND('',#1430,.T.);
#878=FACE_OUTER_BOUND('',#1431,.T.);
#879=FACE_OUTER_BOUND('',#1432,.T.);
#880=FACE_OUTER_BOUND('',#1433,.T.);
#881=FACE_OUTER_BOUND('',#1434,.T.);
#882=FACE_OUTER_BOUND('',#1435,.T.);
#883=FACE_OUTER_BOUND('',#1436,.T.);
#884=FACE_OUTER_BOUND('',#1437,.T.);
#885=FACE_OUTER_BOUND('',#1438,.T.);
#886=FACE_OUTER_BOUND('',#1439,.T.);
#887=FACE_OUTER_BOUND('',#1440,.T.);
#888=FACE_OUTER_BOUND('',#1441,.T.);
#889=FACE_OUTER_BOUND('',#1442,.T.);
#890=FACE_OUTER_BOUND('',#1443,.T.);
#891=FACE_OUTER_BOUND('',#1444,.T.);
#892=FACE_OUTER_BOUND('',#1445,.T.);
#893=FACE_OUTER_BOUND('',#1446,.T.);
#894=FACE_OUTER_BOUND('',#1447,.T.);
#895=FACE_OUTER_BOUND('',#1448,.T.);
#896=FACE_OUTER_BOUND('',#1449,.T.);
#897=FACE_OUTER_BOUND('',#1450,.T.);
#898=FACE_OUTER_BOUND('',#1451,.T.);
#899=FACE_OUTER_BOUND('',#1452,.T.);
#900=FACE_OUTER_BOUND('',#1453,.T.);
#901=FACE_OUTER_BOUND('',#1454,.T.);
#902=FACE_OUTER_BOUND('',#1455,.T.);
#903=FACE_OUTER_BOUND('',#1456,.T.);
#904=FACE_OUTER_BOUND('',#1457,.T.);
#905=FACE_OUTER_BOUND('',#1458,.T.);
#906=FACE_OUTER_BOUND('',#1459,.T.);
#907=FACE_OUTER_BOUND('',#1460,.T.);
#908=FACE_OUTER_BOUND('',#1461,.T.);
#909=FACE_OUTER_BOUND('',#1462,.T.);
#910=FACE_OUTER_BOUND('',#1463,.T.);
#911=FACE_OUTER_BOUND('',#1464,.T.);
#912=FACE_OUTER_BOUND('',#1465,.T.);
#913=FACE_OUTER_BOUND('',#1466,.T.);
#914=FACE_OUTER_BOUND('',#1467,.T.);
#915=FACE_OUTER_BOUND('',#1468,.T.);
#916=FACE_OUTER_BOUND('',#1469,.T.);
#917=FACE_OUTER_BOUND('',#1470,.T.);
#918=FACE_OUTER_BOUND('',#1471,.T.);
#919=FACE_OUTER_BOUND('',#1472,.T.);
#920=FACE_OUTER_BOUND('',#1473,.T.);
#921=FACE_OUTER_BOUND('',#1474,.T.);
#922=FACE_OUTER_BOUND('',#1475,.T.);
#1424=EDGE_LOOP('',(#7470));
#1425=EDGE_LOOP('',(#7471,#7472,#7473,#7474,#7475,#7476,#7477,#7478,#7479,
#7480,#7481,#7482,#7483,#7484,#7485,#7486,#7487,#7488,#7489,#7490,#7491,
#7492,#7493,#7494));
#1426=EDGE_LOOP('',(#7495,#7496,#7497,#7498));
#1427=EDGE_LOOP('',(#7499,#7500,#7501,#7502));
#1428=EDGE_LOOP('',(#7503,#7504,#7505,#7506,#7507));
#1429=EDGE_LOOP('',(#7508,#7509,#7510,#7511,#7512,#7513,#7514));
#1430=EDGE_LOOP('',(#7515,#7516,#7517,#7518));
#1431=EDGE_LOOP('',(#7519,#7520,#7521,#7522,#7523,#7524));
#1432=EDGE_LOOP('',(#7525,#7526,#7527,#7528,#7529));
#1433=EDGE_LOOP('',(#7530,#7531,#7532,#7533,#7534));
#1434=EDGE_LOOP('',(#7535,#7536,#7537,#7538,#7539));
#1435=EDGE_LOOP('',(#7540,#7541,#7542,#7543,#7544));
#1436=EDGE_LOOP('',(#7545,#7546,#7547,#7548,#7549));
#1437=EDGE_LOOP('',(#7550,#7551,#7552,#7553,#7554));
#1438=EDGE_LOOP('',(#7555,#7556,#7557,#7558,#7559));
#1439=EDGE_LOOP('',(#7560,#7561,#7562,#7563,#7564));
#1440=EDGE_LOOP('',(#7565,#7566,#7567,#7568,#7569));
#1441=EDGE_LOOP('',(#7570,#7571,#7572,#7573,#7574,#7575));
#1442=EDGE_LOOP('',(#7576,#7577,#7578,#7579,#7580));
#1443=EDGE_LOOP('',(#7581,#7582,#7583));
#1444=EDGE_LOOP('',(#7584,#7585,#7586,#7587));
#1445=EDGE_LOOP('',(#7588,#7589,#7590,#7591));
#1446=EDGE_LOOP('',(#7592,#7593,#7594,#7595));
#1447=EDGE_LOOP('',(#7596,#7597,#7598,#7599));
#1448=EDGE_LOOP('',(#7600,#7601,#7602,#7603));
#1449=EDGE_LOOP('',(#7604,#7605,#7606,#7607));
#1450=EDGE_LOOP('',(#7608,#7609,#7610,#7611));
#1451=EDGE_LOOP('',(#7612,#7613,#7614,#7615));
#1452=EDGE_LOOP('',(#7616,#7617,#7618,#7619));
#1453=EDGE_LOOP('',(#7620,#7621,#7622,#7623,#7624,#7625,#7626,#7627,#7628,
#7629,#7630,#7631,#7632,#7633,#7634,#7635,#7636,#7637,#7638,#7639,#7640,
#7641,#7642,#7643));
#1454=EDGE_LOOP('',(#7644,#7645,#7646,#7647));
#1455=EDGE_LOOP('',(#7648,#7649,#7650,#7651));
#1456=EDGE_LOOP('',(#7652,#7653,#7654,#7655));
#1457=EDGE_LOOP('',(#7656,#7657,#7658,#7659));
#1458=EDGE_LOOP('',(#7660,#7661,#7662,#7663));
#1459=EDGE_LOOP('',(#7664,#7665,#7666,#7667));
#1460=EDGE_LOOP('',(#7668,#7669,#7670,#7671));
#1461=EDGE_LOOP('',(#7672,#7673,#7674,#7675));
#1462=EDGE_LOOP('',(#7676,#7677,#7678,#7679));
#1463=EDGE_LOOP('',(#7680,#7681,#7682,#7683));
#1464=EDGE_LOOP('',(#7684,#7685,#7686,#7687));
#1465=EDGE_LOOP('',(#7688,#7689,#7690,#7691));
#1466=EDGE_LOOP('',(#7692,#7693,#7694,#7695));
#1467=EDGE_LOOP('',(#7696,#7697,#7698,#7699));
#1468=EDGE_LOOP('',(#7700,#7701,#7702,#7703));
#1469=EDGE_LOOP('',(#7704,#7705,#7706,#7707));
#1470=EDGE_LOOP('',(#7708,#7709,#7710,#7711));
#1471=EDGE_LOOP('',(#7712,#7713,#7714,#7715));
#1472=EDGE_LOOP('',(#7716,#7717,#7718,#7719));
#1473=EDGE_LOOP('',(#7720,#7721,#7722,#7723));
#1474=EDGE_LOOP('',(#7724,#7725,#7726,#7727));
#1475=EDGE_LOOP('',(#7728,#7729,#7730,#7731));
#1985=CIRCLE('',#9923,2.35);
#1986=CIRCLE('',#9937,2.35);
#1987=CIRCLE('',#9939,1.1);
#1988=CIRCLE('',#9941,0.7);
#1989=CIRCLE('',#9942,1.1);
#1990=CIRCLE('',#9943,1.1);
#1991=CIRCLE('',#9945,1.25);
#1992=CIRCLE('',#9946,1.25);
#2336=B_SPLINE_CURVE_WITH_KNOTS('',3,(#34596,#34597,#34598,#34599),
 .UNSPECIFIED.,.F.,.F.,(4,4),(-0.00619503390723115,0.),.UNSPECIFIED.);
#2337=B_SPLINE_CURVE_WITH_KNOTS('',3,(#34606,#34607,#34608,#34609,#34610,
#34611,#34612,#34613,#34614,#34615,#34616,#34617,#34618,#34619,#34620,#34621,
#34622,#34623,#34624,#34625,#34626,#34627,#34628,#34629,#34630,#34631,#34632,
#34633,#34634,#34635,#34636,#34637,#34638,#34639,#34640,#34641,#34642,#34643,
#34644,#34645,#34646,#34647,#34648,#34649,#34650,#34651,#34652,#34653,#34654,
#34655,#34656,#34657,#34658,#34659,#34660,#34661,#34662,#34663,#34664,#34665,
#34666,#34667,#34668,#34669,#34670,#34671,#34672,#34673,#34674,#34675,#34676,
#34677,#34678,#34679),.UNSPECIFIED.,.F.,.F.,(4,2,2,2,2,2,2,2,2,2,2,2,2,
2,2,2,2,2,2,2,2,2,2,2,2,2,2,2,2,2,2,2,2,2,2,2,4),(5.60374804517138E-5,0.0237574869632762,
0.0393947601276455,0.0585453864332768,0.08182795489794,0.114860762667679,
0.129204845739769,0.147297192833992,0.17057303225174,0.203467586480588,
0.217878012701244,0.235958253934255,0.259262055153465,0.29253982422056,
0.306780812007485,0.324906546091773,0.348145822827213,0.376378338610298,
0.39336918364381,0.410849344394283,0.451548256241227,0.476499668509328,
0.492967499160127,0.510629733377488,0.537942689233428,0.561233542584866,
0.579498114515359,0.594216460000935,0.626663924529217,0.650241887801689,
0.668490357191975,0.68331215520655,0.714495532592327,0.736570127490707,
0.748116113139686,0.765521137638678,0.786892363085868),.UNSPECIFIED.);
#2338=B_SPLINE_CURVE_WITH_KNOTS('',3,(#34822,#34823,#34824,#34825,#34826,
#34827,#34828,#34829,#34830,#34831,#34832,#34833,#34834,#34835,#34836,#34837,
#34838,#34839,#34840,#34841,#34842,#34843,#34844,#34845,#34846,#34847,#34848,
#34849,#34850,#34851,#34852,#34853,#34854,#34855,#34856,#34857,#34858,#34859,
#34860,#34861,#34862,#34863,#34864,#34865,#34866,#34867,#34868,#34869,#34870,
#34871,#34872,#34873,#34874,#34875,#34876,#34877,#34878,#34879,#34880,#34881,
#34882,#34883,#34884,#34885,#34886,#34887,#34888,#34889,#34890,#34891,#34892,
#34893,#34894,#34895,#34896,#34897,#34898,#34899,#34900,#34901,#34902,#34903,
#34904,#34905,#34906,#34907,#34908,#34909,#34910,#34911,#34912,#34913,#34914,
#34915,#34916,#34917,#34918,#34919,#34920,#34921,#34922,#34923,#34924,#34925,
#34926,#34927,#34928,#34929,#34930,#34931,#34932,#34933,#34934,#34935,#34936,
#34937,#34938,#34939),.UNSPECIFIED.,.F.,.F.,(4,2,2,2,2,2,2,2,2,2,2,2,2,
2,2,2,2,2,2,2,2,2,2,2,2,2,2,2,2,2,2,2,2,2,2,2,2,2,2,2,2,2,2,2,2,2,2,2,2,
2,2,2,2,2,2,2,2,2,4),(4.86308899125306E-5,0.025345822067703,0.0499710023559397,
0.0982392916290599,0.144379179758547,0.169738120416293,0.211164235877253,
0.233786911472833,0.259178954607802,0.300715901245229,0.322405039362481,
0.347812455770367,0.389985850776008,0.410393459018824,0.459653300986646,
0.506189829924729,0.53230871013449,0.574815902384265,0.59800879473142,0.624155748676925,
0.667049786253343,0.689141934513977,0.715301339433927,0.758872833057192,
0.77962771324359,0.830354079494171,0.881187653856567,0.907965106170109,
0.95074336338996,0.97675583503304,1.00356887094136,1.04822229000252,1.09298924554976,
1.11895483964794,1.16660560441434,1.215774402086,1.23658842173518,1.27752886770208,
1.30260580018034,1.32487921810867,1.36439772875352,1.38974130281919,1.43631486645491,
1.48427632141474,1.50456999497759,1.54451517828357,1.56897595594586,1.59069371809725,
1.62925310267272,1.65397444333067,1.69940118356495,1.74620026687915,1.76592586239095,
1.80503271787502,1.8288931679946,1.85039255317872,1.88777689653423,1.92593647559982,
1.97078937517229),.UNSPECIFIED.);
#2339=B_SPLINE_CURVE_WITH_KNOTS('',3,(#34943,#34944,#34945,#34946,#34947,
#34948,#34949,#34950,#34951,#34952,#34953,#34954,#34955,#34956,#34957,#34958,
#34959,#34960,#34961,#34962,#34963,#34964,#34965,#34966,#34967,#34968,#34969,
#34970,#34971,#34972,#34973,#34974,#34975,#34976,#34977,#34978,#34979,#34980,
#34981,#34982,#34983,#34984,#34985,#34986,#34987,#34988,#34989,#34990,#34991,
#34992,#34993,#34994,#34995,#34996,#34997,#34998,#34999,#35000,#35001,#35002,
#35003,#35004,#35005,#35006,#35007,#35008,#35009,#35010,#35011,#35012,#35013,
#35014,#35015,#35016,#35017,#35018,#35019,#35020,#35021,#35022,#35023,#35024,
#35025,#35026,#35027,#35028,#35029,#35030,#35031,#35032,#35033,#35034,#35035,
#35036,#35037,#35038,#35039,#35040,#35041,#35042,#35043,#35044,#35045,#35046,
#35047,#35048,#35049,#35050,#35051,#35052,#35053,#35054,#35055,#35056),
 .UNSPECIFIED.,.F.,.F.,(4,2,2,2,2,2,2,2,2,2,2,2,2,2,2,2,2,2,2,2,2,2,2,2,
2,2,2,2,2,2,2,2,2,2,2,2,2,2,2,2,2,2,2,2,2,2,2,2,2,2,2,2,2,2,2,2,4),(5.9483127789702E-5,
0.0316367019429408,0.0599442114156418,0.0883769919119353,0.116199833618219,
0.148646117264541,0.185649600266805,0.230767737668227,0.2833475209531,0.339441855741448,
0.383998353925252,0.423502762154872,0.462978744712189,0.502190993059282,
0.550924538584899,0.614750411652877,0.690541644647774,0.777537898691589,
0.891899588394075,0.990239042783837,1.0695630442833,1.13517856125268,1.1930368282216,
1.25130241000153,1.30822288488409,1.37470140206806,1.45052897133131,1.54326735518799,
1.65154718908405,1.75982702298013,1.85256540683686,1.92839297610017,1.99487149328411,
2.05179196816666,2.11005754994658,2.16791581691547,2.23353133388489,2.31285533538436,
2.41119478977405,2.5255564794758,2.61255273351889,2.6883439665132,2.75216983958068,
2.80090338510622,2.84011563345335,2.87959161601078,2.91909602424063,2.96365252242471,
3.01974685721341,3.0723266404986,3.11744477790028,3.15444826090276,3.18689454454933,
3.21471738625582,3.2431501667523,3.27145767622518,3.30303409387644),
 .UNSPECIFIED.);
#2340=B_SPLINE_CURVE_WITH_KNOTS('',3,(#35057,#35058,#35059,#35060,#35061,
#35062),.UNSPECIFIED.,.F.,.F.,(4,2,4),(-0.0324107798204044,-0.0161950117464181,
-1.97227469921358E-5),.UNSPECIFIED.);
#2341=B_SPLINE_CURVE_WITH_KNOTS('',3,(#35204,#35205,#35206,#35207,#35208,
#35209,#35210,#35211,#35212,#35213,#35214,#35215,#35216,#35217,#35218,#35219,
#35220,#35221,#35222,#35223,#35224,#35225,#35226,#35227,#35228,#35229,#35230,
#35231,#35232,#35233,#35234,#35235,#35236,#35237,#35238,#35239,#35240,#35241,
#35242,#35243,#35244,#35245,#35246,#35247),.UNSPECIFIED.,.F.,.F.,(4,2,2,
2,2,2,2,2,2,2,2,2,2,2,2,2,2,2,2,2,2,4),(7.68002795625173E-5,0.0286518841616717,
0.0572552412024219,0.105896121009425,0.164583029247044,0.2340740159792,
0.265841679009562,0.301384144553815,0.369456475007765,0.404267289112112,
0.440453098676966,0.503487717030501,0.567113082147453,0.604690173343838,
0.676352451170165,0.748055048385089,0.782538922080911,0.853283578669051,
0.926381914489287,0.997290896804745,1.03897238575266,1.08071694913185),
 .UNSPECIFIED.);
#2342=B_SPLINE_CURVE_WITH_KNOTS('',3,(#35249,#35250,#35251,#35252,#35253,
#35254),.UNSPECIFIED.,.F.,.F.,(4,2,4),(-0.0323546880682321,-0.0162250198953441,
-7.66108474423785E-6),.UNSPECIFIED.);
#2343=B_SPLINE_CURVE_WITH_KNOTS('',3,(#35256,#35257,#35258,#35259,#35260,
#35261,#35262,#35263,#35264,#35265,#35266,#35267,#35268,#35269,#35270,#35271,
#35272,#35273,#35274,#35275,#35276,#35277,#35278,#35279,#35280,#35281,#35282,
#35283,#35284,#35285,#35286,#35287,#35288,#35289,#35290,#35291,#35292,#35293,
#35294,#35295,#35296,#35297,#35298,#35299,#35300,#35301,#35302,#35303,#35304,
#35305,#35306,#35307,#35308,#35309,#35310,#35311,#35312,#35313,#35314,#35315,
#35316,#35317,#35318,#35319,#35320,#35321,#35322,#35323,#35324,#35325,#35326,
#35327,#35328,#35329,#35330,#35331,#35332,#35333,#35334,#35335,#35336,#35337,
#35338,#35339,#35340,#35341,#35342,#35343,#35344,#35345,#35346,#35347,#35348,
#35349,#35350,#35351,#35352,#35353,#35354,#35355,#35356,#35357,#35358,#35359,
#35360,#35361,#35362,#35363,#35364,#35365,#35366,#35367,#35368,#35369),
 .UNSPECIFIED.,.F.,.F.,(4,2,2,2,2,2,2,2,2,2,2,2,2,2,2,2,2,2,2,2,2,2,2,2,
2,2,2,2,2,2,2,2,2,2,2,2,2,2,2,2,2,2,2,2,2,2,2,2,2,2,2,2,2,2,2,2,4),(-3.30330797806971,
-3.2717281475933,-3.24341828644006,-3.21498314385619,-3.18715799073372,
-3.1547090115732,-3.1177024544619,-3.07258056881672,-3.01999641740284,-2.96389742250988,
-2.91933722274118,-2.87982953263513,-2.84035027056288,-2.8011347646109,
-2.75239717048713,-2.68856599500766,-2.61276846556455,-2.52576498420185,
-2.41139379376385,-2.31304616970509,-2.23371557826834,-2.16809461021059,
-2.11023153659623,-2.05196111433268,-1.99503591071289,-1.92855187074577,
-1.85271800201556,-1.75997191380558,-1.65168308443146,-1.54339425505734,
-1.4506481668473,-1.37481429811705,-1.30833025814995,-1.25140505453017,
-1.19313463226664,-1.13527155865229,-1.06965059059451,-0.990319999157752,
-0.891972375099075,-0.777601184661876,-0.690597703299961,-0.614800173857485,
-0.550968998378546,-0.50223140425488,-0.463015898302877,-0.423536636230542,
-0.384028946124274,-0.339468746355297,-0.283369751461995,-0.230785600047816,
-0.18566371440238,-0.148657157290866,-0.116208178130105,-0.0883830250074371,
-0.0599478824233905,-0.0316380212699721,-5.8970516573392E-5),
 .UNSPECIFIED.);
#2344=B_SPLINE_CURVE_WITH_KNOTS('',3,(#35512,#35513,#35514,#35515,#35516,
#35517,#35518,#35519,#35520,#35521,#35522,#35523,#35524,#35525,#35526,#35527,
#35528,#35529,#35530,#35531,#35532,#35533,#35534,#35535,#35536,#35537,#35538,
#35539,#35540,#35541,#35542,#35543,#35544,#35545,#35546,#35547,#35548,#35549,
#35550,#35551,#35552,#35553,#35554,#35555,#35556,#35557,#35558,#35559,#35560,
#35561,#35562,#35563,#35564,#35565,#35566,#35567,#35568,#35569,#35570,#35571,
#35572,#35573,#35574,#35575,#35576,#35577,#35578,#35579,#35580,#35581,#35582,
#35583,#35584,#35585,#35586,#35587,#35588,#35589,#35590,#35591,#35592,#35593,
#35594,#35595,#35596,#35597,#35598,#35599,#35600,#35601,#35602,#35603,#35604,
#35605,#35606,#35607,#35608,#35609,#35610,#35611,#35612,#35613,#35614,#35615,
#35616,#35617,#35618,#35619,#35620,#35621,#35622,#35623,#35624,#35625,#35626,
#35627,#35628,#35629),.UNSPECIFIED.,.F.,.F.,(4,2,2,2,2,2,2,2,2,2,2,2,2,
2,2,2,2,2,2,2,2,2,2,2,2,2,2,2,2,2,2,2,2,2,2,2,2,2,2,2,2,2,2,2,2,2,2,2,2,
2,2,2,2,2,2,2,2,2,4),(4.00512479403123E-5,0.0342074993316949,0.0631190140398426,
0.0925899546592947,0.10920786339202,0.127582223175736,0.157810038290439,
0.173443507766134,0.191832595775175,0.222341299061909,0.237090305071392,
0.272742999074723,0.306561294379606,0.325476646462585,0.356234881757118,
0.373150128431719,0.392087242288704,0.423090526652374,0.439265919840542,
0.458214798157994,0.48966564000899,0.504885740673708,0.541623698931582,
0.576311534812893,0.595787709949363,0.627489287296732,0.644765443703326,
0.664262365513633,0.696256286921859,0.712704551881602,0.732210340892689,
0.768190524101217,0.784517774259878,0.818349961866105,0.860212671232351,
0.916855859608072,0.94190207849065,0.9880100743632,1.01725619500541,1.06975386109676,
1.12552134681956,1.14924716271827,1.19554501871853,1.22399233697437,1.24941480692896,
1.29413044929263,1.32287514891999,1.37597186041185,1.43024555593699,1.45318819332844,
1.49839331258465,1.52607408936872,1.55051417176749,1.59432174380684,1.6222909588055,
1.67460232111634,1.72809366111648,1.75478242650006,1.782350223907),
 .UNSPECIFIED.);
#2345=B_SPLINE_CURVE_WITH_KNOTS('',3,(#35632,#35633,#35634,#35635,#35636,
#35637,#35638,#35639,#35640,#35641,#35642,#35643,#35644,#35645,#35646,#35647,
#35648,#35649,#35650,#35651,#35652,#35653,#35654,#35655,#35656,#35657,#35658,
#35659,#35660,#35661,#35662,#35663,#35664,#35665,#35666,#35667,#35668,#35669,
#35670,#35671,#35672,#35673,#35674,#35675,#35676,#35677,#35678,#35679,#35680,
#35681,#35682,#35683,#35684,#35685,#35686,#35687,#35688,#35689,#35690,#35691,
#35692,#35693,#35694,#35695,#35696,#35697,#35698,#35699,#35700,#35701,#35702,
#35703,#35704,#35705,#35706,#35707,#35708,#35709,#35710,#35711,#35712,#35713,
#35714,#35715,#35716,#35717,#35718,#35719,#35720,#35721,#35722,#35723,#35724,
#35725,#35726,#35727,#35728,#35729,#35730,#35731,#35732,#35733,#35734,#35735,
#35736,#35737,#35738,#35739,#35740,#35741,#35742,#35743,#35744,#35745),
 .UNSPECIFIED.,.F.,.F.,(4,2,2,2,2,2,2,2,2,2,2,2,2,2,2,2,2,2,2,2,2,2,2,2,
2,2,2,2,2,2,2,2,2,2,2,2,2,2,2,2,2,2,2,2,2,2,2,2,2,2,2,2,2,2,2,2,4),(5.94831277841767E-5,
0.0316367019429338,0.0599442114156145,0.0883769919118842,0.116199833618184,
0.148646117264509,0.185649600266781,0.230767737668212,0.283347520953061,
0.339441855741405,0.383998353925216,0.423502762154843,0.462978744712232,
0.5021909930594,0.550924538585036,0.614750411653134,0.690541644648174,0.777537898691899,
0.891899588395087,0.990239042787321,1.0695630442889,1.13517856126005,1.19303682823043,
1.25130241001183,1.3082228848959,1.37470140208164,1.45052897134696,1.54326735520618,
1.65154718910504,1.7598270230039,1.85256540686313,1.92839297612847,1.9948714933142,
2.05179196819826,2.11005754997969,2.16791581695011,2.23353133392122,2.31285533542278,
2.41119478981526,2.52555647952116,2.6125527335676,2.68834396656478,2.75216983963467,
2.80090338516196,2.84011563351046,2.87959161606925,2.91909602430044,2.96365252248596,
3.01974685727651,3.07232664056349,3.11744477796673,3.15444826097047,3.18689454461805,
3.21471738632542,3.24315016682283,3.27145767629665,3.30303488345968),
 .UNSPECIFIED.);
#2346=B_SPLINE_CURVE_WITH_KNOTS('',3,(#35887,#35888,#35889,#35890,#35891,
#35892,#35893,#35894,#35895,#35896,#35897,#35898,#35899,#35900,#35901,#35902,
#35903,#35904,#35905,#35906,#35907,#35908,#35909,#35910,#35911,#35912,#35913,
#35914,#35915,#35916,#35917,#35918,#35919,#35920,#35921,#35922,#35923,#35924,
#35925,#35926,#35927,#35928,#35929,#35930),.UNSPECIFIED.,.F.,.F.,(4,2,2,
2,2,2,2,2,2,2,2,2,2,2,2,2,2,2,2,2,2,4),(4.00913727096806E-5,0.0285826648472843,
0.0571136238949599,0.105754976155757,0.164159095723717,0.23287028670703,
0.264108714287391,0.299243064816363,0.366669064921763,0.40106244750476,
0.436833432270234,0.499315877244998,0.5624507698616,0.599844554878724,0.671009797795569,
0.74195779649287,0.776103848397365,0.84609583637898,0.905678874599204,0.955226346235828,
0.984408120187647,1.01363013542304),.UNSPECIFIED.);
#2347=B_SPLINE_CURVE_WITH_KNOTS('',3,(#35932,#35933,#35934,#35935,#35936,
#35937,#35938,#35939,#35940,#35941,#35942,#35943,#35944,#35945,#35946,#35947,
#35948,#35949,#35950,#35951,#35952,#35953,#35954,#35955,#35956,#35957,#35958,
#35959,#35960,#35961,#35962,#35963,#35964,#35965,#35966,#35967,#35968,#35969,
#35970,#35971,#35972,#35973,#35974,#35975,#35976,#35977,#35978,#35979,#35980,
#35981,#35982,#35983,#35984,#35985,#35986,#35987,#35988,#35989,#35990,#35991,
#35992,#35993,#35994,#35995,#35996,#35997,#35998,#35999,#36000,#36001,#36002,
#36003,#36004,#36005,#36006,#36007,#36008,#36009,#36010,#36011,#36012,#36013,
#36014,#36015,#36016,#36017,#36018,#36019,#36020,#36021,#36022,#36023,#36024,
#36025,#36026,#36027,#36028,#36029,#36030,#36031,#36032,#36033,#36034,#36035,
#36036,#36037,#36038,#36039,#36040,#36041,#36042,#36043,#36044,#36045),
 .UNSPECIFIED.,.F.,.F.,(4,2,2,2,2,2,2,2,2,2,2,2,2,2,2,2,2,2,2,2,2,2,2,2,
2,2,2,2,2,2,2,2,2,2,2,2,2,2,2,2,2,2,2,2,2,2,2,2,2,2,2,2,2,2,2,2,4),(-3.30303488333095,
-3.2714576761704,-3.2431501666988,-3.21471738620362,-3.18689454449838,-3.1544482608533,
-3.11744477785245,-3.07232664045274,-3.01974685716991,-2.96365252238372,
-2.91909602420161,-2.8795916159735,-2.84011563341763,-2.80090338507197,
-2.7521698395482,-2.68834396648255,-2.61255273349043,-2.52555647945005,
-2.41119478975125,-2.31285533536284,-2.23353133386437,-2.1679158168958,
-2.11005754992768,-2.05179196814856,-1.99487149326671,-1.92839297608357,
-1.85256540682122,-1.75982702296562,-1.65154718907099,-1.54326735517636,
-1.45052897132076,-1.37470140205837,-1.30822288487525,-1.25130240999341,
-1.19303682821425,-1.1351785612461,-1.06956304427756,-0.990239042779093,
-0.891899588390449,-0.777537898689057,-0.690541644646066,-0.614750411651893,
-0.550924538584524,-0.502190993059153,-0.462978744712191,-0.423502762154953,
-0.383998353925325,-0.339441855741553,-0.2833475209532,-0.230767737668287,
-0.185649600266819,-0.148646117264527,-0.116199833618222,-0.0883769919119469,
-0.0599442114156555,-0.0316367019429495,-5.94831277973711E-5),
 .UNSPECIFIED.);
#2348=B_SPLINE_CURVE_WITH_KNOTS('',3,(#36188,#36189,#36190,#36191,#36192,
#36193,#36194,#36195,#36196,#36197,#36198,#36199,#36200,#36201,#36202,#36203,
#36204,#36205,#36206,#36207,#36208,#36209,#36210,#36211,#36212,#36213,#36214,
#36215,#36216,#36217,#36218,#36219,#36220,#36221,#36222,#36223,#36224,#36225,
#36226,#36227,#36228,#36229,#36230,#36231,#36232,#36233,#36234,#36235,#36236,
#36237,#36238,#36239,#36240,#36241,#36242,#36243,#36244,#36245,#36246,#36247,
#36248,#36249,#36250,#36251,#36252,#36253,#36254,#36255,#36256,#36257,#36258,
#36259,#36260,#36261,#36262,#36263,#36264,#36265,#36266,#36267,#36268,#36269,
#36270,#36271,#36272,#36273,#36274,#36275,#36276,#36277,#36278,#36279,#36280,
#36281,#36282,#36283,#36284,#36285,#36286,#36287,#36288,#36289,#36290,#36291,
#36292,#36293,#36294,#36295,#36296,#36297,#36298,#36299,#36300,#36301,#36302,
#36303),.UNSPECIFIED.,.F.,.F.,(4,2,2,2,2,2,2,2,2,2,2,2,2,2,2,2,2,2,2,2,
2,2,2,2,2,2,2,2,2,2,2,2,2,2,2,2,2,2,2,2,2,2,2,2,2,2,2,2,2,2,2,2,2,2,2,2,
2,4),(7.6698861386074E-5,0.0253641144717246,0.0500064399592511,0.0982743512795232,
0.144396900860148,0.169754042124687,0.211180728494791,0.233786149641564,
0.259176234358203,0.300717954836437,0.322382035728535,0.347787127447208,
0.389971219681712,0.410351428726807,0.45960754915082,0.506309943404491,
0.532445730872144,0.574944756721432,0.598305762915829,0.624471352988871,
0.667316727791965,0.689646583714177,0.715828165174297,0.759295458119143,
0.780303810677911,0.831065128875955,0.879135074458262,0.931225408976213,
0.984294307137153,1.03610471716903,1.0589297141727,1.10681084378159,1.13379207944822,
1.15842115031494,1.19987899724597,1.22681729209237,1.27791685866676,1.32980038383556,
1.3518321432672,1.39495327783279,1.42141763652019,1.44501563941602,1.48665214587862,
1.5133950465113,1.56269008377841,1.61322123807819,1.63458710491603,1.67669797009781,
1.70246836128344,1.72533098712041,1.76593565513026,1.79198213681011,1.83957602019648,
1.88879043609758,1.90998743513082,1.95065703719148,1.9894885146296,2.02909458871922),
 .UNSPECIFIED.);
#2349=B_SPLINE_CURVE_WITH_KNOTS('',3,(#36306,#36307,#36308,#36309,#36310,
#36311,#36312,#36313,#36314,#36315,#36316,#36317,#36318,#36319,#36320,#36321,
#36322,#36323,#36324,#36325,#36326,#36327,#36328,#36329,#36330,#36331,#36332,
#36333,#36334,#36335,#36336,#36337,#36338,#36339,#36340,#36341,#36342,#36343,
#36344,#36345,#36346,#36347,#36348,#36349,#36350,#36351,#36352,#36353,#36354,
#36355,#36356,#36357,#36358,#36359,#36360,#36361,#36362,#36363,#36364,#36365,
#36366,#36367,#36368,#36369,#36370,#36371,#36372,#36373,#36374,#36375,#36376,
#36377,#36378,#36379,#36380,#36381,#36382,#36383,#36384,#36385,#36386,#36387,
#36388,#36389,#36390,#36391,#36392,#36393,#36394,#36395,#36396,#36397,#36398,
#36399,#36400,#36401,#36402,#36403,#36404,#36405,#36406,#36407,#36408,#36409,
#36410,#36411,#36412,#36413,#36414,#36415,#36416,#36417,#36418,#36419),
 .UNSPECIFIED.,.F.,.F.,(4,2,2,2,2,2,2,2,2,2,2,2,2,2,2,2,2,2,2,2,2,2,2,2,
2,2,2,2,2,2,2,2,2,2,2,2,2,2,2,2,2,2,2,2,2,2,2,2,2,2,2,2,2,2,2,2,4),(5.94831277856605E-5,
0.0316367019428793,0.05994421141559,0.0883769919118876,0.116199833618172,
0.148646117264482,0.185649600266723,0.230767737668117,0.283347520953013,
0.3394418557413,0.383998353924985,0.423502762154574,0.462978744711714,0.502190993058523,
0.550924538583601,0.614750411650344,0.690541644643776,0.777537898685706,
0.891899588386907,0.990239042779026,1.06956304428088,1.13517856125222,1.19303682822286,
1.2513024100045,1.30822288488875,1.37470140207469,1.45052897134019,1.54326735519958,
1.65154718909885,1.75982702299812,1.85256540685745,1.92839297612289,1.99487149330899,
2.05179196819336,2.11005754997495,2.16791581694551,2.23353133391694,2.31285533541884,
2.41119478981148,2.52555647951633,2.61255273356166,2.68834396655795,2.75216983962711,
2.80090338515382,2.84011563350184,2.87959161606014,2.91909602429086,2.96365252247589,
3.0197468572658,3.07232664055213,3.11744477795483,3.15444826095814,3.18689454460537,
3.21471738631243,3.2431501668095,3.27145767628297,3.30303488344564),
 .UNSPECIFIED.);
#2350=B_SPLINE_CURVE_WITH_KNOTS('',3,(#36561,#36562,#36563,#36564,#36565,
#36566,#36567,#36568,#36569,#36570,#36571,#36572,#36573,#36574,#36575,#36576,
#36577,#36578,#36579,#36580,#36581,#36582,#36583,#36584,#36585,#36586,#36587,
#36588,#36589,#36590,#36591,#36592,#36593,#36594,#36595,#36596,#36597,#36598,
#36599,#36600,#36601,#36602,#36603,#36604),.UNSPECIFIED.,.F.,.F.,(4,2,2,
2,2,2,2,2,2,2,2,2,2,2,2,2,2,2,2,2,2,4),(7.68002794356204E-5,0.0287777493485966,
0.0575152407768132,0.106155181951881,0.165514264466246,0.236890561238667,
0.269992967924706,0.342297528574894,0.41385280051629,0.451122206439615,
0.514413059508262,0.57781052913482,0.614649187845566,0.65011886251284,0.714826966817939,
0.751033279270129,0.78582652402978,0.856066631699381,0.929434885992276,
1.00126014577657,1.04560443038775,1.08990031448452),.UNSPECIFIED.);
#2351=B_SPLINE_CURVE_WITH_KNOTS('',3,(#36606,#36607,#36608,#36609,#36610,
#36611,#36612,#36613,#36614,#36615,#36616,#36617,#36618,#36619,#36620,#36621,
#36622,#36623,#36624,#36625,#36626,#36627,#36628,#36629,#36630,#36631,#36632,
#36633,#36634,#36635,#36636,#36637,#36638,#36639,#36640,#36641,#36642,#36643,
#36644,#36645,#36646,#36647,#36648,#36649,#36650,#36651,#36652,#36653,#36654,
#36655,#36656,#36657,#36658,#36659,#36660,#36661,#36662,#36663,#36664,#36665,
#36666,#36667,#36668,#36669,#36670,#36671,#36672,#36673,#36674,#36675,#36676,
#36677,#36678,#36679,#36680,#36681,#36682,#36683,#36684,#36685,#36686,#36687,
#36688,#36689,#36690,#36691,#36692,#36693,#36694,#36695,#36696,#36697,#36698,
#36699,#36700,#36701,#36702,#36703,#36704,#36705,#36706,#36707,#36708,#36709,
#36710,#36711,#36712,#36713,#36714,#36715,#36716,#36717,#36718,#36719),
 .UNSPECIFIED.,.F.,.F.,(4,2,2,2,2,2,2,2,2,2,2,2,2,2,2,2,2,2,2,2,2,2,2,2,
2,2,2,2,2,2,2,2,2,2,2,2,2,2,2,2,2,2,2,2,2,2,2,2,2,2,2,2,2,2,2,2,4),(-3.30303488335142,
-3.27145767619062,-3.24315016671873,-3.21471738622325,-3.18689454451777,
-3.1544482608724,-3.11744477787123,-3.07232664047114,-3.01974685718777,
-2.96365252240111,-2.91909602421871,-2.87959161599026,-2.84011563343427,
-2.8009033850886,-2.75216983956494,-2.68834396650006,-2.61255273350884,
-2.52555647946945,-2.41119478977154,-2.31285533538221,-2.23353133388263,
-2.16791581691316,-2.11005754994417,-2.05179196816421,-1.99487149328159,
-1.92839297609755,-1.85256540683422,-1.75982702297748,-1.65154718908131,
-1.54326735518514,-1.45052897132847,-1.3747014020652,-1.30822288488101,
-1.25130240999827,-1.19303682821834,-1.13517856124945,-1.06956304427989,
-0.990239042780272,-0.891899588390439,-0.777537898688797,-0.690541644645899,
-0.614750411651723,-0.550924538584345,-0.502190993058996,-0.462978744712068,
-0.423502762154865,-0.38399835392525,-0.339441855741458,-0.283347520953114,
-0.230767737668244,-0.185649600266803,-0.148646117264526,-0.1161998336182,
-0.0883769919119069,-0.0599442114156348,-0.0316367019429531,-5.9483127788608E-5),
 .UNSPECIFIED.);
#2352=B_SPLINE_CURVE_WITH_KNOTS('',3,(#36862,#36863,#36864,#36865,#36866,
#36867,#36868,#36869,#36870,#36871,#36872,#36873,#36874,#36875,#36876,#36877,
#36878,#36879,#36880,#36881,#36882,#36883,#36884,#36885,#36886,#36887,#36888,
#36889,#36890,#36891,#36892,#36893,#36894,#36895,#36896,#36897,#36898,#36899,
#36900,#36901,#36902,#36903,#36904,#36905,#36906,#36907,#36908,#36909,#36910,
#36911,#36912,#36913,#36914,#36915,#36916,#36917,#36918,#36919,#36920,#36921,
#36922,#36923,#36924,#36925,#36926,#36927,#36928,#36929,#36930,#36931,#36932,
#36933,#36934,#36935,#36936,#36937,#36938,#36939,#36940,#36941,#36942,#36943,
#36944,#36945,#36946,#36947,#36948,#36949,#36950,#36951,#36952,#36953,#36954,
#36955,#36956,#36957,#36958,#36959,#36960,#36961,#36962,#36963,#36964,#36965,
#36966,#36967,#36968,#36969,#36970,#36971,#36972,#36973,#36974,#36975,#36976,
#36977,#36978,#36979,#36980,#36981),.UNSPECIFIED.,.F.,.F.,(4,2,2,2,2,2,
2,2,2,2,2,2,2,2,2,2,2,2,2,2,2,2,2,2,2,2,2,2,2,2,2,2,2,2,2,2,2,2,2,2,2,2,
2,2,2,2,2,2,2,2,2,2,2,2,2,2,2,2,2,4),(4.0051248426754E-5,0.0342064761731191,
0.0631175860317564,0.0925901191772445,0.109204719988194,0.127579480307699,
0.157809813748144,0.17343819129591,0.191827601357051,0.222340229122194,
0.237083590647375,0.272737092201538,0.306595004693092,0.325515137613875,
0.356273057630785,0.373228961128414,0.392171250118677,0.423164564769037,
0.439399493407582,0.458354387574874,0.489781306563202,0.505067114058951,
0.541814948000685,0.576121524170463,0.595585940952813,0.627358776285785,
0.644284692241037,0.663765570017339,0.695920050526438,0.705048117245191,
0.742539832779656,0.761952372673167,0.779181946526965,0.809783461597958,
0.829402822794386,0.865434106670318,0.902572827052802,0.918291063237675,
0.949218481843105,0.968159729435232,0.984979059868996,1.01483166754968,
1.03397445379827,1.06914541132536,1.10537577037675,1.12070664338408,1.15088038093645,
1.16935823240658,1.18576522071897,1.21489233668997,1.23356698054014,1.26788472670369,
1.30323601192855,1.31813615732139,1.34767715894864,1.36570095301968,1.38194088462811,
1.41018067834471,1.43900555726746,1.47288628947006),.UNSPECIFIED.);
#2353=B_SPLINE_CURVE_WITH_KNOTS('',3,(#36984,#36985,#36986,#36987,#36988,
#36989,#36990,#36991,#36992,#36993,#36994,#36995,#36996,#36997,#36998,#36999,
#37000,#37001,#37002,#37003,#37004,#37005,#37006,#37007,#37008,#37009,#37010,
#37011,#37012,#37013,#37014,#37015,#37016,#37017,#37018,#37019,#37020,#37021,
#37022,#37023,#37024,#37025,#37026,#37027,#37028,#37029,#37030,#37031,#37032,
#37033,#37034,#37035,#37036,#37037,#37038,#37039,#37040,#37041,#37042,#37043,
#37044,#37045,#37046,#37047,#37048,#37049,#37050,#37051,#37052,#37053,#37054,
#37055,#37056,#37057,#37058,#37059,#37060,#37061,#37062,#37063,#37064,#37065,
#37066,#37067,#37068,#37069,#37070,#37071,#37072,#37073,#37074,#37075,#37076,
#37077,#37078,#37079,#37080,#37081,#37082,#37083,#37084,#37085,#37086,#37087,
#37088,#37089,#37090,#37091,#37092,#37093,#37094,#37095,#37096,#37097),
 .UNSPECIFIED.,.F.,.F.,(4,2,2,2,2,2,2,2,2,2,2,2,2,2,2,2,2,2,2,2,2,2,2,2,
2,2,2,2,2,2,2,2,2,2,2,2,2,2,2,2,2,2,2,2,2,2,2,2,2,2,2,2,2,2,2,2,4),(5.94831277915571E-5,
0.0316367019429085,0.0599442114156052,0.0883769919118883,0.116199833618177,
0.148646117264504,0.185649600266749,0.230767737668142,0.283347520952984,
0.339441855741318,0.383998353925107,0.423502762154725,0.462978744712151,
0.502190993059384,0.550924538585165,0.614750411653649,0.690541644649133,
0.777537898693328,0.891899588396945,0.99023904278927,1.069563044291,1.1351785612623,
1.19303682823281,1.25130241001434,1.30822288489854,1.37470140208444,1.45052897134983,
1.54326735520912,1.65154718910821,1.7598270230073,1.85256540686662,1.92839297613204,
1.99487149331798,2.05179196820223,2.11005754998372,2.1679158169542,2.23353133392551,
2.31285533542727,2.41119478981956,2.52555647952189,2.61255273356476,2.68834396655906,
2.75216983962656,2.80090338515208,2.84011563349924,2.87959161605671,2.9190960242866,
2.96365252247078,3.01974685725952,3.07232664054471,3.11744477794648,3.15444826094903,
3.18689454459555,3.21471738630203,3.24315016679852,3.27145767627144,3.30303488343336),
 .UNSPECIFIED.);
#2354=B_SPLINE_CURVE_WITH_KNOTS('',3,(#37239,#37240,#37241,#37242,#37243,
#37244,#37245,#37246,#37247,#37248,#37249,#37250,#37251,#37252,#37253,#37254,
#37255,#37256,#37257,#37258,#37259,#37260,#37261,#37262,#37263,#37264,#37265,
#37266,#37267,#37268,#37269,#37270,#37271,#37272,#37273,#37274,#37275,#37276,
#37277,#37278,#37279,#37280,#37281,#37282,#37283,#37284),.UNSPECIFIED.,
 .F.,.F.,(4,2,2,2,2,2,2,2,2,2,2,2,2,2,2,2,2,2,2,2,2,2,4),(4.00913729709594E-5,
0.0255224163009285,0.0506628404716964,0.0675638222751209,0.115459262979836,
0.139046414941069,0.163661762441637,0.209957952667681,0.234239146303838,
0.282831016253925,0.306172802073132,0.357736918849856,0.385227490793403,
0.411763916933472,0.463568750602167,0.51847542001774,0.571406026873824,
0.625515387332744,0.679017081593755,0.731021185439546,0.784186981559513,
0.809198205683984,0.834926852586118),.UNSPECIFIED.);
#2355=B_SPLINE_CURVE_WITH_KNOTS('',3,(#37286,#37287,#37288,#37289,#37290,
#37291,#37292,#37293,#37294,#37295,#37296,#37297,#37298,#37299,#37300,#37301,
#37302,#37303,#37304,#37305,#37306,#37307,#37308,#37309,#37310,#37311,#37312,
#37313,#37314,#37315,#37316,#37317,#37318,#37319,#37320,#37321,#37322,#37323,
#37324,#37325,#37326,#37327,#37328,#37329,#37330,#37331,#37332,#37333,#37334,
#37335,#37336,#37337,#37338,#37339,#37340,#37341,#37342,#37343,#37344,#37345,
#37346,#37347,#37348,#37349,#37350,#37351,#37352,#37353,#37354,#37355,#37356,
#37357,#37358,#37359,#37360,#37361,#37362,#37363,#37364,#37365,#37366,#37367,
#37368,#37369,#37370,#37371,#37372,#37373,#37374,#37375,#37376,#37377,#37378,
#37379,#37380,#37381,#37382,#37383,#37384,#37385,#37386,#37387,#37388,#37389,
#37390,#37391,#37392,#37393,#37394,#37395,#37396,#37397,#37398,#37399),
 .UNSPECIFIED.,.F.,.F.,(4,2,2,2,2,2,2,2,2,2,2,2,2,2,2,2,2,2,2,2,2,2,2,2,
2,2,2,2,2,2,2,2,2,2,2,2,2,2,2,2,2,2,2,2,2,2,2,2,2,2,2,2,2,2,2,2,4),(-3.30303488340775,
-3.27145767624626,-3.24315016677379,-3.21471738627774,-3.18689454457167,
-3.15444826092561,-3.11744477792366,-3.07232664052264,-3.01974685723822,
-2.96365252245034,-2.91909602426692,-2.87959161603762,-2.84011563348052,
-2.80090338513361,-2.75216983960824,-2.68834396654031,-2.61255273354548,
-2.52555647950205,-2.4111947897994,-2.31285533540785,-2.23353133390672,
-2.16791581693593,-2.11005754996586,-2.05179196818478,-1.99487149330102,
-1.92839297611563,-1.85256540685082,-1.75982702299225,-1.65154718909399,
-1.54326735519573,-1.45052897133712,-1.37470140207228,-1.30822288488685,
-1.25130241000305,-1.19303682822201,-1.13517856125197,-1.06956304428115,
-0.990239042780001,-0.891899588388456,-0.777537898686937,-0.690541644644683,
-0.614750411650919,-0.550924538583876,-0.502190993058717,-0.462978744711846,
-0.423502762154673,-0.383998353925072,-0.339441855741231,-0.283347520952903,
-0.230767737668099,-0.18564960026667,-0.148646117264394,-0.11619983361811,
-0.0883769919118416,-0.0599442114155554,-0.0316367019428531,-5.94831277862293E-5),
 .UNSPECIFIED.);
#2356=B_SPLINE_CURVE_WITH_KNOTS('',3,(#37542,#37543,#37544,#37545,#37546,
#37547,#37548,#37549,#37550,#37551,#37552,#37553,#37554,#37555,#37556,#37557,
#37558,#37559,#37560,#37561,#37562,#37563,#37564,#37565,#37566,#37567,#37568,
#37569,#37570,#37571,#37572,#37573,#37574,#37575,#37576,#37577,#37578,#37579,
#37580,#37581,#37582,#37583,#37584,#37585,#37586,#37587,#37588,#37589,#37590,
#37591,#37592,#37593,#37594,#37595,#37596,#37597,#37598,#37599,#37600,#37601,
#37602,#37603,#37604,#37605,#37606,#37607,#37608,#37609,#37610,#37611,#37612,
#37613,#37614,#37615,#37616,#37617,#37618,#37619,#37620,#37621,#37622,#37623,
#37624,#37625,#37626,#37627,#37628,#37629,#37630,#37631,#37632,#37633,#37634,
#37635,#37636,#37637,#37638,#37639,#37640,#37641,#37642,#37643,#37644,#37645,
#37646,#37647,#37648,#37649,#37650,#37651,#37652,#37653,#37654,#37655),
 .UNSPECIFIED.,.F.,.F.,(4,2,2,2,2,2,2,2,2,2,2,2,2,2,2,2,2,2,2,2,2,2,2,2,
2,2,2,2,2,2,2,2,2,2,2,2,2,2,2,2,2,2,2,2,2,2,2,2,2,2,2,2,2,2,2,2,4),(7.66667039813964E-5,
0.0343822570135638,0.0637613764833492,0.094199059661914,0.11047498602631,
0.12930195093692,0.160694844424638,0.175767290920764,0.212272713042494,
0.246749040585014,0.266102424593384,0.297603712513506,0.314777680002683,
0.334151582098445,0.365942900382604,0.382292601247752,0.401675502261559,
0.433971521537711,0.449330739706536,0.486917336364386,0.524517255803242,
0.562773220070549,0.602183403859061,0.639402116718175,0.679257550990186,
0.714264232281347,0.728825399703001,0.748794148989186,0.788083652792557,
0.804416787023143,0.837512446363635,0.857536416517704,0.874909500560555,
0.906807390286947,0.927057081979138,0.96346744856945,1.00205549387321,1.01846649219655,
1.05050898548041,1.07019271009353,1.08777765812595,1.11872228788031,1.13861213663028,
1.17533033601046,1.21288546357669,1.2287576670532,1.26006322092035,1.27921565891491,
1.29619753766833,1.32638200672507,1.34573993774699,1.38109560231843,1.41768017926844,
1.43343946269429,1.46366967964336,1.49253830141179,1.52198322200782),
 .UNSPECIFIED.);
#2357=B_SPLINE_CURVE_WITH_KNOTS('',3,(#37658,#37659,#37660,#37661,#37662,
#37663,#37664,#37665,#37666,#37667,#37668,#37669,#37670,#37671,#37672,#37673,
#37674,#37675,#37676,#37677,#37678,#37679,#37680,#37681,#37682,#37683,#37684,
#37685,#37686,#37687,#37688,#37689,#37690,#37691,#37692,#37693,#37694,#37695,
#37696,#37697,#37698,#37699,#37700,#37701,#37702,#37703,#37704,#37705,#37706,
#37707,#37708,#37709,#37710,#37711,#37712,#37713,#37714,#37715,#37716,#37717,
#37718,#37719,#37720,#37721,#37722,#37723,#37724,#37725,#37726,#37727,#37728,
#37729,#37730,#37731,#37732,#37733,#37734,#37735,#37736,#37737,#37738,#37739,
#37740,#37741,#37742,#37743,#37744,#37745,#37746,#37747,#37748,#37749,#37750,
#37751,#37752,#37753,#37754,#37755,#37756,#37757,#37758,#37759,#37760,#37761,
#37762,#37763,#37764,#37765,#37766,#37767,#37768,#37769,#37770,#37771),
 .UNSPECIFIED.,.F.,.F.,(4,2,2,2,2,2,2,2,2,2,2,2,2,2,2,2,2,2,2,2,2,2,2,2,
2,2,2,2,2,2,2,2,2,2,2,2,2,2,2,2,2,2,2,2,2,2,2,2,2,2,2,2,2,2,2,2,4),(4.94894020204337E-5,
0.0316314923673886,0.0599439530140688,0.0883817065950881,0.116209414703643,
0.148661373423333,0.185671328583896,0.230797357451291,0.28338633729426,
0.339490483359371,0.384054774774603,0.423566092591166,0.463048979763645,
0.502268086597013,0.551010155947864,0.614847192590904,0.690651681982884,
0.777663152257347,0.892044844589388,0.990401499212093,1.06973937501396,
1.1353663685795,1.19323475534907,1.25151052817173,1.30844095882898,1.37493110355368,
1.45077193556961,1.54352653999428,1.65182531276284,1.76012408553141,1.85287868995618,
1.92871952197216,1.99520966669679,2.05214009735399,2.11041587017671,2.16828425694633,
2.23391125051183,2.31324912631368,2.41160578093638,2.52598747326715,2.61299894354021,
2.68880343293115,2.75264046957332,2.80138253892366,2.84060164575671,2.88008453292891,
2.91959585074528,2.9641601421603,3.0202642882251,3.07285326806776,3.11797929693492,
3.15498925209528,3.18744121081486,3.21526891892331,3.24370667250417,3.27201913315071,
3.3036018633784),.UNSPECIFIED.);
#2358=B_SPLINE_CURVE_WITH_KNOTS('',3,(#37913,#37914,#37915,#37916,#37917,
#37918,#37919,#37920,#37921,#37922,#37923,#37924,#37925,#37926,#37927,#37928,
#37929,#37930,#37931,#37932,#37933,#37934,#37935,#37936,#37937,#37938,#37939,
#37940,#37941,#37942,#37943,#37944,#37945,#37946,#37947,#37948,#37949,#37950,
#37951,#37952,#37953,#37954,#37955,#37956),.UNSPECIFIED.,.F.,.F.,(4,2,2,
2,2,2,2,2,2,2,2,2,2,2,2,2,2,2,2,2,2,4),(6.66069981017537E-5,0.0257114809926198,
0.0510662466252859,0.0996676030717527,0.136326971149926,0.165900839293608,
0.203535749058119,0.253888941376676,0.278755475981711,0.304647335999316,
0.354681677934622,0.366819850806871,0.413020641579737,0.438815758028813,
0.463596322699854,0.5135634301164,0.550658857331488,0.579591342752336,0.614849419992928,
0.659933842154479,0.683662933835049,0.707689106989728),.UNSPECIFIED.);
#2359=B_SPLINE_CURVE_WITH_KNOTS('',3,(#37958,#37959,#37960,#37961,#37962,
#37963,#37964,#37965,#37966,#37967,#37968,#37969,#37970,#37971,#37972,#37973,
#37974,#37975,#37976,#37977,#37978,#37979,#37980,#37981,#37982,#37983,#37984,
#37985,#37986,#37987,#37988,#37989,#37990,#37991,#37992,#37993,#37994,#37995,
#37996,#37997,#37998,#37999,#38000,#38001,#38002,#38003,#38004,#38005,#38006,
#38007,#38008,#38009,#38010,#38011,#38012,#38013,#38014,#38015,#38016,#38017,
#38018,#38019,#38020,#38021,#38022,#38023,#38024,#38025,#38026,#38027,#38028,
#38029,#38030,#38031,#38032,#38033,#38034,#38035,#38036,#38037,#38038,#38039,
#38040,#38041,#38042,#38043,#38044,#38045,#38046,#38047,#38048,#38049,#38050,
#38051,#38052,#38053,#38054,#38055,#38056,#38057,#38058,#38059,#38060,#38061,
#38062,#38063,#38064,#38065,#38066,#38067,#38068,#38069,#38070,#38071),
 .UNSPECIFIED.,.F.,.F.,(4,2,2,2,2,2,2,2,2,2,2,2,2,2,2,2,2,2,2,2,2,2,2,2,
2,2,2,2,2,2,2,2,2,2,2,2,2,2,2,2,2,2,2,2,2,2,2,2,2,2,2,2,2,2,2,2,4),(-3.30303418879995,
-3.27145767624004,-3.24315016676724,-3.21471738627084,-3.18689454456452,
-3.15444826091816,-3.11744477791575,-3.07232664051416,-3.01974685722908,
-2.96365252244057,-2.91909602425668,-2.87959161602693,-2.84011563346943,
-2.80090338512216,-2.75216983959636,-2.68834396652805,-2.61255273353278,
-2.52555647948861,-2.4111947897857,-2.31285533539524,-2.23353133389494,
-2.16791581692479,-2.11005754995539,-2.051791968175,-1.99487149329178,-1.92839297610701,
-1.85256540684313,-1.75982702298575,-1.65154718908867,-1.54326735519157,
-1.45052897133412,-1.37470140207019,-1.30822288488551,-1.25130241000235,
-1.19303682822191,-1.13517856125246,-1.06956304428236,-0.990239042782088,
-0.891899588391592,-0.777537898689638,-0.690541644646586,-0.614750411652103,
-0.550924538584464,-0.502190993059046,-0.462978744712006,-0.423502762154696,
-0.383998353925075,-0.339441855741319,-0.283347520953013,-0.230767737668155,
-0.185649600266737,-0.148646117264472,-0.116199833618172,-0.0883769919118998,
-0.0599442114156078,-0.0316367019429014,-5.94831277983696E-5),
 .UNSPECIFIED.);
#2360=B_SPLINE_CURVE_WITH_KNOTS('',3,(#38214,#38215,#38216,#38217,#38218,
#38219,#38220,#38221,#38222,#38223,#38224,#38225,#38226,#38227,#38228,#38229,
#38230,#38231,#38232,#38233,#38234,#38235,#38236,#38237,#38238,#38239,#38240,
#38241,#38242,#38243,#38244,#38245,#38246,#38247,#38248,#38249,#38250,#38251,
#38252,#38253,#38254,#38255,#38256,#38257,#38258,#38259,#38260,#38261,#38262,
#38263,#38264,#38265,#38266,#38267,#38268,#38269,#38270,#38271,#38272,#38273,
#38274,#38275,#38276,#38277,#38278,#38279,#38280,#38281,#38282,#38283,#38284,
#38285,#38286,#38287,#38288,#38289,#38290,#38291,#38292,#38293,#38294,#38295,
#38296,#38297,#38298,#38299,#38300,#38301,#38302,#38303,#38304,#38305,#38306,
#38307,#38308,#38309,#38310,#38311),.UNSPECIFIED.,.F.,.F.,(4,2,2,2,2,2,
2,2,2,2,2,2,2,2,2,2,2,2,2,2,2,2,2,2,2,2,2,2,2,2,2,2,2,2,2,2,2,2,2,2,2,2,
2,2,2,2,2,2,4),(6.66228729229431E-5,0.0225476992818617,0.0442896901705524,
0.0591711937710805,0.104450063255743,0.134337450528061,0.15508110800453,
0.175912746947078,0.196048962747963,0.22351804937836,0.244541747565316,
0.27188301377946,0.294089951435767,0.316542973695342,0.336496597886517,
0.343517373123556,0.352726143951829,0.362515304186564,0.370161375413743,
0.377077685058301,0.387290271145451,0.404658951155952,0.423205010581693,
0.44195805752164,0.464515615946775,0.480911330011926,0.503550191581656,
0.527051081788821,0.54294486906486,0.578085257945204,0.599501605476778,
0.619019564203727,0.639300414853292,0.668132715757297,0.696074102483784,
0.717738403103488,0.728524348566846,0.739821161329477,0.750855444682612,
0.764498264544529,0.779141577748808,0.790310292685832,0.80307257247109,
0.818064081166539,0.837091745472003,0.848407593361733,0.859726051869667,
0.873284898580614,0.886799076579605),.UNSPECIFIED.);
#2361=B_SPLINE_CURVE_WITH_KNOTS('',3,(#38313,#38314,#38315,#38316,#38317,
#38318,#38319,#38320,#38321,#38322,#38323,#38324,#38325,#38326,#38327,#38328,
#38329,#38330,#38331,#38332,#38333,#38334,#38335,#38336,#38337,#38338),
 .UNSPECIFIED.,.F.,.F.,(4,2,2,2,2,2,2,2,2,2,2,2,4),(-0.349172101168083,
-0.30613774295609,-0.268493936474377,-0.249567397365854,-0.230355139827257,
-0.209628324386868,-0.191150939236384,-0.149007240432192,-0.117442311272233,
-0.0928116777959336,-0.0725064298073674,-0.0362198133233974,-2.55123851692849E-6),
 .UNSPECIFIED.);
#2362=B_SPLINE_CURVE_WITH_KNOTS('',3,(#38340,#38341,#38342,#38343,#38344,
#38345,#38346,#38347,#38348,#38349,#38350,#38351,#38352,#38353,#38354,#38355),
 .UNSPECIFIED.,.F.,.F.,(4,2,2,2,2,2,2,4),(-0.211885266973906,-0.196996598406475,
-0.181637026962749,-0.152787959014052,-0.117981173952917,-0.0783349442213858,
-0.0396812097311858,-3.20864029342772E-5),.UNSPECIFIED.);
#2363=B_SPLINE_CURVE_WITH_KNOTS('',3,(#38356,#38357,#38358,#38359,#38360,
#38361,#38362,#38363,#38364,#38365,#38366,#38367,#38368,#38369,#38370,#38371,
#38372,#38373,#38374,#38375,#38376,#38377,#38378,#38379,#38380,#38381,#38382,
#38383,#38384,#38385,#38386,#38387,#38388,#38389,#38390,#38391,#38392,#38393,
#38394,#38395,#38396,#38397,#38398,#38399,#38400,#38401,#38402,#38403,#38404,
#38405,#38406,#38407,#38408,#38409,#38410,#38411,#38412,#38413,#38414,#38415,
#38416,#38417,#38418,#38419,#38420,#38421,#38422,#38423,#38424,#38425,#38426,
#38427,#38428,#38429,#38430,#38431,#38432,#38433,#38434,#38435,#38436,#38437,
#38438,#38439,#38440,#38441,#38442,#38443,#38444,#38445,#38446,#38447,#38448,
#38449,#38450,#38451,#38452,#38453,#38454,#38455,#38456,#38457,#38458,#38459,
#38460,#38461,#38462,#38463,#38464,#38465,#38466,#38467,#38468,#38469,#38470,
#38471,#38472,#38473,#38474,#38475,#38476,#38477,#38478,#38479,#38480,#38481,
#38482,#38483,#38484,#38485,#38486,#38487,#38488,#38489,#38490,#38491,#38492,
#38493,#38494,#38495,#38496,#38497,#38498,#38499,#38500,#38501,#38502,#38503,
#38504,#38505,#38506,#38507,#38508,#38509,#38510,#38511,#38512,#38513,#38514,
#38515,#38516,#38517,#38518,#38519,#38520,#38521,#38522,#38523,#38524,#38525,
#38526,#38527,#38528,#38529,#38530,#38531,#38532,#38533,#38534,#38535,#38536,
#38537,#38538,#38539,#38540,#38541,#38542,#38543,#38544,#38545,#38546,#38547,
#38548,#38549,#38550,#38551),.UNSPECIFIED.,.F.,.F.,(4,2,2,2,2,2,2,2,2,2,
2,2,2,2,2,2,2,2,2,2,2,2,2,2,2,2,2,2,2,2,2,2,2,2,2,2,2,2,2,2,2,2,2,2,2,2,
2,2,2,2,2,2,2,2,2,2,2,2,2,2,2,2,2,2,2,2,2,2,2,2,2,2,2,2,2,2,2,2,2,2,2,2,
2,2,2,2,2,2,2,2,2,2,2,2,2,2,2,4),(0.000122652419997842,0.0276557142056561,
0.0548465532433756,0.0813319888533599,0.103445171604568,0.115816501830552,
0.122915814684137,0.135255605630576,0.140319560704333,0.14744633344284,
0.154191750101741,0.161382504212589,0.164946904823102,0.174356942050893,
0.17879527499184,0.184043768051259,0.188461477252554,0.192304551229565,
0.199594960441583,0.203034163875464,0.208670143610847,0.214717929164853,
0.222418730236186,0.225925018803337,0.235374252774503,0.239404309627104,
0.245544517663036,0.249502270007744,0.255205166531046,0.261251781907313,
0.266952340527656,0.272380500394639,0.281162721812626,0.289183682462574,
0.294722045602088,0.308694051842449,0.322765635411611,0.336572747895524,
0.344022753864475,0.356156366722283,0.364519285824678,0.370402346202873,
0.379037801767753,0.385001889576374,0.389757098712872,0.394272191758983,
0.40215252660916,0.407307790504656,0.410686758612044,0.417787992809562,
0.423400397500185,0.429613164782095,0.435329819529971,0.441713614987118,
0.444955924424928,0.451603094281047,0.456621478459793,0.464872671209544,
0.469666978601246,0.475175342349373,0.482934363353185,0.491739297739543,
0.496324515501596,0.503324561292956,0.516467205564147,0.52342352311931,
0.537228833926293,0.544092313574322,0.55745794089263,0.571067445650911,
0.5853212861971,0.590748042360905,0.595676057995859,0.602648937952715,0.608041695946353,
0.612019344091071,0.618008163606214,0.621609774966156,0.629401051040114,
0.633758561165747,0.640694591247517,0.644435352788924,0.64916605878867,
0.653981150987846,0.660154578341861,0.667158608840516,0.672437143489509,
0.678316991527251,0.68272216058364,0.69232166733335,0.696306656105387,0.702984169138243,
0.71012576320964,0.71727759998328,0.722900094763324,0.731656752166302,0.742171028011585,
0.755579756858543),.UNSPECIFIED.);
#2364=B_SPLINE_CURVE_WITH_KNOTS('',3,(#38693,#38694,#38695,#38696,#38697,
#38698,#38699,#38700,#38701,#38702,#38703,#38704,#38705,#38706,#38707,#38708,
#38709,#38710,#38711,#38712,#38713,#38714,#38715,#38716,#38717,#38718,#38719,
#38720,#38721,#38722,#38723,#38724,#38725,#38726,#38727,#38728,#38729,#38730,
#38731,#38732,#38733,#38734,#38735,#38736,#38737,#38738,#38739,#38740,#38741,
#38742,#38743,#38744,#38745,#38746,#38747,#38748,#38749,#38750,#38751,#38752,
#38753,#38754,#38755,#38756,#38757,#38758,#38759,#38760,#38761,#38762,#38763,
#38764,#38765,#38766,#38767,#38768,#38769,#38770,#38771,#38772,#38773,#38774,
#38775,#38776,#38777,#38778,#38779,#38780,#38781,#38782,#38783,#38784,#38785,
#38786,#38787,#38788,#38789,#38790,#38791,#38792,#38793,#38794,#38795,#38796,
#38797,#38798,#38799,#38800,#38801,#38802,#38803,#38804,#38805,#38806,#38807,
#38808,#38809,#38810,#38811,#38812,#38813,#38814,#38815,#38816,#38817,#38818,
#38819,#38820,#38821,#38822,#38823,#38824,#38825,#38826,#38827,#38828,#38829,
#38830,#38831,#38832,#38833,#38834,#38835,#38836,#38837,#38838,#38839,#38840,
#38841,#38842,#38843,#38844,#38845,#38846,#38847,#38848,#38849,#38850,#38851,
#38852,#38853,#38854),.UNSPECIFIED.,.F.,.F.,(4,2,2,2,2,2,2,2,2,2,2,2,2,
2,2,2,2,2,2,2,2,2,2,2,2,2,2,2,2,2,2,2,2,2,2,2,2,2,2,2,2,2,2,2,2,2,2,2,2,
2,2,2,2,2,2,2,2,2,2,2,2,2,2,2,2,2,2,2,2,2,2,2,2,2,2,2,2,2,2,2,4),(-4.07132161405629,
-4.00254204476235,-3.94917628400674,-3.86795081813188,-3.79332164531464,
-3.74072831013231,-3.68013965831211,-3.62552568967953,-3.56801317961879,
-3.52417666717784,-3.44856266284831,-3.40540846135397,-3.32669109777936,
-3.23487237385695,-3.13850440833536,-3.08645769787531,-3.05261484298801,
-2.96563410991923,-2.91656098005686,-2.86751731174139,-2.75489628469704,
-2.63126531072298,-2.513177710874,-2.38918165075726,-2.29341735780137,-2.23088977537095,
-2.19395315434401,-2.15469465057632,-2.09719660594431,-2.06819801622426,
-2.02951834482612,-1.98366456753363,-1.95300592485793,-1.91770365730641,
-1.88548048679027,-1.85188758413217,-1.82623395367009,-1.79604688936397,
-1.76674581938805,-1.7355621004847,-1.70471705422878,-1.66878201729108,
-1.64442858220071,-1.60296803607516,-1.56376092859971,-1.53634240109056,
-1.47445473086875,-1.37923891142332,-1.29995519569865,-1.18058216401935,
-1.06184737759313,-0.948750431355718,-0.863398080645727,-0.798764826289785,
-0.776013241654084,-0.742153628487462,-0.708920662731534,-0.672900978419029,
-0.647342028991442,-0.59047469202054,-0.565959615586883,-0.532894643003156,
-0.498221639823335,-0.474840364742629,-0.446916707542781,-0.420111565412746,
-0.392838466973543,-0.361655184901136,-0.336878232420111,-0.317827718572486,
-0.28935652060261,-0.247826078558967,-0.223680401877466,-0.186986046828687,
-0.144119788584455,-0.131147823980291,-0.110060597497317,-0.0909381017436983,
-0.0676719087717867,-0.0340691893263995,-4.90219995722183E-5),
 .UNSPECIFIED.);
#2365=B_SPLINE_CURVE_WITH_KNOTS('',3,(#38855,#38856,#38857,#38858,#38859,
#38860,#38861,#38862,#38863,#38864,#38865,#38866,#38867,#38868),
 .UNSPECIFIED.,.F.,.F.,(4,2,2,2,2,2,4),(-0.122023436879687,-0.106448133343434,
-0.0921171939725468,-0.0737837856348753,-0.0478286240892578,-0.0261030661831481,
-1.94845283136557E-5),.UNSPECIFIED.);
#2366=B_SPLINE_CURVE_WITH_KNOTS('',3,(#38870,#38871,#38872,#38873,#38874,
#38875,#38876,#38877,#38878,#38879,#38880,#38881,#38882,#38883,#38884,#38885,
#38886,#38887,#38888,#38889,#38890,#38891,#38892,#38893,#38894,#38895,#38896,
#38897,#38898,#38899,#38900,#38901,#38902,#38903,#38904,#38905,#38906,#38907,
#38908,#38909,#38910,#38911,#38912,#38913,#38914,#38915,#38916,#38917,#38918,
#38919,#38920,#38921,#38922,#38923,#38924,#38925,#38926,#38927,#38928,#38929,
#38930,#38931,#38932,#38933,#38934,#38935,#38936,#38937,#38938,#38939,#38940,
#38941,#38942,#38943,#38944,#38945,#38946,#38947,#38948),.UNSPECIFIED.,
 .F.,.F.,(4,3,3,3,3,3,3,3,3,3,3,3,3,3,3,3,3,3,3,3,3,3,3,3,3,3,4),(7.95863275788224E-5,
0.064551352652461,0.117854587835117,0.177729271849115,0.21074324143075,
0.260240782777837,0.30320069554456,0.357169753186396,0.404857781481859,
0.448155184829136,0.47909625451946,0.503910515180243,0.546919912939329,
0.570033569021481,0.608240220497836,0.649721217879779,0.683507534352941,
0.706246676627233,0.758819622585974,0.79057152095178,0.813334638529592,
0.857858751710615,0.880864688605644,0.904150315147694,0.944593770952623,
0.985288372137794,0.99955530932234),.UNSPECIFIED.);
#2367=B_SPLINE_CURVE_WITH_KNOTS('',3,(#39794,#39795,#39796,#39797,#39798,
#39799),.UNSPECIFIED.,.F.,.F.,(4,2,4),(-0.0127260790025929,-0.00639347718755023,
-5.76939431744538E-5),.UNSPECIFIED.);
#2759=LINE('',#34535,#3224);
#2760=LINE('',#34539,#3225);
#2761=LINE('',#34543,#3226);
#2762=LINE('',#34547,#3227);
#2763=LINE('',#34551,#3228);
#2764=LINE('',#34555,#3229);
#2765=LINE('',#34559,#3230);
#2766=LINE('',#34563,#3231);
#2767=LINE('',#34567,#3232);
#2768=LINE('',#34571,#3233);
#2769=LINE('',#34575,#3234);
#2770=LINE('',#34578,#3235);
#2771=LINE('',#34581,#3236);
#2772=LINE('',#34585,#3237);
#2773=LINE('',#34602,#3238);
#2774=LINE('',#34680,#3239);
#2775=LINE('',#34941,#3240);
#2776=LINE('',#35370,#3241);
#2777=LINE('',#35631,#3242);
#2778=LINE('',#36046,#3243);
#2779=LINE('',#36305,#3244);
#2780=LINE('',#36720,#3245);
#2781=LINE('',#36983,#3246);
#2782=LINE('',#37400,#3247);
#2783=LINE('',#37657,#3248);
#2784=LINE('',#38072,#3249);
#2785=LINE('',#39089,#3250);
#2786=LINE('',#39230,#3251);
#2787=LINE('',#39371,#3252);
#2788=LINE('',#39512,#3253);
#2789=LINE('',#39653,#3254);
#2790=LINE('',#39803,#3255);
#2791=LINE('',#39806,#3256);
#2792=LINE('',#39809,#3257);
#2793=LINE('',#39810,#3258);
#2794=LINE('',#39814,#3259);
#2795=LINE('',#39818,#3260);
#2796=LINE('',#39821,#3261);
#2797=LINE('',#39825,#3262);
#2798=LINE('',#39829,#3263);
#2799=LINE('',#39833,#3264);
#2800=LINE('',#39837,#3265);
#2801=LINE('',#39841,#3266);
#2802=LINE('',#39845,#3267);
#2803=LINE('',#39849,#3268);
#2804=LINE('',#39853,#3269);
#2805=LINE('',#39856,#3270);
#2806=LINE('',#39857,#3271);
#2807=LINE('',#39859,#3272);
#2808=LINE('',#39861,#3273);
#2809=LINE('',#39863,#3274);
#2810=LINE('',#39865,#3275);
#2811=LINE('',#39867,#3276);
#2812=LINE('',#39869,#3277);
#2813=LINE('',#39871,#3278);
#2814=LINE('',#39873,#3279);
#2815=LINE('',#39875,#3280);
#2816=LINE('',#39877,#3281);
#2817=LINE('',#39879,#3282);
#2818=LINE('',#39881,#3283);
#2819=LINE('',#39883,#3284);
#2820=LINE('',#39885,#3285);
#2821=LINE('',#39887,#3286);
#2822=LINE('',#39889,#3287);
#2823=LINE('',#39892,#3288);
#2824=LINE('',#39894,#3289);
#2825=LINE('',#39896,#3290);
#3224=VECTOR('',#11807,0.4519026509541);
#3225=VECTOR('',#11810,0.3019026509541);
#3226=VECTOR('',#11813,0.4519026509541);
#3227=VECTOR('',#11816,0.4519026509541);
#3228=VECTOR('',#11819,0.3019026509541);
#3229=VECTOR('',#11822,0.4519026509541);
#3230=VECTOR('',#11825,0.4519026509541);
#3231=VECTOR('',#11828,0.3019026509541);
#3232=VECTOR('',#11831,0.4519026509541);
#3233=VECTOR('',#11834,0.4519026509541);
#3234=VECTOR('',#11837,0.3019026509541);
#3235=VECTOR('',#11840,0.4519026509541);
#3236=VECTOR('',#11843,2.35);
#3237=VECTOR('',#11848,1.725);
#3238=VECTOR('',#11863,1.175);
#3239=VECTOR('',#11868,0.45);
#3240=VECTOR('',#11869,0.323316150746213);
#3241=VECTOR('',#11870,0.323316150746213);
#3242=VECTOR('',#11871,0.32331615074619);
#3243=VECTOR('',#11872,0.32331615074619);
#3244=VECTOR('',#11873,0.323316150746185);
#3245=VECTOR('',#11874,0.323316150746185);
#3246=VECTOR('',#11875,0.323316150746214);
#3247=VECTOR('',#11876,0.323316150746214);
#3248=VECTOR('',#11877,0.3233161507462);
#3249=VECTOR('',#11878,0.3233161507462);
#3250=VECTOR('',#11881,0.1266838492538);
#3251=VECTOR('',#11882,0.1266838492538);
#3252=VECTOR('',#11883,0.1266838492538);
#3253=VECTOR('',#11884,0.1266838492538);
#3254=VECTOR('',#11885,0.1266838492538);
#3255=VECTOR('',#11890,1.20915023334004);
#3256=VECTOR('',#11893,1.20915023334004);
#3257=VECTOR('',#11896,1.20915023334004);
#3258=VECTOR('',#11897,0.4519026509541);
#3259=VECTOR('',#11900,0.4519026509541);
#3260=VECTOR('',#11903,0.09192985849191);
#3261=VECTOR('',#11906,0.4519026509541);
#3262=VECTOR('',#11909,0.09192985849191);
#3263=VECTOR('',#11912,0.4519026509541);
#3264=VECTOR('',#11915,0.4519026509541);
#3265=VECTOR('',#11918,0.09192985849191);
#3266=VECTOR('',#11921,0.4519026509541);
#3267=VECTOR('',#11924,0.4519026509541);
#3268=VECTOR('',#11927,0.09192985849191);
#3269=VECTOR('',#11930,0.4519026509541);
#3270=VECTOR('',#11935,1.20915023334004);
#3271=VECTOR('',#11936,1.20915023334004);
#3272=VECTOR('',#11939,1.20915023334004);
#3273=VECTOR('',#11942,1.20915023334004);
#3274=VECTOR('',#11945,1.20915023334004);
#3275=VECTOR('',#11948,1.20915023334004);
#3276=VECTOR('',#11951,1.20915023334004);
#3277=VECTOR('',#11954,1.20915023334004);
#3278=VECTOR('',#11957,1.20915023334004);
#3279=VECTOR('',#11960,1.20915023334004);
#3280=VECTOR('',#11963,1.20915023334004);
#3281=VECTOR('',#11966,1.20915023334004);
#3282=VECTOR('',#11969,1.20915023334004);
#3283=VECTOR('',#11972,1.20915023334004);
#3284=VECTOR('',#11975,1.20915023334004);
#3285=VECTOR('',#11978,1.20915023334004);
#3286=VECTOR('',#11981,1.20915023334004);
#3287=VECTOR('',#11984,1.20915023334004);
#3288=VECTOR('',#11989,1.20915023334004);
#3289=VECTOR('',#11992,1.20915023334004);
#3290=VECTOR('',#11995,1.20915023334004);
#3982=VERTEX_POINT('',#34529);
#3983=VERTEX_POINT('',#34531);
#3984=VERTEX_POINT('',#34532);
#3985=VERTEX_POINT('',#34534);
#3986=VERTEX_POINT('',#34536);
#3987=VERTEX_POINT('',#34538);
#3988=VERTEX_POINT('',#34540);
#3989=VERTEX_POINT('',#34542);
#3990=VERTEX_POINT('',#34544);
#3991=VERTEX_POINT('',#34546);
#3992=VERTEX_POINT('',#34548);
#3993=VERTEX_POINT('',#34550);
#3994=VERTEX_POINT('',#34552);
#3995=VERTEX_POINT('',#34554);
#3996=VERTEX_POINT('',#34556);
#3997=VERTEX_POINT('',#34558);
#3998=VERTEX_POINT('',#34560);
#3999=VERTEX_POINT('',#34562);
#4000=VERTEX_POINT('',#34564);
#4001=VERTEX_POINT('',#34566);
#4002=VERTEX_POINT('',#34568);
#4003=VERTEX_POINT('',#34570);
#4004=VERTEX_POINT('',#34572);
#4005=VERTEX_POINT('',#34574);
#4006=VERTEX_POINT('',#34576);
#4007=VERTEX_POINT('',#34580);
#4008=VERTEX_POINT('',#34584);
#4009=VERTEX_POINT('',#34588);
#4010=VERTEX_POINT('',#34590);
#4011=VERTEX_POINT('',#34594);
#4012=VERTEX_POINT('',#34595);
#4013=VERTEX_POINT('',#34600);
#4014=VERTEX_POINT('',#34605);
#4015=VERTEX_POINT('',#34821);
#4016=VERTEX_POINT('',#34940);
#4017=VERTEX_POINT('',#34942);
#4018=VERTEX_POINT('',#35203);
#4019=VERTEX_POINT('',#35248);
#4020=VERTEX_POINT('',#35255);
#4021=VERTEX_POINT('',#35511);
#4022=VERTEX_POINT('',#35630);
#4023=VERTEX_POINT('',#35886);
#4024=VERTEX_POINT('',#35931);
#4025=VERTEX_POINT('',#36187);
#4026=VERTEX_POINT('',#36304);
#4027=VERTEX_POINT('',#36560);
#4028=VERTEX_POINT('',#36605);
#4029=VERTEX_POINT('',#36861);
#4030=VERTEX_POINT('',#36982);
#4031=VERTEX_POINT('',#37238);
#4032=VERTEX_POINT('',#37285);
#4033=VERTEX_POINT('',#37541);
#4034=VERTEX_POINT('',#37656);
#4035=VERTEX_POINT('',#37912);
#4036=VERTEX_POINT('',#37957);
#4037=VERTEX_POINT('',#38213);
#4038=VERTEX_POINT('',#38312);
#4039=VERTEX_POINT('',#38339);
#4040=VERTEX_POINT('',#38692);
#4041=VERTEX_POINT('',#39802);
#4042=VERTEX_POINT('',#39804);
#4043=VERTEX_POINT('',#39808);
#4044=VERTEX_POINT('',#39812);
#4045=VERTEX_POINT('',#39813);
#4046=VERTEX_POINT('',#39815);
#4047=VERTEX_POINT('',#39817);
#4048=VERTEX_POINT('',#39819);
#4049=VERTEX_POINT('',#39822);
#4050=VERTEX_POINT('',#39824);
#4051=VERTEX_POINT('',#39826);
#4052=VERTEX_POINT('',#39828);
#4053=VERTEX_POINT('',#39830);
#4054=VERTEX_POINT('',#39832);
#4055=VERTEX_POINT('',#39834);
#4056=VERTEX_POINT('',#39836);
#4057=VERTEX_POINT('',#39838);
#4058=VERTEX_POINT('',#39840);
#4059=VERTEX_POINT('',#39842);
#4060=VERTEX_POINT('',#39844);
#4061=VERTEX_POINT('',#39846);
#4062=VERTEX_POINT('',#39848);
#4063=VERTEX_POINT('',#39850);
#4064=VERTEX_POINT('',#39852);
#5181=EDGE_CURVE('',#3982,#3982,#1985,.T.);
#5182=EDGE_CURVE('',#3983,#3984,#92,.T.);
#5183=EDGE_CURVE('',#3984,#3985,#2759,.T.);
#5184=EDGE_CURVE('',#3985,#3986,#93,.T.);
#5185=EDGE_CURVE('',#3986,#3987,#2760,.T.);
#5186=EDGE_CURVE('',#3987,#3988,#94,.T.);
#5187=EDGE_CURVE('',#3988,#3989,#2761,.T.);
#5188=EDGE_CURVE('',#3989,#3990,#95,.T.);
#5189=EDGE_CURVE('',#3990,#3991,#2762,.T.);
#5190=EDGE_CURVE('',#3991,#3992,#96,.T.);
#5191=EDGE_CURVE('',#3992,#3993,#2763,.T.);
#5192=EDGE_CURVE('',#3993,#3994,#97,.T.);
#5193=EDGE_CURVE('',#3994,#3995,#2764,.T.);
#5194=EDGE_CURVE('',#3995,#3996,#98,.T.);
#5195=EDGE_CURVE('',#3996,#3997,#2765,.T.);
#5196=EDGE_CURVE('',#3997,#3998,#99,.T.);
#5197=EDGE_CURVE('',#3998,#3999,#2766,.T.);
#5198=EDGE_CURVE('',#3999,#4000,#100,.T.);
#5199=EDGE_CURVE('',#4000,#4001,#2767,.T.);
#5200=EDGE_CURVE('',#4001,#4002,#101,.T.);
#5201=EDGE_CURVE('',#4002,#4003,#2768,.T.);
#5202=EDGE_CURVE('',#4003,#4004,#102,.T.);
#5203=EDGE_CURVE('',#4004,#4005,#2769,.T.);
#5204=EDGE_CURVE('',#4005,#4006,#103,.T.);
#5205=EDGE_CURVE('',#4006,#3983,#2770,.T.);
#5206=EDGE_CURVE('',#3982,#4007,#2771,.T.);
#5207=EDGE_CURVE('',#4007,#4007,#1986,.T.);
#5208=EDGE_CURVE('',#4007,#4008,#2772,.T.);
#5209=EDGE_CURVE('',#4008,#4008,#1987,.T.);
#5210=EDGE_CURVE('',#4008,#4009,#1988,.T.);
#5211=EDGE_CURVE('',#4009,#4010,#1989,.T.);
#5212=EDGE_CURVE('',#4010,#4009,#1990,.T.);
#5213=EDGE_CURVE('',#4011,#4012,#2336,.T.);
#5214=EDGE_CURVE('',#4011,#4013,#1991,.T.);
#5215=EDGE_CURVE('',#4013,#4010,#2773,.T.);
#5216=EDGE_CURVE('',#4013,#4012,#1992,.T.);
#5217=EDGE_CURVE('',#4014,#4012,#2337,.T.);
#5218=EDGE_CURVE('',#4014,#4011,#2774,.T.);
#5219=EDGE_CURVE('',#4015,#4014,#2338,.F.);
#5220=EDGE_CURVE('',#4016,#4015,#2775,.T.);
#5221=EDGE_CURVE('',#4016,#4017,#2339,.T.);
#5222=EDGE_CURVE('',#4017,#4011,#2340,.T.);
#5223=EDGE_CURVE('',#4018,#4015,#2341,.T.);
#5224=EDGE_CURVE('',#4014,#4019,#2342,.T.);
#5225=EDGE_CURVE('',#4020,#4019,#2343,.T.);
#5226=EDGE_CURVE('',#4018,#4020,#2776,.T.);
#5227=EDGE_CURVE('',#4021,#4018,#2344,.F.);
#5228=EDGE_CURVE('',#4022,#4021,#2777,.T.);
#5229=EDGE_CURVE('',#4022,#4016,#2345,.T.);
#5230=EDGE_CURVE('',#4023,#4021,#2346,.T.);
#5231=EDGE_CURVE('',#4024,#4020,#2347,.T.);
#5232=EDGE_CURVE('',#4023,#4024,#2778,.T.);
#5233=EDGE_CURVE('',#4025,#4023,#2348,.F.);
#5234=EDGE_CURVE('',#4026,#4025,#2779,.T.);
#5235=EDGE_CURVE('',#4026,#4022,#2349,.T.);
#5236=EDGE_CURVE('',#4027,#4025,#2350,.T.);
#5237=EDGE_CURVE('',#4028,#4024,#2351,.T.);
#5238=EDGE_CURVE('',#4027,#4028,#2780,.T.);
#5239=EDGE_CURVE('',#4029,#4027,#2352,.F.);
#5240=EDGE_CURVE('',#4030,#4029,#2781,.T.);
#5241=EDGE_CURVE('',#4030,#4026,#2353,.T.);
#5242=EDGE_CURVE('',#4031,#4029,#2354,.T.);
#5243=EDGE_CURVE('',#4032,#4028,#2355,.T.);
#5244=EDGE_CURVE('',#4031,#4032,#2782,.T.);
#5245=EDGE_CURVE('',#4033,#4031,#2356,.F.);
#5246=EDGE_CURVE('',#4034,#4033,#2783,.T.);
#5247=EDGE_CURVE('',#4034,#4030,#2357,.T.);
#5248=EDGE_CURVE('',#4035,#4033,#2358,.T.);
#5249=EDGE_CURVE('',#4036,#4032,#2359,.T.);
#5250=EDGE_CURVE('',#4035,#4036,#2784,.T.);
#5251=EDGE_CURVE('',#4037,#4035,#2360,.F.);
#5252=EDGE_CURVE('',#4038,#4037,#2361,.T.);
#5253=EDGE_CURVE('',#4039,#4038,#2362,.T.);
#5254=EDGE_CURVE('',#4039,#4034,#2363,.T.);
#5255=EDGE_CURVE('',#4040,#4036,#2364,.T.);
#5256=EDGE_CURVE('',#4038,#4040,#2365,.T.);
#5257=EDGE_CURVE('',#4040,#4039,#2366,.T.);
#5258=EDGE_CURVE('',#4036,#4034,#2785,.T.);
#5259=EDGE_CURVE('',#4032,#4030,#2786,.T.);
#5260=EDGE_CURVE('',#4028,#4026,#2787,.T.);
#5261=EDGE_CURVE('',#4024,#4022,#2788,.T.);
#5262=EDGE_CURVE('',#4020,#4016,#2789,.T.);
#5263=EDGE_CURVE('',#4019,#4017,#2367,.T.);
#5264=EDGE_CURVE('',#3983,#4041,#2790,.T.);
#5265=EDGE_CURVE('',#4042,#4041,#104,.T.);
#5266=EDGE_CURVE('',#3984,#4042,#2791,.T.);
#5267=EDGE_CURVE('',#4043,#4006,#2792,.T.);
#5268=EDGE_CURVE('',#4043,#4041,#2793,.T.);
#5269=EDGE_CURVE('',#4044,#4045,#2794,.T.);
#5270=EDGE_CURVE('',#4045,#4046,#105,.T.);
#5271=EDGE_CURVE('',#4046,#4047,#2795,.T.);
#5272=EDGE_CURVE('',#4047,#4048,#106,.T.);
#5273=EDGE_CURVE('',#4042,#4048,#2796,.T.);
#5274=EDGE_CURVE('',#4043,#4049,#107,.T.);
#5275=EDGE_CURVE('',#4050,#4049,#2797,.T.);
#5276=EDGE_CURVE('',#4050,#4051,#108,.T.);
#5277=EDGE_CURVE('',#4051,#4052,#2798,.T.);
#5278=EDGE_CURVE('',#4052,#4053,#109,.T.);
#5279=EDGE_CURVE('',#4054,#4053,#2799,.T.);
#5280=EDGE_CURVE('',#4054,#4055,#110,.T.);
#5281=EDGE_CURVE('',#4055,#4056,#2800,.T.);
#5282=EDGE_CURVE('',#4056,#4057,#111,.T.);
#5283=EDGE_CURVE('',#4057,#4058,#2801,.T.);
#5284=EDGE_CURVE('',#4058,#4059,#112,.T.);
#5285=EDGE_CURVE('',#4059,#4060,#2802,.T.);
#5286=EDGE_CURVE('',#4060,#4061,#113,.T.);
#5287=EDGE_CURVE('',#4062,#4061,#2803,.T.);
#5288=EDGE_CURVE('',#4062,#4063,#114,.T.);
#5289=EDGE_CURVE('',#4063,#4064,#2804,.T.);
#5290=EDGE_CURVE('',#4064,#4044,#115,.T.);
#5291=EDGE_CURVE('',#3989,#4044,#2805,.T.);
#5292=EDGE_CURVE('',#4045,#3988,#2806,.T.);
#5293=EDGE_CURVE('',#3990,#4064,#2807,.T.);
#5294=EDGE_CURVE('',#4063,#3991,#2808,.T.);
#5295=EDGE_CURVE('',#4062,#3992,#2809,.T.);
#5296=EDGE_CURVE('',#4061,#3993,#2810,.T.);
#5297=EDGE_CURVE('',#4060,#3994,#2811,.T.);
#5298=EDGE_CURVE('',#3995,#4059,#2812,.T.);
#5299=EDGE_CURVE('',#3996,#4058,#2813,.T.);
#5300=EDGE_CURVE('',#4057,#3997,#2814,.T.);
#5301=EDGE_CURVE('',#4056,#3998,#2815,.T.);
#5302=EDGE_CURVE('',#4055,#3999,#2816,.T.);
#5303=EDGE_CURVE('',#4054,#4000,#2817,.T.);
#5304=EDGE_CURVE('',#4001,#4053,#2818,.T.);
#5305=EDGE_CURVE('',#4002,#4052,#2819,.T.);
#5306=EDGE_CURVE('',#4051,#4003,#2820,.T.);
#5307=EDGE_CURVE('',#4050,#4004,#2821,.T.);
#5308=EDGE_CURVE('',#4049,#4005,#2822,.T.);
#5309=EDGE_CURVE('',#4046,#3987,#2823,.T.);
#5310=EDGE_CURVE('',#4047,#3986,#2824,.T.);
#5311=EDGE_CURVE('',#4048,#3985,#2825,.T.);
#7470=ORIENTED_EDGE('',*,*,#5181,.T.);
#7471=ORIENTED_EDGE('',*,*,#5182,.T.);
#7472=ORIENTED_EDGE('',*,*,#5183,.T.);
#7473=ORIENTED_EDGE('',*,*,#5184,.T.);
#7474=ORIENTED_EDGE('',*,*,#5185,.T.);
#7475=ORIENTED_EDGE('',*,*,#5186,.T.);
#7476=ORIENTED_EDGE('',*,*,#5187,.T.);
#7477=ORIENTED_EDGE('',*,*,#5188,.T.);
#7478=ORIENTED_EDGE('',*,*,#5189,.T.);
#7479=ORIENTED_EDGE('',*,*,#5190,.T.);
#7480=ORIENTED_EDGE('',*,*,#5191,.T.);
#7481=ORIENTED_EDGE('',*,*,#5192,.T.);
#7482=ORIENTED_EDGE('',*,*,#5193,.T.);
#7483=ORIENTED_EDGE('',*,*,#5194,.T.);
#7484=ORIENTED_EDGE('',*,*,#5195,.T.);
#7485=ORIENTED_EDGE('',*,*,#5196,.T.);
#7486=ORIENTED_EDGE('',*,*,#5197,.T.);
#7487=ORIENTED_EDGE('',*,*,#5198,.T.);
#7488=ORIENTED_EDGE('',*,*,#5199,.T.);
#7489=ORIENTED_EDGE('',*,*,#5200,.T.);
#7490=ORIENTED_EDGE('',*,*,#5201,.T.);
#7491=ORIENTED_EDGE('',*,*,#5202,.T.);
#7492=ORIENTED_EDGE('',*,*,#5203,.T.);
#7493=ORIENTED_EDGE('',*,*,#5204,.T.);
#7494=ORIENTED_EDGE('',*,*,#5205,.T.);
#7495=ORIENTED_EDGE('',*,*,#5181,.F.);
#7496=ORIENTED_EDGE('',*,*,#5206,.T.);
#7497=ORIENTED_EDGE('',*,*,#5207,.T.);
#7498=ORIENTED_EDGE('',*,*,#5206,.F.);
#7499=ORIENTED_EDGE('',*,*,#5207,.F.);
#7500=ORIENTED_EDGE('',*,*,#5208,.T.);
#7501=ORIENTED_EDGE('',*,*,#5209,.T.);
#7502=ORIENTED_EDGE('',*,*,#5208,.F.);
#7503=ORIENTED_EDGE('',*,*,#5209,.F.);
#7504=ORIENTED_EDGE('',*,*,#5210,.T.);
#7505=ORIENTED_EDGE('',*,*,#5211,.T.);
#7506=ORIENTED_EDGE('',*,*,#5212,.T.);
#7507=ORIENTED_EDGE('',*,*,#5210,.F.);
#7508=ORIENTED_EDGE('',*,*,#5213,.F.);
#7509=ORIENTED_EDGE('',*,*,#5214,.T.);
#7510=ORIENTED_EDGE('',*,*,#5215,.T.);
#7511=ORIENTED_EDGE('',*,*,#5211,.F.);
#7512=ORIENTED_EDGE('',*,*,#5212,.F.);
#7513=ORIENTED_EDGE('',*,*,#5215,.F.);
#7514=ORIENTED_EDGE('',*,*,#5216,.T.);
#7515=ORIENTED_EDGE('',*,*,#5217,.T.);
#7516=ORIENTED_EDGE('',*,*,#5216,.F.);
#7517=ORIENTED_EDGE('',*,*,#5214,.F.);
#7518=ORIENTED_EDGE('',*,*,#5218,.F.);
#7519=ORIENTED_EDGE('',*,*,#5219,.F.);
#7520=ORIENTED_EDGE('',*,*,#5220,.F.);
#7521=ORIENTED_EDGE('',*,*,#5221,.T.);
#7522=ORIENTED_EDGE('',*,*,#5222,.T.);
#7523=ORIENTED_EDGE('',*,*,#5213,.T.);
#7524=ORIENTED_EDGE('',*,*,#5217,.F.);
#7525=ORIENTED_EDGE('',*,*,#5223,.T.);
#7526=ORIENTED_EDGE('',*,*,#5219,.T.);
#7527=ORIENTED_EDGE('',*,*,#5224,.T.);
#7528=ORIENTED_EDGE('',*,*,#5225,.F.);
#7529=ORIENTED_EDGE('',*,*,#5226,.F.);
#7530=ORIENTED_EDGE('',*,*,#5227,.F.);
#7531=ORIENTED_EDGE('',*,*,#5228,.F.);
#7532=ORIENTED_EDGE('',*,*,#5229,.T.);
#7533=ORIENTED_EDGE('',*,*,#5220,.T.);
#7534=ORIENTED_EDGE('',*,*,#5223,.F.);
#7535=ORIENTED_EDGE('',*,*,#5230,.T.);
#7536=ORIENTED_EDGE('',*,*,#5227,.T.);
#7537=ORIENTED_EDGE('',*,*,#5226,.T.);
#7538=ORIENTED_EDGE('',*,*,#5231,.F.);
#7539=ORIENTED_EDGE('',*,*,#5232,.F.);
#7540=ORIENTED_EDGE('',*,*,#5233,.F.);
#7541=ORIENTED_EDGE('',*,*,#5234,.F.);
#7542=ORIENTED_EDGE('',*,*,#5235,.T.);
#7543=ORIENTED_EDGE('',*,*,#5228,.T.);
#7544=ORIENTED_EDGE('',*,*,#5230,.F.);
#7545=ORIENTED_EDGE('',*,*,#5236,.T.);
#7546=ORIENTED_EDGE('',*,*,#5233,.T.);
#7547=ORIENTED_EDGE('',*,*,#5232,.T.);
#7548=ORIENTED_EDGE('',*,*,#5237,.F.);
#7549=ORIENTED_EDGE('',*,*,#5238,.F.);
#7550=ORIENTED_EDGE('',*,*,#5239,.F.);
#7551=ORIENTED_EDGE('',*,*,#5240,.F.);
#7552=ORIENTED_EDGE('',*,*,#5241,.T.);
#7553=ORIENTED_EDGE('',*,*,#5234,.T.);
#7554=ORIENTED_EDGE('',*,*,#5236,.F.);
#7555=ORIENTED_EDGE('',*,*,#5242,.T.);
#7556=ORIENTED_EDGE('',*,*,#5239,.T.);
#7557=ORIENTED_EDGE('',*,*,#5238,.T.);
#7558=ORIENTED_EDGE('',*,*,#5243,.F.);
#7559=ORIENTED_EDGE('',*,*,#5244,.F.);
#7560=ORIENTED_EDGE('',*,*,#5245,.F.);
#7561=ORIENTED_EDGE('',*,*,#5246,.F.);
#7562=ORIENTED_EDGE('',*,*,#5247,.T.);
#7563=ORIENTED_EDGE('',*,*,#5240,.T.);
#7564=ORIENTED_EDGE('',*,*,#5242,.F.);
#7565=ORIENTED_EDGE('',*,*,#5248,.T.);
#7566=ORIENTED_EDGE('',*,*,#5245,.T.);
#7567=ORIENTED_EDGE('',*,*,#5244,.T.);
#7568=ORIENTED_EDGE('',*,*,#5249,.F.);
#7569=ORIENTED_EDGE('',*,*,#5250,.F.);
#7570=ORIENTED_EDGE('',*,*,#5251,.F.);
#7571=ORIENTED_EDGE('',*,*,#5252,.F.);
#7572=ORIENTED_EDGE('',*,*,#5253,.F.);
#7573=ORIENTED_EDGE('',*,*,#5254,.T.);
#7574=ORIENTED_EDGE('',*,*,#5246,.T.);
#7575=ORIENTED_EDGE('',*,*,#5248,.F.);
#7576=ORIENTED_EDGE('',*,*,#5251,.T.);
#7577=ORIENTED_EDGE('',*,*,#5250,.T.);
#7578=ORIENTED_EDGE('',*,*,#5255,.F.);
#7579=ORIENTED_EDGE('',*,*,#5256,.F.);
#7580=ORIENTED_EDGE('',*,*,#5252,.T.);
#7581=ORIENTED_EDGE('',*,*,#5256,.T.);
#7582=ORIENTED_EDGE('',*,*,#5257,.T.);
#7583=ORIENTED_EDGE('',*,*,#5253,.T.);
#7584=ORIENTED_EDGE('',*,*,#5257,.F.);
#7585=ORIENTED_EDGE('',*,*,#5255,.T.);
#7586=ORIENTED_EDGE('',*,*,#5258,.T.);
#7587=ORIENTED_EDGE('',*,*,#5254,.F.);
#7588=ORIENTED_EDGE('',*,*,#5258,.F.);
#7589=ORIENTED_EDGE('',*,*,#5249,.T.);
#7590=ORIENTED_EDGE('',*,*,#5259,.T.);
#7591=ORIENTED_EDGE('',*,*,#5247,.F.);
#7592=ORIENTED_EDGE('',*,*,#5259,.F.);
#7593=ORIENTED_EDGE('',*,*,#5243,.T.);
#7594=ORIENTED_EDGE('',*,*,#5260,.T.);
#7595=ORIENTED_EDGE('',*,*,#5241,.F.);
#7596=ORIENTED_EDGE('',*,*,#5260,.F.);
#7597=ORIENTED_EDGE('',*,*,#5237,.T.);
#7598=ORIENTED_EDGE('',*,*,#5261,.T.);
#7599=ORIENTED_EDGE('',*,*,#5235,.F.);
#7600=ORIENTED_EDGE('',*,*,#5261,.F.);
#7601=ORIENTED_EDGE('',*,*,#5231,.T.);
#7602=ORIENTED_EDGE('',*,*,#5262,.T.);
#7603=ORIENTED_EDGE('',*,*,#5229,.F.);
#7604=ORIENTED_EDGE('',*,*,#5262,.F.);
#7605=ORIENTED_EDGE('',*,*,#5225,.T.);
#7606=ORIENTED_EDGE('',*,*,#5263,.T.);
#7607=ORIENTED_EDGE('',*,*,#5221,.F.);
#7608=ORIENTED_EDGE('',*,*,#5218,.T.);
#7609=ORIENTED_EDGE('',*,*,#5222,.F.);
#7610=ORIENTED_EDGE('',*,*,#5263,.F.);
#7611=ORIENTED_EDGE('',*,*,#5224,.F.);
#7612=ORIENTED_EDGE('',*,*,#5264,.T.);
#7613=ORIENTED_EDGE('',*,*,#5265,.F.);
#7614=ORIENTED_EDGE('',*,*,#5266,.F.);
#7615=ORIENTED_EDGE('',*,*,#5182,.F.);
#7616=ORIENTED_EDGE('',*,*,#5264,.F.);
#7617=ORIENTED_EDGE('',*,*,#5205,.F.);
#7618=ORIENTED_EDGE('',*,*,#5267,.F.);
#7619=ORIENTED_EDGE('',*,*,#5268,.T.);
#7620=ORIENTED_EDGE('',*,*,#5269,.T.);
#7621=ORIENTED_EDGE('',*,*,#5270,.T.);
#7622=ORIENTED_EDGE('',*,*,#5271,.T.);
#7623=ORIENTED_EDGE('',*,*,#5272,.T.);
#7624=ORIENTED_EDGE('',*,*,#5273,.F.);
#7625=ORIENTED_EDGE('',*,*,#5265,.T.);
#7626=ORIENTED_EDGE('',*,*,#5268,.F.);
#7627=ORIENTED_EDGE('',*,*,#5274,.T.);
#7628=ORIENTED_EDGE('',*,*,#5275,.F.);
#7629=ORIENTED_EDGE('',*,*,#5276,.T.);
#7630=ORIENTED_EDGE('',*,*,#5277,.T.);
#7631=ORIENTED_EDGE('',*,*,#5278,.T.);
#7632=ORIENTED_EDGE('',*,*,#5279,.F.);
#7633=ORIENTED_EDGE('',*,*,#5280,.T.);
#7634=ORIENTED_EDGE('',*,*,#5281,.T.);
#7635=ORIENTED_EDGE('',*,*,#5282,.T.);
#7636=ORIENTED_EDGE('',*,*,#5283,.T.);
#7637=ORIENTED_EDGE('',*,*,#5284,.T.);
#7638=ORIENTED_EDGE('',*,*,#5285,.T.);
#7639=ORIENTED_EDGE('',*,*,#5286,.T.);
#7640=ORIENTED_EDGE('',*,*,#5287,.F.);
#7641=ORIENTED_EDGE('',*,*,#5288,.T.);
#7642=ORIENTED_EDGE('',*,*,#5289,.T.);
#7643=ORIENTED_EDGE('',*,*,#5290,.T.);
#7644=ORIENTED_EDGE('',*,*,#5291,.F.);
#7645=ORIENTED_EDGE('',*,*,#5187,.F.);
#7646=ORIENTED_EDGE('',*,*,#5292,.F.);
#7647=ORIENTED_EDGE('',*,*,#5269,.F.);
#7648=ORIENTED_EDGE('',*,*,#5291,.T.);
#7649=ORIENTED_EDGE('',*,*,#5290,.F.);
#7650=ORIENTED_EDGE('',*,*,#5293,.F.);
#7651=ORIENTED_EDGE('',*,*,#5188,.F.);
#7652=ORIENTED_EDGE('',*,*,#5293,.T.);
#7653=ORIENTED_EDGE('',*,*,#5289,.F.);
#7654=ORIENTED_EDGE('',*,*,#5294,.T.);
#7655=ORIENTED_EDGE('',*,*,#5189,.F.);
#7656=ORIENTED_EDGE('',*,*,#5295,.T.);
#7657=ORIENTED_EDGE('',*,*,#5190,.F.);
#7658=ORIENTED_EDGE('',*,*,#5294,.F.);
#7659=ORIENTED_EDGE('',*,*,#5288,.F.);
#7660=ORIENTED_EDGE('',*,*,#5295,.F.);
#7661=ORIENTED_EDGE('',*,*,#5287,.T.);
#7662=ORIENTED_EDGE('',*,*,#5296,.T.);
#7663=ORIENTED_EDGE('',*,*,#5191,.F.);
#7664=ORIENTED_EDGE('',*,*,#5297,.T.);
#7665=ORIENTED_EDGE('',*,*,#5192,.F.);
#7666=ORIENTED_EDGE('',*,*,#5296,.F.);
#7667=ORIENTED_EDGE('',*,*,#5286,.F.);
#7668=ORIENTED_EDGE('',*,*,#5298,.F.);
#7669=ORIENTED_EDGE('',*,*,#5193,.F.);
#7670=ORIENTED_EDGE('',*,*,#5297,.F.);
#7671=ORIENTED_EDGE('',*,*,#5285,.F.);
#7672=ORIENTED_EDGE('',*,*,#5298,.T.);
#7673=ORIENTED_EDGE('',*,*,#5284,.F.);
#7674=ORIENTED_EDGE('',*,*,#5299,.F.);
#7675=ORIENTED_EDGE('',*,*,#5194,.F.);
#7676=ORIENTED_EDGE('',*,*,#5299,.T.);
#7677=ORIENTED_EDGE('',*,*,#5283,.F.);
#7678=ORIENTED_EDGE('',*,*,#5300,.T.);
#7679=ORIENTED_EDGE('',*,*,#5195,.F.);
#7680=ORIENTED_EDGE('',*,*,#5301,.T.);
#7681=ORIENTED_EDGE('',*,*,#5196,.F.);
#7682=ORIENTED_EDGE('',*,*,#5300,.F.);
#7683=ORIENTED_EDGE('',*,*,#5282,.F.);
#7684=ORIENTED_EDGE('',*,*,#5301,.F.);
#7685=ORIENTED_EDGE('',*,*,#5281,.F.);
#7686=ORIENTED_EDGE('',*,*,#5302,.T.);
#7687=ORIENTED_EDGE('',*,*,#5197,.F.);
#7688=ORIENTED_EDGE('',*,*,#5303,.T.);
#7689=ORIENTED_EDGE('',*,*,#5198,.F.);
#7690=ORIENTED_EDGE('',*,*,#5302,.F.);
#7691=ORIENTED_EDGE('',*,*,#5280,.F.);
#7692=ORIENTED_EDGE('',*,*,#5304,.F.);
#7693=ORIENTED_EDGE('',*,*,#5199,.F.);
#7694=ORIENTED_EDGE('',*,*,#5303,.F.);
#7695=ORIENTED_EDGE('',*,*,#5279,.T.);
#7696=ORIENTED_EDGE('',*,*,#5304,.T.);
#7697=ORIENTED_EDGE('',*,*,#5278,.F.);
#7698=ORIENTED_EDGE('',*,*,#5305,.F.);
#7699=ORIENTED_EDGE('',*,*,#5200,.F.);
#7700=ORIENTED_EDGE('',*,*,#5305,.T.);
#7701=ORIENTED_EDGE('',*,*,#5277,.F.);
#7702=ORIENTED_EDGE('',*,*,#5306,.T.);
#7703=ORIENTED_EDGE('',*,*,#5201,.F.);
#7704=ORIENTED_EDGE('',*,*,#5307,.T.);
#7705=ORIENTED_EDGE('',*,*,#5202,.F.);
#7706=ORIENTED_EDGE('',*,*,#5306,.F.);
#7707=ORIENTED_EDGE('',*,*,#5276,.F.);
#7708=ORIENTED_EDGE('',*,*,#5308,.T.);
#7709=ORIENTED_EDGE('',*,*,#5203,.F.);
#7710=ORIENTED_EDGE('',*,*,#5307,.F.);
#7711=ORIENTED_EDGE('',*,*,#5275,.T.);
#7712=ORIENTED_EDGE('',*,*,#5267,.T.);
#7713=ORIENTED_EDGE('',*,*,#5204,.F.);
#7714=ORIENTED_EDGE('',*,*,#5308,.F.);
#7715=ORIENTED_EDGE('',*,*,#5274,.F.);
#7716=ORIENTED_EDGE('',*,*,#5292,.T.);
#7717=ORIENTED_EDGE('',*,*,#5186,.F.);
#7718=ORIENTED_EDGE('',*,*,#5309,.F.);
#7719=ORIENTED_EDGE('',*,*,#5270,.F.);
#7720=ORIENTED_EDGE('',*,*,#5310,.F.);
#7721=ORIENTED_EDGE('',*,*,#5271,.F.);
#7722=ORIENTED_EDGE('',*,*,#5309,.T.);
#7723=ORIENTED_EDGE('',*,*,#5185,.F.);
#7724=ORIENTED_EDGE('',*,*,#5310,.T.);
#7725=ORIENTED_EDGE('',*,*,#5184,.F.);
#7726=ORIENTED_EDGE('',*,*,#5311,.F.);
#7727=ORIENTED_EDGE('',*,*,#5272,.F.);
#7728=ORIENTED_EDGE('',*,*,#5266,.T.);
#7729=ORIENTED_EDGE('',*,*,#5273,.T.);
#7730=ORIENTED_EDGE('',*,*,#5311,.T.);
#7731=ORIENTED_EDGE('',*,*,#5183,.F.);
#8523=CYLINDRICAL_SURFACE('',#9936,2.35);
#8524=CYLINDRICAL_SURFACE('',#9947,1.25);
#8525=CYLINDRICAL_SURFACE('',#9950,0.25);
#8526=CYLINDRICAL_SURFACE('',#9966,0.25);
#8527=CYLINDRICAL_SURFACE('',#9968,0.25);
#8528=CYLINDRICAL_SURFACE('',#9970,0.25);
#8529=CYLINDRICAL_SURFACE('',#9972,0.25);
#8530=CYLINDRICAL_SURFACE('',#9974,0.25);
#8531=CYLINDRICAL_SURFACE('',#9976,0.25);
#8532=CYLINDRICAL_SURFACE('',#9978,0.25);
#8533=CYLINDRICAL_SURFACE('',#9980,0.25);
#8534=CYLINDRICAL_SURFACE('',#9982,0.25);
#8535=CYLINDRICAL_SURFACE('',#9983,0.25);
#8536=CYLINDRICAL_SURFACE('',#9985,0.25);
#8935=ADVANCED_FACE('',(#872,#303),#468,.T.);
#8936=ADVANCED_FACE('',(#873),#8523,.T.);
#8937=ADVANCED_FACE('',(#874),#205,.T.);
#8938=ADVANCED_FACE('',(#875),#219,.F.);
#8939=ADVANCED_FACE('',(#876),#206,.T.);
#8940=ADVANCED_FACE('',(#877),#8524,.T.);
#8941=ADVANCED_FACE('',(#878),#370,.F.);
#8942=ADVANCED_FACE('',(#879),#371,.F.);
#8943=ADVANCED_FACE('',(#880),#372,.F.);
#8944=ADVANCED_FACE('',(#881),#373,.F.);
#8945=ADVANCED_FACE('',(#882),#374,.F.);
#8946=ADVANCED_FACE('',(#883),#375,.F.);
#8947=ADVANCED_FACE('',(#884),#376,.F.);
#8948=ADVANCED_FACE('',(#885),#377,.F.);
#8949=ADVANCED_FACE('',(#886),#378,.F.);
#8950=ADVANCED_FACE('',(#887),#379,.F.);
#8951=ADVANCED_FACE('',(#888),#380,.F.);
#8952=ADVANCED_FACE('',(#889),#381,.F.);
#8953=ADVANCED_FACE('',(#890),#469,.F.);
#8954=ADVANCED_FACE('',(#891),#382,.F.);
#8955=ADVANCED_FACE('',(#892),#383,.F.);
#8956=ADVANCED_FACE('',(#893),#384,.F.);
#8957=ADVANCED_FACE('',(#894),#385,.F.);
#8958=ADVANCED_FACE('',(#895),#386,.F.);
#8959=ADVANCED_FACE('',(#896),#387,.F.);
#8960=ADVANCED_FACE('',(#897),#470,.F.);
#8961=ADVANCED_FACE('',(#898),#8525,.T.);
#8962=ADVANCED_FACE('',(#899),#471,.F.);
#8963=ADVANCED_FACE('',(#900),#472,.T.);
#8964=ADVANCED_FACE('',(#901),#473,.F.);
#8965=ADVANCED_FACE('',(#902),#8526,.T.);
#8966=ADVANCED_FACE('',(#903),#474,.F.);
#8967=ADVANCED_FACE('',(#904),#8527,.F.);
#8968=ADVANCED_FACE('',(#905),#475,.F.);
#8969=ADVANCED_FACE('',(#906),#8528,.F.);
#8970=ADVANCED_FACE('',(#907),#476,.F.);
#8971=ADVANCED_FACE('',(#908),#8529,.T.);
#8972=ADVANCED_FACE('',(#909),#477,.F.);
#8973=ADVANCED_FACE('',(#910),#8530,.F.);
#8974=ADVANCED_FACE('',(#911),#478,.F.);
#8975=ADVANCED_FACE('',(#912),#8531,.F.);
#8976=ADVANCED_FACE('',(#913),#479,.F.);
#8977=ADVANCED_FACE('',(#914),#8532,.T.);
#8978=ADVANCED_FACE('',(#915),#480,.F.);
#8979=ADVANCED_FACE('',(#916),#8533,.F.);
#8980=ADVANCED_FACE('',(#917),#481,.F.);
#8981=ADVANCED_FACE('',(#918),#8534,.F.);
#8982=ADVANCED_FACE('',(#919),#8535,.F.);
#8983=ADVANCED_FACE('',(#920),#482,.F.);
#8984=ADVANCED_FACE('',(#921),#8536,.F.);
#8985=ADVANCED_FACE('',(#922),#483,.F.);
#9124=CLOSED_SHELL('',(#8935,#8936,#8937,#8938,#8939,#8940,#8941,#8942,
#8943,#8944,#8945,#8946,#8947,#8948,#8949,#8950,#8951,#8952,#8953,#8954,
#8955,#8956,#8957,#8958,#8959,#8960,#8961,#8962,#8963,#8964,#8965,#8966,
#8967,#8968,#8969,#8970,#8971,#8972,#8973,#8974,#8975,#8976,#8977,#8978,
#8979,#8980,#8981,#8982,#8983,#8984,#8985));
#9921=AXIS2_PLACEMENT_3D('',#34527,#11799,#11800);
#9922=AXIS2_PLACEMENT_3D('',#34528,#11801,#11802);
#9923=AXIS2_PLACEMENT_3D('',#34530,#11803,#11804);
#9924=AXIS2_PLACEMENT_3D('',#34533,#11805,#11806);
#9925=AXIS2_PLACEMENT_3D('',#34537,#11808,#11809);
#9926=AXIS2_PLACEMENT_3D('',#34541,#11811,#11812);
#9927=AXIS2_PLACEMENT_3D('',#34545,#11814,#11815);
#9928=AXIS2_PLACEMENT_3D('',#34549,#11817,#11818);
#9929=AXIS2_PLACEMENT_3D('',#34553,#11820,#11821);
#9930=AXIS2_PLACEMENT_3D('',#34557,#11823,#11824);
#9931=AXIS2_PLACEMENT_3D('',#34561,#11826,#11827);
#9932=AXIS2_PLACEMENT_3D('',#34565,#11829,#11830);
#9933=AXIS2_PLACEMENT_3D('',#34569,#11832,#11833);
#9934=AXIS2_PLACEMENT_3D('',#34573,#11835,#11836);
#9935=AXIS2_PLACEMENT_3D('',#34577,#11838,#11839);
#9936=AXIS2_PLACEMENT_3D('',#34579,#11841,#11842);
#9937=AXIS2_PLACEMENT_3D('',#34582,#11844,#11845);
#9938=AXIS2_PLACEMENT_3D('',#34583,#11846,#11847);
#9939=AXIS2_PLACEMENT_3D('',#34586,#11849,#11850);
#9940=AXIS2_PLACEMENT_3D('',#34587,#11851,#11852);
#9941=AXIS2_PLACEMENT_3D('',#34589,#11853,#11854);
#9942=AXIS2_PLACEMENT_3D('',#34591,#11855,#11856);
#9943=AXIS2_PLACEMENT_3D('',#34592,#11857,#11858);
#9944=AXIS2_PLACEMENT_3D('',#34593,#11859,#11860);
#9945=AXIS2_PLACEMENT_3D('',#34601,#11861,#11862);
#9946=AXIS2_PLACEMENT_3D('',#34603,#11864,#11865);
#9947=AXIS2_PLACEMENT_3D('',#34604,#11866,#11867);
#9948=AXIS2_PLACEMENT_3D('',#38869,#11879,#11880);
#9949=AXIS2_PLACEMENT_3D('',#39800,#11886,#11887);
#9950=AXIS2_PLACEMENT_3D('',#39801,#11888,#11889);
#9951=AXIS2_PLACEMENT_3D('',#39805,#11891,#11892);
#9952=AXIS2_PLACEMENT_3D('',#39807,#11894,#11895);
#9953=AXIS2_PLACEMENT_3D('',#39811,#11898,#11899);
#9954=AXIS2_PLACEMENT_3D('',#39816,#11901,#11902);
#9955=AXIS2_PLACEMENT_3D('',#39820,#11904,#11905);
#9956=AXIS2_PLACEMENT_3D('',#39823,#11907,#11908);
#9957=AXIS2_PLACEMENT_3D('',#39827,#11910,#11911);
#9958=AXIS2_PLACEMENT_3D('',#39831,#11913,#11914);
#9959=AXIS2_PLACEMENT_3D('',#39835,#11916,#11917);
#9960=AXIS2_PLACEMENT_3D('',#39839,#11919,#11920);
#9961=AXIS2_PLACEMENT_3D('',#39843,#11922,#11923);
#9962=AXIS2_PLACEMENT_3D('',#39847,#11925,#11926);
#9963=AXIS2_PLACEMENT_3D('',#39851,#11928,#11929);
#9964=AXIS2_PLACEMENT_3D('',#39854,#11931,#11932);
#9965=AXIS2_PLACEMENT_3D('',#39855,#11933,#11934);
#9966=AXIS2_PLACEMENT_3D('',#39858,#11937,#11938);
#9967=AXIS2_PLACEMENT_3D('',#39860,#11940,#11941);
#9968=AXIS2_PLACEMENT_3D('',#39862,#11943,#11944);
#9969=AXIS2_PLACEMENT_3D('',#39864,#11946,#11947);
#9970=AXIS2_PLACEMENT_3D('',#39866,#11949,#11950);
#9971=AXIS2_PLACEMENT_3D('',#39868,#11952,#11953);
#9972=AXIS2_PLACEMENT_3D('',#39870,#11955,#11956);
#9973=AXIS2_PLACEMENT_3D('',#39872,#11958,#11959);
#9974=AXIS2_PLACEMENT_3D('',#39874,#11961,#11962);
#9975=AXIS2_PLACEMENT_3D('',#39876,#11964,#11965);
#9976=AXIS2_PLACEMENT_3D('',#39878,#11967,#11968);
#9977=AXIS2_PLACEMENT_3D('',#39880,#11970,#11971);
#9978=AXIS2_PLACEMENT_3D('',#39882,#11973,#11974);
#9979=AXIS2_PLACEMENT_3D('',#39884,#11976,#11977);
#9980=AXIS2_PLACEMENT_3D('',#39886,#11979,#11980);
#9981=AXIS2_PLACEMENT_3D('',#39888,#11982,#11983);
#9982=AXIS2_PLACEMENT_3D('',#39890,#11985,#11986);
#9983=AXIS2_PLACEMENT_3D('',#39891,#11987,#11988);
#9984=AXIS2_PLACEMENT_3D('',#39893,#11990,#11991);
#9985=AXIS2_PLACEMENT_3D('',#39895,#11993,#11994);
#9986=AXIS2_PLACEMENT_3D('',#39897,#11996,#11997);
#11799=DIRECTION('axis',(0.,0.,1.));
#11800=DIRECTION('refdir',(1.,0.,0.));
#11801=DIRECTION('center_axis',(0.,0.,-1.));
#11802=DIRECTION('ref_axis',(0.,-1.,0.));
#11803=DIRECTION('center_axis',(0.,0.,-1.));
#11804=DIRECTION('ref_axis',(0.,1.,0.));
#11805=DIRECTION('center_axis',(0.,0.,-1.));
#11806=DIRECTION('ref_axis',(0.707106781186549,0.707106781186546,0.));
#11807=DIRECTION('',(0.,-1.,0.));
#11808=DIRECTION('center_axis',(0.,0.,1.));
#11809=DIRECTION('ref_axis',(-0.707106781186546,-0.707106781186549,0.));
#11810=DIRECTION('',(1.,0.,0.));
#11811=DIRECTION('center_axis',(0.,0.,1.));
#11812=DIRECTION('ref_axis',(0.707106781186549,-0.707106781186546,0.));
#11813=DIRECTION('',(0.,1.,0.));
#11814=DIRECTION('center_axis',(0.,0.,-1.));
#11815=DIRECTION('ref_axis',(-0.707106781186546,0.707106781186549,0.));
#11816=DIRECTION('',(1.,0.,0.));
#11817=DIRECTION('center_axis',(0.,0.,1.));
#11818=DIRECTION('ref_axis',(0.707106781186549,-0.707106781186546,0.));
#11819=DIRECTION('',(0.,1.,0.));
#11820=DIRECTION('center_axis',(0.,0.,1.));
#11821=DIRECTION('ref_axis',(0.707106781186546,0.707106781186549,0.));
#11822=DIRECTION('',(-1.,0.,0.));
#11823=DIRECTION('center_axis',(0.,0.,-1.));
#11824=DIRECTION('ref_axis',(-0.707106781186549,-0.707106781186546,0.));
#11825=DIRECTION('',(0.,1.,0.));
#11826=DIRECTION('center_axis',(0.,0.,1.));
#11827=DIRECTION('ref_axis',(0.707106781186546,0.707106781186549,0.));
#11828=DIRECTION('',(-1.,0.,0.));
#11829=DIRECTION('center_axis',(0.,0.,1.));
#11830=DIRECTION('ref_axis',(-0.707106781186549,0.707106781186546,0.));
#11831=DIRECTION('',(0.,-1.,0.));
#11832=DIRECTION('center_axis',(0.,0.,-1.));
#11833=DIRECTION('ref_axis',(0.707106781186546,-0.707106781186549,0.));
#11834=DIRECTION('',(-1.,0.,0.));
#11835=DIRECTION('center_axis',(0.,0.,1.));
#11836=DIRECTION('ref_axis',(-0.707106781186549,0.707106781186546,0.));
#11837=DIRECTION('',(0.,-1.,0.));
#11838=DIRECTION('center_axis',(0.,0.,1.));
#11839=DIRECTION('ref_axis',(-0.707106781186546,-0.707106781186549,0.));
#11840=DIRECTION('',(1.,0.,0.));
#11841=DIRECTION('center_axis',(0.,0.,-1.));
#11842=DIRECTION('ref_axis',(0.,-1.,0.));
#11843=DIRECTION('',(0.,0.,1.));
#11844=DIRECTION('center_axis',(0.,0.,-1.));
#11845=DIRECTION('ref_axis',(0.,1.,0.));
#11846=DIRECTION('center_axis',(0.,0.,-1.));
#11847=DIRECTION('ref_axis',(0.,-1.,0.));
#11848=DIRECTION('',(-8.65956056235493E-17,-0.707106781186547,0.707106781186547));
#11849=DIRECTION('center_axis',(0.,0.,-1.));
#11850=DIRECTION('ref_axis',(0.,1.,0.));
#11851=DIRECTION('center_axis',(0.,0.,-1.));
#11852=DIRECTION('ref_axis',(0.,-1.,0.));
#11853=DIRECTION('center_axis',(-1.,1.22464679914735E-16,0.));
#11854=DIRECTION('ref_axis',(1.22464679914735E-16,1.,0.));
#11855=DIRECTION('center_axis',(0.,0.,-1.));
#11856=DIRECTION('ref_axis',(0.,1.,0.));
#11857=DIRECTION('center_axis',(0.,0.,-1.));
#11858=DIRECTION('ref_axis',(0.,1.,0.));
#11859=DIRECTION('center_axis',(0.,0.,1.));
#11860=DIRECTION('ref_axis',(0.,1.,0.));
#11861=DIRECTION('center_axis',(0.,0.,-1.));
#11862=DIRECTION('ref_axis',(0.,1.,0.));
#11863=DIRECTION('',(-8.65956056235493E-17,0.707106781186547,-0.707106781186547));
#11864=DIRECTION('center_axis',(0.,0.,-1.));
#11865=DIRECTION('ref_axis',(0.,1.,0.));
#11866=DIRECTION('center_axis',(0.,0.,-1.));
#11867=DIRECTION('ref_axis',(-0.951797481692839,0.306727165153609,0.));
#11868=DIRECTION('',(-2.319132540328E-14,-6.945061809599E-14,-1.));
#11869=DIRECTION('',(-0.749745402825771,0.433453378048483,-0.499999999999981));
#11870=DIRECTION('',(0.749745402825771,-0.433453378048483,-0.499999999999981));
#11871=DIRECTION('',(0.64330979105792,-0.579786609649618,-0.500000000000016));
#11872=DIRECTION('',(-0.64330979105792,0.579786609649618,-0.500000000000016));
#11873=DIRECTION('',(-0.508789886402224,0.700808712484933,-0.500000000000023));
#11874=DIRECTION('',(0.508789886402224,-0.700808712484933,-0.500000000000023));
#11875=DIRECTION('',(0.352058281587984,-0.791236353035765,-0.499999999999978));
#11876=DIRECTION('',(-0.352058281587984,0.791236353035765,-0.499999999999978));
#11877=DIRECTION('',(-0.1799572419677,0.847121827757601,-0.5));
#11878=DIRECTION('',(0.1799572419677,-0.847121827757601,-0.5));
#11879=DIRECTION('center_axis',(0.,0.,-1.));
#11880=DIRECTION('ref_axis',(0.,-1.,0.));
#11881=DIRECTION('',(0.,0.,-1.));
#11882=DIRECTION('',(0.,0.,-1.));
#11883=DIRECTION('',(0.,0.,-1.));
#11884=DIRECTION('',(0.,0.,-1.));
#11885=DIRECTION('',(0.,0.,-1.));
#11886=DIRECTION('center_axis',(-0.309687603986101,-0.950838360573104,0.));
#11887=DIRECTION('ref_axis',(-0.950838360573104,0.309687603986101,0.));
#11888=DIRECTION('center_axis',(0.0868265938642471,0.0868265938642471,0.992432509138967));
#11889=DIRECTION('ref_axis',(0.996194698091746,5.403663627668E-16,-0.0871557427476577));
#11890=DIRECTION('',(0.0868265938642471,0.0868265938642471,0.992432509138967));
#11891=DIRECTION('center_axis',(0.,0.,1.));
#11892=DIRECTION('ref_axis',(0.707106781186549,0.707106781186546,0.));
#11893=DIRECTION('',(0.0868265938642471,0.0868265938642471,0.992432509138967));
#11894=DIRECTION('center_axis',(0.,-0.996194698091745,0.087155742747664));
#11895=DIRECTION('ref_axis',(1.,0.,0.));
#11896=DIRECTION('',(-0.0868265938642471,-0.0868265938642471,-0.992432509138967));
#11897=DIRECTION('',(1.,0.,0.));
#11898=DIRECTION('center_axis',(0.,0.,-1.));
#11899=DIRECTION('ref_axis',(1.,0.,0.));
#11900=DIRECTION('',(0.,-1.,0.));
#11901=DIRECTION('center_axis',(0.,0.,-1.));
#11902=DIRECTION('ref_axis',(0.707106781186549,-0.707106781186546,0.));
#11903=DIRECTION('',(-1.,0.,-1.932295848749E-14));
#11904=DIRECTION('center_axis',(0.,0.,-1.));
#11905=DIRECTION('ref_axis',(-0.707106781186546,-0.707106781186549,0.));
#11906=DIRECTION('',(0.,-1.,0.));
#11907=DIRECTION('center_axis',(0.,0.,-1.));
#11908=DIRECTION('ref_axis',(-0.707106781186546,-0.707106781186549,0.));
#11909=DIRECTION('',(0.,-1.,0.));
#11910=DIRECTION('center_axis',(0.,0.,-1.));
#11911=DIRECTION('ref_axis',(-0.707106781186549,0.707106781186546,0.));
#11912=DIRECTION('',(1.,0.,0.));
#11913=DIRECTION('center_axis',(0.,0.,1.));
#11914=DIRECTION('ref_axis',(0.707106781186546,-0.707106781186549,0.));
#11915=DIRECTION('',(0.,-1.,0.));
#11916=DIRECTION('center_axis',(0.,0.,-1.));
#11917=DIRECTION('ref_axis',(-0.707106781186549,0.707106781186546,0.));
#11918=DIRECTION('',(1.,0.,-1.932295848749E-14));
#11919=DIRECTION('center_axis',(0.,0.,-1.));
#11920=DIRECTION('ref_axis',(0.707106781186546,0.707106781186549,0.));
#11921=DIRECTION('',(0.,-1.,0.));
#11922=DIRECTION('center_axis',(0.,0.,1.));
#11923=DIRECTION('ref_axis',(-0.707106781186549,-0.707106781186546,0.));
#11924=DIRECTION('',(1.,0.,0.));
#11925=DIRECTION('center_axis',(0.,0.,-1.));
#11926=DIRECTION('ref_axis',(0.707106781186546,0.707106781186549,0.));
#11927=DIRECTION('',(0.,1.,1.932295848749E-14));
#11928=DIRECTION('center_axis',(0.,0.,-1.));
#11929=DIRECTION('ref_axis',(0.707106781186549,-0.707106781186546,0.));
#11930=DIRECTION('',(-1.,0.,0.));
#11931=DIRECTION('center_axis',(0.,0.,1.));
#11932=DIRECTION('ref_axis',(-0.707106781186546,0.707106781186549,0.));
#11933=DIRECTION('center_axis',(0.996194698091745,0.,0.087155742747664));
#11934=DIRECTION('ref_axis',(0.,1.,0.));
#11935=DIRECTION('',(-0.0868265938642471,0.0868265938642471,0.992432509138967));
#11936=DIRECTION('',(0.0868265938642471,-0.0868265938642471,-0.992432509138967));
#11937=DIRECTION('center_axis',(-0.0868265938642471,0.0868265938642471,
0.992432509138967));
#11938=DIRECTION('ref_axis',(-5.403663627668E-16,0.996194698091746,-0.0871557427476577));
#11939=DIRECTION('',(-0.0868265938642471,0.0868265938642471,0.992432509138967));
#11940=DIRECTION('center_axis',(0.,-0.996194698091745,0.087155742747664));
#11941=DIRECTION('ref_axis',(1.,0.,0.));
#11942=DIRECTION('',(0.0868265938642471,-0.0868265938642471,-0.992432509138967));
#11943=DIRECTION('center_axis',(0.0868265938642471,-0.0868265938642471,
-0.992432509138967));
#11944=DIRECTION('ref_axis',(0.996194698091746,-5.403663627668E-16,0.0871557427476577));
#11945=DIRECTION('',(0.0868265938642471,-0.0868265938642471,-0.992432509138967));
#11946=DIRECTION('center_axis',(0.996194698091745,0.,0.087155742747664));
#11947=DIRECTION('ref_axis',(0.,1.,0.));
#11948=DIRECTION('',(0.0868265938642471,0.0868265938642471,-0.992432509138967));
#11949=DIRECTION('center_axis',(0.0868265938642471,0.0868265938642471,-0.992432509138967));
#11950=DIRECTION('ref_axis',(5.403663627668E-16,0.996194698091746,0.0871557427476577));
#11951=DIRECTION('',(0.0868265938642471,0.0868265938642471,-0.992432509138967));
#11952=DIRECTION('center_axis',(0.,0.996194698091745,0.087155742747664));
#11953=DIRECTION('ref_axis',(-1.,0.,0.));
#11954=DIRECTION('',(-0.0868265938642471,-0.0868265938642471,0.992432509138967));
#11955=DIRECTION('center_axis',(-0.0868265938642471,-0.0868265938642471,
0.992432509138967));
#11956=DIRECTION('ref_axis',(-0.996194698091746,-5.403663627668E-16,-0.0871557427476577));
#11957=DIRECTION('',(-0.0868265938642471,-0.0868265938642471,0.992432509138967));
#11958=DIRECTION('center_axis',(0.996194698091745,0.,0.087155742747664));
#11959=DIRECTION('ref_axis',(0.,1.,0.));
#11960=DIRECTION('',(0.0868265938642471,0.0868265938642471,-0.992432509138967));
#11961=DIRECTION('center_axis',(0.0868265938642471,0.0868265938642471,-0.992432509138967));
#11962=DIRECTION('ref_axis',(5.403663627668E-16,0.996194698091746,0.0871557427476577));
#11963=DIRECTION('',(0.0868265938642471,0.0868265938642471,-0.992432509138967));
#11964=DIRECTION('center_axis',(0.,0.996194698091745,0.087155742747664));
#11965=DIRECTION('ref_axis',(-1.,0.,0.));
#11966=DIRECTION('',(-0.0868265938642471,0.0868265938642471,-0.992432509138967));
#11967=DIRECTION('center_axis',(-0.0868265938642471,0.0868265938642471,
-0.992432509138967));
#11968=DIRECTION('ref_axis',(-0.996194698091746,5.403663627668E-16,0.0871557427476577));
#11969=DIRECTION('',(-0.0868265938642471,0.0868265938642471,-0.992432509138967));
#11970=DIRECTION('center_axis',(-0.996194698091745,0.,0.087155742747664));
#11971=DIRECTION('ref_axis',(0.,-1.,0.));
#11972=DIRECTION('',(0.0868265938642471,-0.0868265938642471,0.992432509138967));
#11973=DIRECTION('center_axis',(0.0868265938642471,-0.0868265938642471,
0.992432509138967));
#11974=DIRECTION('ref_axis',(5.403663627668E-16,-0.996194698091746,-0.0871557427476577));
#11975=DIRECTION('',(0.0868265938642471,-0.0868265938642471,0.992432509138967));
#11976=DIRECTION('center_axis',(0.,0.996194698091745,0.087155742747664));
#11977=DIRECTION('ref_axis',(-1.,0.,0.));
#11978=DIRECTION('',(-0.0868265938642471,0.0868265938642471,-0.992432509138967));
#11979=DIRECTION('center_axis',(-0.0868265938642471,0.0868265938642471,
-0.992432509138967));
#11980=DIRECTION('ref_axis',(-0.996194698091746,5.403663627668E-16,0.0871557427476577));
#11981=DIRECTION('',(-0.0868265938642471,0.0868265938642471,-0.992432509138967));
#11982=DIRECTION('center_axis',(-0.996194698091745,0.,0.087155742747664));
#11983=DIRECTION('ref_axis',(0.,-1.,0.));
#11984=DIRECTION('',(-0.0868265938642471,-0.0868265938642471,-0.992432509138967));
#11985=DIRECTION('center_axis',(-0.0868265938642471,-0.0868265938642471,
-0.992432509138967));
#11986=DIRECTION('ref_axis',(-5.403663627668E-16,-0.996194698091746,0.0871557427476577));
#11987=DIRECTION('center_axis',(0.0868265938642471,-0.0868265938642471,
-0.992432509138967));
#11988=DIRECTION('ref_axis',(0.996194698091746,-5.403663627668E-16,0.0871557427476577));
#11989=DIRECTION('',(0.0868265938642471,-0.0868265938642471,-0.992432509138967));
#11990=DIRECTION('center_axis',(0.,-0.996194698091745,0.087155742747664));
#11991=DIRECTION('ref_axis',(1.,0.,0.));
#11992=DIRECTION('',(-0.0868265938642471,-0.0868265938642471,-0.992432509138967));
#11993=DIRECTION('center_axis',(-0.0868265938642471,-0.0868265938642471,
-0.992432509138967));
#11994=DIRECTION('ref_axis',(-5.403663627668E-16,-0.996194698091746,0.0871557427476577));
#11995=DIRECTION('',(-0.0868265938642471,-0.0868265938642471,-0.992432509138967));
#11996=DIRECTION('center_axis',(-0.996194698091745,0.,0.087155742747664));
#11997=DIRECTION('ref_axis',(0.,-1.,0.));
#34527=CARTESIAN_POINT('',(0.,0.,0.));
#34528=CARTESIAN_POINT('Origin',(0.,0.,-12.));
#34529=CARTESIAN_POINT('',(2.87791997799628E-16,2.35,-12.));
#34530=CARTESIAN_POINT('Origin',(0.,0.,-12.));
#34531=CARTESIAN_POINT('',(-0.6490486745229,-0.4,-12.));
#34532=CARTESIAN_POINT('',(-0.4,-0.6490486745229,-12.));
#34533=CARTESIAN_POINT('Origin',(-0.650954959386273,-0.650954959386273,
-12.));
#34534=CARTESIAN_POINT('',(-0.4,-1.100951325477,-12.));
#34535=CARTESIAN_POINT('',(-0.4,-0.6490486745229,-12.));
#34536=CARTESIAN_POINT('',(-0.1509513254771,-1.35,-12.));
#34537=CARTESIAN_POINT('Origin',(-0.149045040613789,-1.09904504061379,-12.));
#34538=CARTESIAN_POINT('',(0.1509513254771,-1.35,-12.));
#34539=CARTESIAN_POINT('',(-0.1509513254771,-1.35,-12.));
#34540=CARTESIAN_POINT('',(0.4,-1.100951325477,-12.));
#34541=CARTESIAN_POINT('Origin',(0.149045040614538,-1.09904504061454,-12.));
#34542=CARTESIAN_POINT('',(0.4,-0.6490486745229,-12.));
#34543=CARTESIAN_POINT('',(0.4,-1.100951325477,-12.));
#34544=CARTESIAN_POINT('',(0.6490486745229,-0.4,-12.));
#34545=CARTESIAN_POINT('Origin',(0.650954959386273,-0.650954959386273,-12.));
#34546=CARTESIAN_POINT('',(1.100951325477,-0.4,-12.));
#34547=CARTESIAN_POINT('',(0.6490486745229,-0.4,-12.));
#34548=CARTESIAN_POINT('',(1.35,-0.1509513254771,-12.));
#34549=CARTESIAN_POINT('Origin',(1.09904504061396,-0.149045040613957,-12.));
#34550=CARTESIAN_POINT('',(1.35,0.1509513254771,-12.));
#34551=CARTESIAN_POINT('',(1.35,-0.1509513254771,-12.));
#34552=CARTESIAN_POINT('',(1.100951325477,0.4,-12.));
#34553=CARTESIAN_POINT('Origin',(1.09904504061419,0.149045040614192,-12.));
#34554=CARTESIAN_POINT('',(0.6490486745229,0.4,-12.));
#34555=CARTESIAN_POINT('',(1.100951325477,0.4,-12.));
#34556=CARTESIAN_POINT('',(0.4,0.6490486745229,-12.));
#34557=CARTESIAN_POINT('Origin',(0.650954959386273,0.650954959386273,-12.));
#34558=CARTESIAN_POINT('',(0.4,1.100951325477,-12.));
#34559=CARTESIAN_POINT('',(0.4,0.6490486745229,-12.));
#34560=CARTESIAN_POINT('',(0.1509513254771,1.35,-12.));
#34561=CARTESIAN_POINT('Origin',(0.149045040614081,1.09904504061408,-12.));
#34562=CARTESIAN_POINT('',(-0.1509513254771,1.35,-12.));
#34563=CARTESIAN_POINT('',(0.1509513254771,1.35,-12.));
#34564=CARTESIAN_POINT('',(-0.4,1.100951325477,-12.));
#34565=CARTESIAN_POINT('Origin',(-0.149045040614321,1.09904504061432,-12.));
#34566=CARTESIAN_POINT('',(-0.4,0.6490486745229,-12.));
#34567=CARTESIAN_POINT('',(-0.4,1.100951325477,-12.));
#34568=CARTESIAN_POINT('',(-0.6490486745229,0.4,-12.));
#34569=CARTESIAN_POINT('Origin',(-0.650954959386273,0.650954959386273,-12.));
#34570=CARTESIAN_POINT('',(-1.100951325477,0.4,-12.));
#34571=CARTESIAN_POINT('',(-0.6490486745229,0.4,-12.));
#34572=CARTESIAN_POINT('',(-1.35,0.1509513254771,-12.));
#34573=CARTESIAN_POINT('Origin',(-1.09904504061453,0.149045040614529,-12.));
#34574=CARTESIAN_POINT('',(-1.35,-0.1509513254771,-12.));
#34575=CARTESIAN_POINT('',(-1.35,0.1509513254771,-12.));
#34576=CARTESIAN_POINT('',(-1.100951325477,-0.4,-12.));
#34577=CARTESIAN_POINT('Origin',(-1.09904504061437,-0.14904504061437,-12.));
#34578=CARTESIAN_POINT('',(-1.100951325477,-0.4,-12.));
#34579=CARTESIAN_POINT('Origin',(0.,0.,0.6));
#34580=CARTESIAN_POINT('',(2.87791997799628E-16,2.35,-11.75));
#34581=CARTESIAN_POINT('',(2.87791997799628E-16,2.35,0.6));
#34582=CARTESIAN_POINT('Origin',(0.,0.,-11.75));
#34583=CARTESIAN_POINT('Origin',(0.,0.,-11.125));
#34584=CARTESIAN_POINT('',(1.34711147906209E-16,1.1,-10.5));
#34585=CARTESIAN_POINT('',(2.11251572852918E-16,1.725,-11.125));
#34586=CARTESIAN_POINT('Origin',(0.,0.,-10.5));
#34587=CARTESIAN_POINT('Origin',(0.,0.,-10.00502525317));
#34588=CARTESIAN_POINT('',(1.34711147906209E-16,1.1,-9.510050506339));
#34589=CARTESIAN_POINT('Origin',(1.95328071842744E-16,1.594974746831,-10.00502525317));
#34590=CARTESIAN_POINT('',(0.,-1.1,-9.510050506339));
#34591=CARTESIAN_POINT('Origin',(0.,0.,-9.510050506339));
#34592=CARTESIAN_POINT('Origin',(0.,0.,-9.510050506339));
#34593=CARTESIAN_POINT('Origin',(0.,0.,-9.435050506339));
#34594=CARTESIAN_POINT('',(1.18854637777596,-0.387097539267644,-9.36025909322078));
#34595=CARTESIAN_POINT('',(1.1909259399931,-0.379730701223331,-9.360050506339));
#34596=CARTESIAN_POINT('Ctrl Pts',(1.18855167546869,-0.387098068634525,
-9.36027610426639));
#34597=CARTESIAN_POINT('Ctrl Pts',(1.18935069806761,-0.384644737745942,
-9.36020090495726));
#34598=CARTESIAN_POINT('Ctrl Pts',(1.19014212463371,-0.382188932913971,
-9.36012570564813));
#34599=CARTESIAN_POINT('Ctrl Pts',(1.1909259399931,-0.379730701223331,-9.360050506339));
#34600=CARTESIAN_POINT('',(1.53080849893419E-16,-1.25,-9.360050506339));
#34601=CARTESIAN_POINT('Origin',(0.,0.,-9.360050506339));
#34602=CARTESIAN_POINT('',(1.43895998899814E-16,-1.175,-9.435050506339));
#34603=CARTESIAN_POINT('Origin',(0.,0.,-9.360050506339));
#34604=CARTESIAN_POINT('Origin',(0.,0.,0.6));
#34605=CARTESIAN_POINT('',(1.18816042873021,-0.386967048621457,-8.91034431420074));
#34606=CARTESIAN_POINT('Ctrl Pts',(1.18855640372918,-0.38708355061195,-8.91058202070716));
#34607=CARTESIAN_POINT('Ctrl Pts',(1.16413132682989,-0.462081781651053,
-8.91508847295526));
#34608=CARTESIAN_POINT('Ctrl Pts',(1.13266199825274,-0.534601882845992,
-8.91946732035472));
#34609=CARTESIAN_POINT('Ctrl Pts',(1.06943293093651,-0.649247028299995,
-8.9267268440218));
#34610=CARTESIAN_POINT('Ctrl Pts',(1.04147855168549,-0.693203093692481,
-8.92960709921868));
#34611=CARTESIAN_POINT('Ctrl Pts',(0.97337862165096,-0.786826391411868,
-8.93616039337431));
#34612=CARTESIAN_POINT('Ctrl Pts',(0.932008000915598,-0.8354165182367,-8.93989564203244));
#34613=CARTESIAN_POINT('Ctrl Pts',(0.832546666127682,-0.935610250253769,
-8.94824133870191));
#34614=CARTESIAN_POINT('Ctrl Pts',(0.772978226416659,-0.985396518974392,
-8.95282616050993));
#34615=CARTESIAN_POINT('Ctrl Pts',(0.618671935476158,-1.09170780359273,
-8.96367433065787));
#34616=CARTESIAN_POINT('Ctrl Pts',(0.520329667238918,-1.14185818423537,
-8.96976236919656));
#34617=CARTESIAN_POINT('Ctrl Pts',(0.371691624455368,-1.19441355795944,
-8.97850737152109));
#34618=CARTESIAN_POINT('Ctrl Pts',(0.325816418750769,-1.2077341218078,-8.98115804797177));
#34619=CARTESIAN_POINT('Ctrl Pts',(0.220615147060026,-1.23184946901154,
-8.98728686123821));
#34620=CARTESIAN_POINT('Ctrl Pts',(0.161047964386293,-1.24104231737691,
-8.99082088203554));
#34621=CARTESIAN_POINT('Ctrl Pts',(0.0238806519370219,-1.2521682136863,
-8.99895621396837));
#34622=CARTESIAN_POINT('Ctrl Pts',(-0.0537157585731863,-1.25124389506131,
-9.00353896719078));
#34623=CARTESIAN_POINT('Ctrl Pts',(-0.239568482987995,-1.23169960660012,
-9.01435748756445));
#34624=CARTESIAN_POINT('Ctrl Pts',(-0.346435839153362,-1.20601051855738,
-9.02042076300827));
#34625=CARTESIAN_POINT('Ctrl Pts',(-0.493347783717673,-1.14952465294486,
-9.02915104624019));
#34626=CARTESIAN_POINT('Ctrl Pts',(-0.537072452143536,-1.12975739849677,
-9.03181314963083));
#34627=CARTESIAN_POINT('Ctrl Pts',(-0.632848812995777,-1.07963919468376,
-9.03795036581202));
#34628=CARTESIAN_POINT('Ctrl Pts',(-0.684056972718885,-1.047942167664,-9.04148084445673));
#34629=CARTESIAN_POINT('Ctrl Pts',(-0.795576763520356,-0.967246630185234,
-9.04961796971787));
#34630=CARTESIAN_POINT('Ctrl Pts',(-0.854015446033157,-0.916060693483113,
-9.0542061050254));
#34631=CARTESIAN_POINT('Ctrl Pts',(-0.983480523777688,-0.779436108665668,
-9.06510343699372));
#34632=CARTESIAN_POINT('Ctrl Pts',(-1.04861434943958,-0.689321925959037,
-9.07123258517349));
#34633=CARTESIAN_POINT('Ctrl Pts',(-1.12346025073986,-0.550074277954606,
-9.08000220024469));
#34634=CARTESIAN_POINT('Ctrl Pts',(-1.14349938581666,-0.507102987868424,
-9.08263399136271));
#34635=CARTESIAN_POINT('Ctrl Pts',(-1.18338925656768,-0.407094063396869,
-9.08874989646326));
#34636=CARTESIAN_POINT('Ctrl Pts',(-1.20164379046778,-0.349551485777399,
-9.09229079738387));
#34637=CARTESIAN_POINT('Ctrl Pts',(-1.23366235105788,-0.21575659514829,
-9.10042397685363));
#34638=CARTESIAN_POINT('Ctrl Pts',(-1.24464131079082,-0.139078612350456,
-9.10499760044744));
#34639=CARTESIAN_POINT('Ctrl Pts',(-1.25311600265331,0.0319140825237386,
-9.11490711541765));
#34640=CARTESIAN_POINT('Ctrl Pts',(-1.24718126828869,0.125932814875664,
-9.12015487713516));
#34641=CARTESIAN_POINT('Ctrl Pts',(-1.22089657875062,0.274054897676782,
-9.12849996685543));
#34642=CARTESIAN_POINT('Ctrl Pts',(-1.20725839404362,0.328970048428431,
-9.13161923643358));
#34643=CARTESIAN_POINT('Ctrl Pts',(-1.17214728603828,0.438122683060954,
-9.13809282547281));
#34644=CARTESIAN_POINT('Ctrl Pts',(-1.15050467962027,0.492156612235245,
-9.1414772579062));
#34645=CARTESIAN_POINT('Ctrl Pts',(-1.06622963442149,0.666312641266624,
-9.15289125023255));
#34646=CARTESIAN_POINT('Ctrl Pts',(-0.987868291319226,0.777780814022605,
-9.16085817819223));
#34647=CARTESIAN_POINT('Ctrl Pts',(-0.835093386727763,0.933813314838567,
-9.17315703402815));
#34648=CARTESIAN_POINT('Ctrl Pts',(-0.771268030342051,0.987184811152829,
-9.17770514022099));
#34649=CARTESIAN_POINT('Ctrl Pts',(-0.657321116790375,1.06462642447898,
-9.1853936547973));
#34650=CARTESIAN_POINT('Ctrl Pts',(-0.610048486753047,1.09240141502545,
-9.18849779461628));
#34651=CARTESIAN_POINT('Ctrl Pts',(-0.508610567848914,1.14335744969678,
-9.19512167880244));
#34652=CARTESIAN_POINT('Ctrl Pts',(-0.454323897972156,1.16599338879742,
-9.19861193166071));
#34653=CARTESIAN_POINT('Ctrl Pts',(-0.312550422081531,1.21369861571125,
-9.20744880516734));
#34654=CARTESIAN_POINT('Ctrl Pts',(-0.223544763956586,1.2332000923951,-9.21272511069972));
#34655=CARTESIAN_POINT('Ctrl Pts',(-0.0561715868345206,1.25113840523285,
-9.22224513286719));
#34656=CARTESIAN_POINT('Ctrl Pts',(0.021464382452435,1.25221492718816,-9.22651245554135));
#34657=CARTESIAN_POINT('Ctrl Pts',(0.159269818008017,1.24129960385597,-9.23419087281889));
#34658=CARTESIAN_POINT('Ctrl Pts',(0.219400811913379,1.23209357394894,-9.23758920462251));
#34659=CARTESIAN_POINT('Ctrl Pts',(0.326356131212141,1.20763766369272,-9.24395278280466));
#34660=CARTESIAN_POINT('Ctrl Pts',(0.373400299605481,1.19393006249441,-9.24684707489846));
#34661=CARTESIAN_POINT('Ctrl Pts',(0.521186162664686,1.1412771440385,-9.25612626363962));
#34662=CARTESIAN_POINT('Ctrl Pts',(0.617746000260806,1.09203603236742,-9.26243472457194));
#34663=CARTESIAN_POINT('Ctrl Pts',(0.771479412321522,0.986647072753507,
-9.27297496860113));
#34664=CARTESIAN_POINT('Ctrl Pts',(0.831858888671005,0.936303404942699,
-9.27729432363076));
#34665=CARTESIAN_POINT('Ctrl Pts',(0.92989420575625,0.837545636596112,-9.28503045659138));
#34666=CARTESIAN_POINT('Ctrl Pts',(0.969465204010896,0.791405612439474,
-9.28843293504891));
#34667=CARTESIAN_POINT('Ctrl Pts',(1.03482248474956,0.702903866462278,-9.29482777606118));
#34668=CARTESIAN_POINT('Ctrl Pts',(1.06174150119686,0.66154072979425,-9.29774880070318));
#34669=CARTESIAN_POINT('Ctrl Pts',(1.13749105883596,0.528559544995029,-9.30681538083952));
#34670=CARTESIAN_POINT('Ctrl Pts',(1.17742084251681,0.432371587683507,-9.3128900576519));
#34671=CARTESIAN_POINT('Ctrl Pts',(1.22453557398548,0.261547640566241,-9.32292858043613));
#34672=CARTESIAN_POINT('Ctrl Pts',(1.23778581263021,0.189159618845307,-9.32698346808543));
#34673=CARTESIAN_POINT('Ctrl Pts',(1.24816957810944,0.077773154565253,-9.33318083186472));
#34674=CARTESIAN_POINT('Ctrl Pts',(1.2499700776908,0.0393777287403109,-9.33531181110441));
#34675=CARTESIAN_POINT('Ctrl Pts',(1.25004417904819,-0.0569489147089241,
-9.34073521958816));
#34676=CARTESIAN_POINT('Ctrl Pts',(1.2460644211611,-0.114784823015238,-9.34409354123995));
#34677=CARTESIAN_POINT('Ctrl Pts',(1.22830219349293,-0.242544049892459,
-9.3516843718206));
#34678=CARTESIAN_POINT('Ctrl Pts',(1.21252321367746,-0.311996505960803,
-9.35590110221895));
#34679=CARTESIAN_POINT('Ctrl Pts',(1.1909259399931,-0.379730701223331,-9.360050506339));
#34680=CARTESIAN_POINT('',(1.188547950716,-0.3871095049826,-8.910050506339));
#34681=CARTESIAN_POINT('Ctrl Pts',(-0.9517960794344,0.08450243785415,-7.598835283632));
#34682=CARTESIAN_POINT('Ctrl Pts',(-0.9318560570757,0.3090975570804,-7.615735374824));
#34683=CARTESIAN_POINT('Ctrl Pts',(-0.7263408395568,0.7424211378759,-7.649535557208));
#34684=CARTESIAN_POINT('Ctrl Pts',(-0.06894632644086,1.036484977236,-7.700235830784));
#34685=CARTESIAN_POINT('Ctrl Pts',(0.6215603569723,0.832233457129,-7.75093610436));
#34686=CARTESIAN_POINT('Ctrl Pts',(1.013379111199,0.2281099298227,-7.801636377936));
#34687=CARTESIAN_POINT('Ctrl Pts',(0.9182129530189,-0.4856491429445,-7.852336651512));
#34688=CARTESIAN_POINT('Ctrl Pts',(0.3817962122075,-0.9660231513296,-7.903036925088));
#34689=CARTESIAN_POINT('Ctrl Pts',(-0.3380943571131,-0.9821719785036,-7.953737198664));
#34690=CARTESIAN_POINT('Ctrl Pts',(-0.8955122787772,-0.5263337477631,-8.00443747224));
#34691=CARTESIAN_POINT('Ctrl Pts',(-1.022588136825,0.1824362236354,-8.055137745816));
#34692=CARTESIAN_POINT('Ctrl Pts',(-0.6582551008476,0.8035357477226,-8.105838019392));
#34693=CARTESIAN_POINT('Ctrl Pts',(0.02240510300165,1.038492891054,-8.156538292968));
#34694=CARTESIAN_POINT('Ctrl Pts',(0.6922984435386,0.7743980496026,-8.207238566544));
#34695=CARTESIAN_POINT('Ctrl Pts',(1.029504948709,0.1381630724743,-8.25793884012));
#34696=CARTESIAN_POINT('Ctrl Pts',(0.8719786597657,-0.5644667314643,-8.308639113696));
#34697=CARTESIAN_POINT('Ctrl Pts',(0.2954194761216,-0.9958397497356,-8.359339387272));
#34698=CARTESIAN_POINT('Ctrl Pts',(-0.4231047393978,-0.9486579222881,-8.410039660848));
#34699=CARTESIAN_POINT('Ctrl Pts',(-0.9383042499798,-0.4455946683874,-8.460739934424));
#34700=CARTESIAN_POINT('Ctrl Pts',(-1.002597833476,0.2716009173896,-8.511440208));
#34701=CARTESIAN_POINT('Ctrl Pts',(-0.58508894663,0.8582775766289,-8.562140481576));
#34702=CARTESIAN_POINT('Ctrl Pts',(0.1135868154433,1.032505452534,-8.612840755152));
#34703=CARTESIAN_POINT('Ctrl Pts',(0.7576779706553,0.7105586296663,-8.663541028728));
#34704=CARTESIAN_POINT('Ctrl Pts',(1.037663893743,0.04714996588551,-8.714241302304));
#34705=CARTESIAN_POINT('Ctrl Pts',(0.8189962043018,-0.6389168103985,-8.76494157588));
#34706=CARTESIAN_POINT('Ctrl Pts',(0.2067565703236,-1.017949495851,-8.815641849456));
#34707=CARTESIAN_POINT('Ctrl Pts',(-0.5048408330584,-0.9078024691232,-8.866342123032));
#34708=CARTESIAN_POINT('Ctrl Pts',(-0.9738347030632,-0.3614070387674,-8.917042396608));
#34709=CARTESIAN_POINT('Ctrl Pts',(-0.9748491478262,0.3586631513228,-8.967742670184));
#34710=CARTESIAN_POINT('Ctrl Pts',(-0.50739285913,0.9063795284549,-9.01844294376));
#34711=CARTESIAN_POINT('Ctrl Pts',(0.2038819114907,1.018519499416,-9.069143217336));
#34712=CARTESIAN_POINT('Ctrl Pts',(0.8172222809373,0.6412506900624,-9.119843490912));
#34713=CARTESIAN_POINT('Ctrl Pts',(1.037686853011,-0.04434136061689,-9.170543764488));
#34714=CARTESIAN_POINT('Ctrl Pts',(0.8526090282577,-0.4867800898099,-9.204343946872));
#34715=CARTESIAN_POINT('Ctrl Pts',(0.6988314801645,-0.6516832061369,-9.221244038064));
#34716=CARTESIAN_POINT('Ctrl Pts',(-1.054366052901,0.09360881367962,-7.65828701626));
#34717=CARTESIAN_POINT('Ctrl Pts',(-1.032277200968,0.3424073478153,-7.675187107452));
#34718=CARTESIAN_POINT('Ctrl Pts',(-0.8046147075109,0.8224278935856,-7.708987289836));
#34719=CARTESIAN_POINT('Ctrl Pts',(-0.07637630333028,1.148181420319,-7.759687563412));
#34720=CARTESIAN_POINT('Ctrl Pts',(0.6885425926632,0.9219188061864,-7.810387836988));
#34721=CARTESIAN_POINT('Ctrl Pts',(1.122585558665,0.2526921170736,-7.861088110564));
#34722=CARTESIAN_POINT('Ctrl Pts',(1.017163852547,-0.5379849539255,-7.91178838414));
#34723=CARTESIAN_POINT('Ctrl Pts',(0.4229403482276,-1.070126300251,-7.962488657716));
#34724=CARTESIAN_POINT('Ctrl Pts',(-0.3745289779184,-1.088015400168,-8.013188931292));
#34725=CARTESIAN_POINT('Ctrl Pts',(-0.9920168480411,-0.5830539210323,-8.063889204868));
#34726=CARTESIAN_POINT('Ctrl Pts',(-1.132786991735,0.2020963998243,-8.114589478445));
#34727=CARTESIAN_POINT('Ctrl Pts',(-0.7291917328499,0.8901284981069,-8.165289752021));
#34728=CARTESIAN_POINT('Ctrl Pts',(0.02481958113415,1.150405716271,-8.215990025596));
#34729=CARTESIAN_POINT('Ctrl Pts',(0.7669037445257,0.857850786083,-8.266690299173));
#34730=CARTESIAN_POINT('Ctrl Pts',(1.140449191446,0.1530521679265,-8.317390572749));
#34731=CARTESIAN_POINT('Ctrl Pts',(0.9659471367619,-0.6252962924595,-8.368090846325));
#34732=CARTESIAN_POINT('Ctrl Pts',(0.3272552532192,-1.103156074014,-8.418791119901));
#34733=CARTESIAN_POINT('Ctrl Pts',(-0.4687004744835,-1.050889713341,-8.469491393477));
#34734=CARTESIAN_POINT('Ctrl Pts',(-1.039420281137,-0.4936140228487,-8.520191667053));
#34735=CARTESIAN_POINT('Ctrl Pts',(-1.110642440297,0.3008698957896,-8.570891940629));
#34736=CARTESIAN_POINT('Ctrl Pts',(-0.6481408534701,0.9507695611661,-8.621592214205));
#34737=CARTESIAN_POINT('Ctrl Pts',(0.1258274591041,1.143773043521,-8.672292487781));
#34738=CARTESIAN_POINT('Ctrl Pts',(0.8393288736432,0.7871317332605,-8.722992761357));
#34739=CARTESIAN_POINT('Ctrl Pts',(1.149487382353,0.05223106556044,-8.773693034933));
#34740=CARTESIAN_POINT('Ctrl Pts',(0.9072550454121,-0.7077694582564,-8.824393308509));
#34741=CARTESIAN_POINT('Ctrl Pts',(0.2290376202147,-1.127648469229,-8.875093582085));
#34742=CARTESIAN_POINT('Ctrl Pts',(-0.5592448298497,-1.005631486475,-8.925793855661));
#34743=CARTESIAN_POINT('Ctrl Pts',(-1.07877966114,-0.4003539426031,-8.976494129237));
#34744=CARTESIAN_POINT('Ctrl Pts',(-1.07990342719,0.3973143610824,-9.027194402813));
#34745=CARTESIAN_POINT('Ctrl Pts',(-0.5620718741233,1.004055203101,-9.077894676389));
#34746=CARTESIAN_POINT('Ctrl Pts',(0.2258531747725,1.128279899031,-9.128594949965));
#34747=CARTESIAN_POINT('Ctrl Pts',(0.9052899558132,0.7103548476505,-9.179295223541));
#34748=CARTESIAN_POINT('Ctrl Pts',(1.149512815819,-0.04911979192188,-9.229995497117));
#34749=CARTESIAN_POINT('Ctrl Pts',(0.9444901436511,-0.5392377768865,-9.263795679501));
#34750=CARTESIAN_POINT('Ctrl Pts',(0.7741408115714,-0.7219116201914,-9.280695770693));
#34751=CARTESIAN_POINT('Ctrl Pts',(-1.156936026367,0.1027151895051,-7.717738748889));
#34752=CARTESIAN_POINT('Ctrl Pts',(-1.13269834486,0.3757171385502,-7.734638840081));
#34753=CARTESIAN_POINT('Ctrl Pts',(-0.882888575465,0.9024346492954,-7.768439022465));
#34754=CARTESIAN_POINT('Ctrl Pts',(-0.0838062802197,1.259877863402,-7.819139296041));
#34755=CARTESIAN_POINT('Ctrl Pts',(0.7555248283541,1.011604155244,-7.869839569617));
#34756=CARTESIAN_POINT('Ctrl Pts',(1.231792006131,0.2772743043245,-7.920539843193));
#34757=CARTESIAN_POINT('Ctrl Pts',(1.116114752076,-0.5903207649065,-7.971240116769));
#34758=CARTESIAN_POINT('Ctrl Pts',(0.4640844842477,-1.174229449172,-8.021940390345));
#34759=CARTESIAN_POINT('Ctrl Pts',(-0.4109635987238,-1.193858821833,-8.072640663921));
#34760=CARTESIAN_POINT('Ctrl Pts',(-1.088521417305,-0.6397740943015,-8.123340937497));
#34761=CARTESIAN_POINT('Ctrl Pts',(-1.242985846645,0.2217565760132,-8.174041211073));
#34762=CARTESIAN_POINT('Ctrl Pts',(-0.8001283648521,0.9767212484911,-8.224741484649));
#34763=CARTESIAN_POINT('Ctrl Pts',(0.02723405926664,1.262318541488,-8.275441758225));
#34764=CARTESIAN_POINT('Ctrl Pts',(0.8415090455128,0.9413035225634,-8.326142031801));
#34765=CARTESIAN_POINT('Ctrl Pts',(1.251393434183,0.1679412633786,-8.376842305377));
#34766=CARTESIAN_POINT('Ctrl Pts',(1.059915613758,-0.6861258534547,-8.427542578953));
#34767=CARTESIAN_POINT('Ctrl Pts',(0.3590910303168,-1.210472398292,-8.478242852529));
#34768=CARTESIAN_POINT('Ctrl Pts',(-0.5142962095692,-1.153121504394,-8.528943126105));
#34769=CARTESIAN_POINT('Ctrl Pts',(-1.140536312295,-0.54163337731,-8.579643399681));
#34770=CARTESIAN_POINT('Ctrl Pts',(-1.218687047119,0.3301388741895,-8.630343673257));
#34771=CARTESIAN_POINT('Ctrl Pts',(-0.7111927603103,1.043261545703,-8.681043946833));
#34772=CARTESIAN_POINT('Ctrl Pts',(0.1380681027649,1.255040634509,-8.731744220409));
#34773=CARTESIAN_POINT('Ctrl Pts',(0.9209797766311,0.8637048368548,-8.782444493985));
#34774=CARTESIAN_POINT('Ctrl Pts',(1.261310870964,0.05731216523537,-8.833144767561));
#34775=CARTESIAN_POINT('Ctrl Pts',(0.9955138865225,-0.7766221061142,-8.883845041137));
#34776=CARTESIAN_POINT('Ctrl Pts',(0.2513186701059,-1.237347442608,-8.934545314713));
#34777=CARTESIAN_POINT('Ctrl Pts',(-0.613648826641,-1.103460503827,-8.985245588289));
#34778=CARTESIAN_POINT('Ctrl Pts',(-1.183724619217,-0.4393008464387,-9.035945861865));
#34779=CARTESIAN_POINT('Ctrl Pts',(-1.184957706554,0.4359655708419,-9.086646135441));
#34780=CARTESIAN_POINT('Ctrl Pts',(-0.6167508891167,1.101730877747,-9.137346409017));
#34781=CARTESIAN_POINT('Ctrl Pts',(0.2478244380543,1.238040298645,-9.188046682593));
#34782=CARTESIAN_POINT('Ctrl Pts',(0.9933576306892,0.7794590052386,-9.238746956169));
#34783=CARTESIAN_POINT('Ctrl Pts',(1.261338778627,-0.05389822322687,-9.289447229745));
#34784=CARTESIAN_POINT('Ctrl Pts',(1.036371259045,-0.5916954639631,-9.323247412129));
#34785=CARTESIAN_POINT('Ctrl Pts',(0.8494501429783,-0.7921400342458,-9.340147503321));
#34786=CARTESIAN_POINT('Ctrl Pts',(-1.259505999833,0.1118215653306,-7.777190481517));
#34787=CARTESIAN_POINT('Ctrl Pts',(-1.233119488752,0.4090269292851,-7.794090572709));
#34788=CARTESIAN_POINT('Ctrl Pts',(-0.9611624434191,0.9824414050051,-7.827890755093));
#34789=CARTESIAN_POINT('Ctrl Pts',(-0.09123625710912,1.371574306486,-7.878591028669));
#34790=CARTESIAN_POINT('Ctrl Pts',(0.8225070640451,1.101289504301,-7.929291302245));
#34791=CARTESIAN_POINT('Ctrl Pts',(1.340998453597,0.3018564915754,-7.979991575821));
#34792=CARTESIAN_POINT('Ctrl Pts',(1.215065651604,-0.6426565758875,-8.030691849397));
#34793=CARTESIAN_POINT('Ctrl Pts',(0.5052286202678,-1.278332598092,-8.081392122973));
#34794=CARTESIAN_POINT('Ctrl Pts',(-0.4473982195291,-1.299702243498,-8.132092396549));
#34795=CARTESIAN_POINT('Ctrl Pts',(-1.185025986569,-0.6964942675707,-8.182792670125));
#34796=CARTESIAN_POINT('Ctrl Pts',(-1.353184701554,0.2414167522021,-8.233492943701));
#34797=CARTESIAN_POINT('Ctrl Pts',(-0.8710649968543,1.063313998875,-8.284193217277));
#34798=CARTESIAN_POINT('Ctrl Pts',(0.02964853739914,1.374231366706,-8.334893490853));
#34799=CARTESIAN_POINT('Ctrl Pts',(0.9161143464999,1.024756259044,-8.385593764429));
#34800=CARTESIAN_POINT('Ctrl Pts',(1.362337676919,0.1828303588308,-8.436294038005));
#34801=CARTESIAN_POINT('Ctrl Pts',(1.153884090754,-0.7469554144499,-8.486994311581));
#34802=CARTESIAN_POINT('Ctrl Pts',(0.3909268074144,-1.31778872257,-8.537694585157));
#34803=CARTESIAN_POINT('Ctrl Pts',(-0.5598919446549,-1.255353295447,-8.588394858733));
#34804=CARTESIAN_POINT('Ctrl Pts',(-1.241652343453,-0.5896527317712,-8.639095132309));
#34805=CARTESIAN_POINT('Ctrl Pts',(-1.326731653941,0.3594078525894,-8.689795405885));
#34806=CARTESIAN_POINT('Ctrl Pts',(-0.7742446671504,1.13575353024,-8.740495679461));
#34807=CARTESIAN_POINT('Ctrl Pts',(0.1503087464258,1.366308225497,-8.791195953037));
#34808=CARTESIAN_POINT('Ctrl Pts',(1.002630679619,0.940277940449,-8.841896226613));
#34809=CARTESIAN_POINT('Ctrl Pts',(1.373134359574,0.0623932649103,-8.892596500189));
#34810=CARTESIAN_POINT('Ctrl Pts',(1.083772727633,-0.8454747539721,-8.943296773765));
#34811=CARTESIAN_POINT('Ctrl Pts',(0.273599719997,-1.347046415986,-8.993997047341));
#34812=CARTESIAN_POINT('Ctrl Pts',(-0.6680528234323,-1.201289521179,-9.044697320917));
#34813=CARTESIAN_POINT('Ctrl Pts',(-1.288669577293,-0.4782477502744,-9.095397594493));
#34814=CARTESIAN_POINT('Ctrl Pts',(-1.290011985917,0.4746167806014,-9.146097868069));
#34815=CARTESIAN_POINT('Ctrl Pts',(-0.67142990411,1.199406552392,-9.196798141645));
#34816=CARTESIAN_POINT('Ctrl Pts',(0.2697957013361,1.347800698259,-9.247498415221));
#34817=CARTESIAN_POINT('Ctrl Pts',(1.081425305565,0.8485631628267,-9.298198688797));
#34818=CARTESIAN_POINT('Ctrl Pts',(1.373164741435,-0.05867665453186,-9.348898962373));
#34819=CARTESIAN_POINT('Ctrl Pts',(1.128252374438,-0.6441531510397,-9.382699144757));
#34820=CARTESIAN_POINT('Ctrl Pts',(0.9247594743852,-0.8623684483003,-9.399599235949));
#34821=CARTESIAN_POINT('',(-1.08160103122666,0.6253104283322,-7.79966651028448));
#34822=CARTESIAN_POINT('Ctrl Pts',(1.18776445373124,-0.386850546630963,
-8.91010660769432));
#34823=CARTESIAN_POINT('Ctrl Pts',(1.21389894012659,-0.306820959780672,
-8.90533140571819));
#34824=CARTESIAN_POINT('Ctrl Pts',(1.23211911862249,-0.224180891334396,
-8.90053865713262));
#34825=CARTESIAN_POINT('Ctrl Pts',(1.25122914691389,-0.0591545543099526,
-8.89095571903426));
#34826=CARTESIAN_POINT('Ctrl Pts',(1.25248415592327,0.0224681132745424,
-8.88617355801157));
#34827=CARTESIAN_POINT('Ctrl Pts',(1.23165538021362,0.264497851938584,-8.87211169336854));
#34828=CARTESIAN_POINT('Ctrl Pts',(1.1863428738656,0.422140450351668,-8.86306238556405));
#34829=CARTESIAN_POINT('Ctrl Pts',(1.04450419562274,0.703018871730047,-8.84517378678212));
#34830=CARTESIAN_POINT('Ctrl Pts',(0.953795594053522,0.822133201515228,
-8.83652591928527));
#34831=CARTESIAN_POINT('Ctrl Pts',(0.780308428421203,0.979376320474896,
-8.82305675175317));
#34832=CARTESIAN_POINT('Ctrl Pts',(0.713162962239612,1.02897046095915,-8.8183374927106));
#34833=CARTESIAN_POINT('Ctrl Pts',(0.525446965343875,1.14122663202712,-8.80593816453637));
#34834=CARTESIAN_POINT('Ctrl Pts',(0.397793799379734,1.19237167907088,-8.79825794581198));
#34835=CARTESIAN_POINT('Ctrl Pts',(0.192918828743436,1.23724963922957,-8.78608919494597));
#34836=CARTESIAN_POINT('Ctrl Pts',(0.119687913895011,1.24636780342359,-8.78177732780935));
#34837=CARTESIAN_POINT('Ctrl Pts',(-0.03729988052084,1.25168049021511,-8.77273368780758));
#34838=CARTESIAN_POINT('Ctrl Pts',(-0.120613512342985,1.24613473199111,
-8.76801130831823));
#34839=CARTESIAN_POINT('Ctrl Pts',(-0.33665447329556,1.21044436773023,-8.75559831193133));
#34840=CARTESIAN_POINT('Ctrl Pts',(-0.467335101319121,1.16686544864178,
-8.74791083973229));
#34841=CARTESIAN_POINT('Ctrl Pts',(-0.65008425343955,1.07001048351806,-8.7359203427984));
#34842=CARTESIAN_POINT('Ctrl Pts',(-0.709377937988781,1.03157766149706,
-8.73178757367245));
#34843=CARTESIAN_POINT('Ctrl Pts',(-0.830858325738161,0.936965587454319,
-8.72290880511093));
#34844=CARTESIAN_POINT('Ctrl Pts',(-0.891244037039048,0.879305104391163,
-8.71818155284362));
#34845=CARTESIAN_POINT('Ctrl Pts',(-1.03546993961214,0.711901864368004,
-8.70565107281324));
#34846=CARTESIAN_POINT('Ctrl Pts',(-1.10864028494722,0.592727437309925,
-8.6978574373626));
#34847=CARTESIAN_POINT('Ctrl Pts',(-1.18512691006641,0.402970729603967,
-8.68600895298831));
#34848=CARTESIAN_POINT('Ctrl Pts',(-1.20481770744938,0.339515965118515,
-8.6821193980736));
#34849=CARTESIAN_POINT('Ctrl Pts',(-1.25429322635665,0.117218312956503,
-8.66895700908858));
#34850=CARTESIAN_POINT('Ctrl Pts',(-1.25838642150074,-0.0469307628035679,
-8.6598986947173));
#34851=CARTESIAN_POINT('Ctrl Pts',(-1.20751589435409,-0.355952994894355,
-8.64207574335479));
#34852=CARTESIAN_POINT('Ctrl Pts',(-1.15759529077901,-0.494611154047977,
-8.63355031817807));
#34853=CARTESIAN_POINT('Ctrl Pts',(-1.04190025748575,-0.694611964138388,
-8.62025658208172));
#34854=CARTESIAN_POINT('Ctrl Pts',(-0.993076972439734,-0.762340311683917,
-8.6155365106255));
#34855=CARTESIAN_POINT('Ctrl Pts',(-0.848865411150693,-0.92616222486434,
-8.60316511958854));
#34856=CARTESIAN_POINT('Ctrl Pts',(-0.743338004112428,-1.01355212264371,
-8.59551429489102));
#34857=CARTESIAN_POINT('Ctrl Pts',(-0.562747984357402,-1.11860166499361,
-8.58339622816306));
#34858=CARTESIAN_POINT('Ctrl Pts',(-0.496143011593621,-1.14959386922681,
-8.57910315151415));
#34859=CARTESIAN_POINT('Ctrl Pts',(-0.348671160649515,-1.20272546073072,
-8.57007625207931));
#34860=CARTESIAN_POINT('Ctrl Pts',(-0.26767690493351,-1.22301508983132,
-8.56535305329552));
#34861=CARTESIAN_POINT('Ctrl Pts',(-0.0507253936393136,-1.25540256524797,
-8.55291722473983));
#34862=CARTESIAN_POINT('Ctrl Pts',(0.0874273983933683,-1.25396265423072,
-8.54520870480266));
#34863=CARTESIAN_POINT('Ctrl Pts',(0.290674642156742,-1.21775450942126,
-8.53324200794464));
#34864=CARTESIAN_POINT('Ctrl Pts',(0.358162640473183,-1.19958054989174,
-8.52915331582327));
#34865=CARTESIAN_POINT('Ctrl Pts',(0.502149049544538,-1.14721725217231,
-8.52031534143725));
#34866=CARTESIAN_POINT('Ctrl Pts',(0.577345283375127,-1.11094026511625,
-8.51558709715192));
#34867=CARTESIAN_POINT('Ctrl Pts',(0.766486872415107,-0.995800335897715,
-8.50302902871571));
#34868=CARTESIAN_POINT('Ctrl Pts',(0.873103246093958,-0.904545584898014,
-8.49521040437098));
#34869=CARTESIAN_POINT('Ctrl Pts',(1.0038874648777,-0.747665133688777,-8.48338487869549));
#34870=CARTESIAN_POINT('Ctrl Pts',(1.04168379062914,-0.694013561883215,
-8.47954245776677));
#34871=CARTESIAN_POINT('Ctrl Pts',(1.15695333587187,-0.49851202972154,-8.4664186607839));
#34872=CARTESIAN_POINT('Ctrl Pts',(1.21147962906974,-0.343598554649147,
-8.45735706141955));
#34873=CARTESIAN_POINT('Ctrl Pts',(1.25980138563557,-0.0247520127629011,
-8.43900920418887));
#34874=CARTESIAN_POINT('Ctrl Pts',(1.25307161001532,0.131747980462025,-8.4299541617984));
#34875=CARTESIAN_POINT('Ctrl Pts',(1.19749640573096,0.365854046723757,-8.41614095741044));
#34876=CARTESIAN_POINT('Ctrl Pts',(1.17023996598552,0.444726326046827,-8.41142976340279));
#34877=CARTESIAN_POINT('Ctrl Pts',(1.08037111576438,0.640759304746671,-8.39920900687085));
#34878=CARTESIAN_POINT('Ctrl Pts',(1.00627911447861,0.752822141300582,-8.39169165367907));
#34879=CARTESIAN_POINT('Ctrl Pts',(0.861460438207615,0.909357876985145,
-8.37930071660415));
#34880=CARTESIAN_POINT('Ctrl Pts',(0.801207019656219,0.962639425462861,
-8.37461729888086));
#34881=CARTESIAN_POINT('Ctrl Pts',(0.668766012044842,1.0585690345103,-8.3652322592572));
#34882=CARTESIAN_POINT('Ctrl Pts',(0.596660491617955,1.10055509444973,-8.36052258402282));
#34883=CARTESIAN_POINT('Ctrl Pts',(0.395567112013034,1.19282720630039,-8.34798466330117));
#34884=CARTESIAN_POINT('Ctrl Pts',(0.244779745730883,1.23744693839987,-8.33921484735322));
#34885=CARTESIAN_POINT('Ctrl Pts',(-0.0942681465773919,1.25790359116205,
-8.31940062305443));
#34886=CARTESIAN_POINT('Ctrl Pts',(-0.252399206177538,1.23164286082107,
-8.31048791289327));
#34887=CARTESIAN_POINT('Ctrl Pts',(-0.467784515236734,1.16126395467836,
-8.29764481620107));
#34888=CARTESIAN_POINT('Ctrl Pts',(-0.544357799543096,1.12769434725901,
-8.2929197281268));
#34889=CARTESIAN_POINT('Ctrl Pts',(-0.749776900489063,1.01188378011857,
-8.27935841353761));
#34890=CARTESIAN_POINT('Ctrl Pts',(-0.86600004791654,0.914361460489527,
-8.27058987911233));
#34891=CARTESIAN_POINT('Ctrl Pts',(-1.06710474253659,0.668642688893352,
-8.25252788742803));
#34892=CARTESIAN_POINT('Ctrl Pts',(-1.14559934894644,0.524176456154759,
-8.24345516230645));
#34893=CARTESIAN_POINT('Ctrl Pts',(-1.21407898851338,0.305145856830464,
-8.2301790680903));
#34894=CARTESIAN_POINT('Ctrl Pts',(-1.22884349703746,0.238818066053841,
-8.22620043878002));
#34895=CARTESIAN_POINT('Ctrl Pts',(-1.25612073580432,0.0381673751078928,
-8.21449039586409));
#34896=CARTESIAN_POINT('Ctrl Pts',(-1.25237495437913,-0.0978504113494669,
-8.20690262720282));
#34897=CARTESIAN_POINT('Ctrl Pts',(-1.21277993941473,-0.310697275105849,
-8.19462470009645));
#34898=CARTESIAN_POINT('Ctrl Pts',(-1.18991780553033,-0.390117925561385,
-8.18994440728262));
#34899=CARTESIAN_POINT('Ctrl Pts',(-1.13233970320381,-0.534318190632865,
-8.18099119971793));
#34900=CARTESIAN_POINT('Ctrl Pts',(-1.09944107541918,-0.599225333096936,
-8.17673410877417));
#34901=CARTESIAN_POINT('Ctrl Pts',(-0.991820469578933,-0.771094829383288,
-8.16498621219696));
#34902=CARTESIAN_POINT('Ctrl Pts',(-0.905499002400952,-0.87005822003041,
-8.15764317860667));
#34903=CARTESIAN_POINT('Ctrl Pts',(-0.743019333840984,-1.0076087936808,
-8.14557711844874));
#34904=CARTESIAN_POINT('Ctrl Pts',(-0.674259098429422,-1.05517283860462,
-8.14085222770922));
#34905=CARTESIAN_POINT('Ctrl Pts',(-0.467693144054769,-1.16935883593837,
-8.12727963908351));
#34906=CARTESIAN_POINT('Ctrl Pts',(-0.323432900325891,-1.21716972897081,
-8.11849635205365));
#34907=CARTESIAN_POINT('Ctrl Pts',(-0.00839329125265246,-1.25925588611344,
-8.1004166149262));
#34908=CARTESIAN_POINT('Ctrl Pts',(0.155770183168729,-1.25015882797825,
-8.09134373978432));
#34909=CARTESIAN_POINT('Ctrl Pts',(0.378090424983517,-1.19337570940643,
-8.07806902379924));
#34910=CARTESIAN_POINT('Ctrl Pts',(0.442257656224971,-1.1711079765006,-8.0740921478462));
#34911=CARTESIAN_POINT('Ctrl Pts',(0.627331812925779,-1.08892563459141,
-8.06238196293534));
#34912=CARTESIAN_POINT('Ctrl Pts',(0.741135647012046,-1.01427047048467,
-8.05479229283736));
#34913=CARTESIAN_POINT('Ctrl Pts',(0.90147328248282,-0.8687435346021,-8.04251237370774));
#34914=CARTESIAN_POINT('Ctrl Pts',(0.957042269146757,-0.807569407056488,
-8.03783206363229));
#34915=CARTESIAN_POINT('Ctrl Pts',(1.04947806804033,-0.682848148974821,
-8.02888040521705));
#34916=CARTESIAN_POINT('Ctrl Pts',(1.08741193471821,-0.620783689543349,
-8.02462500675817));
#34917=CARTESIAN_POINT('Ctrl Pts',(1.17713726084828,-0.43892047919556,-8.0128768113644));
#34918=CARTESIAN_POINT('Ctrl Pts',(1.21601424604425,-0.313444814789549,
-8.00553174425828));
#34919=CARTESIAN_POINT('Ctrl Pts',(1.24770477684024,-0.102893502083894,
-7.99346343954392));
#34920=CARTESIAN_POINT('Ctrl Pts',(1.25205457048966,-0.0193983088591022,
-7.98873843434158));
#34921=CARTESIAN_POINT('Ctrl Pts',(1.24069759299588,0.216343298148389,-7.97516608454395));
#34922=CARTESIAN_POINT('Ctrl Pts',(1.20559856560545,0.364165796579141,-7.96638552286236));
#34923=CARTESIAN_POINT('Ctrl Pts',(1.0759763873466,0.654265009491629,-7.94831191257458));
#34924=CARTESIAN_POINT('Ctrl Pts',(0.982021918408664,0.789167333114058,
-7.93924045402717));
#34925=CARTESIAN_POINT('Ctrl Pts',(0.817143064963047,0.948332669867251,
-7.92598182701509));
#34926=CARTESIAN_POINT('Ctrl Pts',(0.764713742800238,0.991091263345376,
-7.92202024240717));
#34927=CARTESIAN_POINT('Ctrl Pts',(0.597517633845365,1.10562433966725,-7.91029806502895));
#34928=CARTESIAN_POINT('Ctrl Pts',(0.473816334907365,1.16346589742896,-7.90268225435661));
#34929=CARTESIAN_POINT('Ctrl Pts',(0.26536034312891,1.22350762209489,-7.8903783660904));
#34930=CARTESIAN_POINT('Ctrl Pts',(0.184146668761152,1.23863100039534,-7.88569985192011));
#34931=CARTESIAN_POINT('Ctrl Pts',(0.0284444971547855,1.25182002642501,
-7.8766907966508));
#34932=CARTESIAN_POINT('Ctrl Pts',(-0.0453326676439841,1.25137631558713,
-7.87237566436378));
#34933=CARTESIAN_POINT('Ctrl Pts',(-0.247385731590191,1.23159625989491,
-7.86062600752601));
#34934=CARTESIAN_POINT('Ctrl Pts',(-0.373685811337089,1.19876010514595,
-7.85333502383646));
#34935=CARTESIAN_POINT('Ctrl Pts',(-0.613162646726261,1.09626220568374,
-7.83857475953763));
#34936=CARTESIAN_POINT('Ctrl Pts',(-0.726484208237983,1.02564926372048,
-7.83105155416904));
#34937=CARTESIAN_POINT('Ctrl Pts',(-0.942729737103368,0.83543644984202,
-7.81423238529045));
#34938=CARTESIAN_POINT('Ctrl Pts',(-1.02459105923527,0.723752586323567,
-7.80643818382151));
#34939=CARTESIAN_POINT('Ctrl Pts',(-1.08145884712781,0.625207535945593,
-7.79998476760701));
#34940=CARTESIAN_POINT('',(-0.839759385524655,0.485493530587476,-7.63838400393921));
#34941=CARTESIAN_POINT('',(-0.8397594776816,0.485493583525,-7.638384013243));
#34942=CARTESIAN_POINT('',(0.921755949282111,-0.300215476520474,-9.19840833878276));
#34943=CARTESIAN_POINT('Ctrl Pts',(-0.839251282090052,0.485201661780047,
-7.63836822668404));
#34944=CARTESIAN_POINT('Ctrl Pts',(-0.786839191115696,0.57623383833446,
-7.64612438145625));
#34945=CARTESIAN_POINT('Ctrl Pts',(-0.710942044109715,0.675391276285392,
-7.65517867510834));
#34946=CARTESIAN_POINT('Ctrl Pts',(-0.49820857711537,0.841279740454847,
-7.67511813742176));
#34947=CARTESIAN_POINT('Ctrl Pts',(-0.381893017926294,0.899770411614538,
-7.68453883645515));
#34948=CARTESIAN_POINT('Ctrl Pts',(-0.135782197717578,0.968838493154299,
-7.70341336104795));
#34949=CARTESIAN_POINT('Ctrl Pts',(-0.00885791301167451,0.978380920800163,
-7.71264786533363));
#34950=CARTESIAN_POINT('Ctrl Pts',(0.243086422407635,0.946582318646724,
-7.73140195555427));
#34951=CARTESIAN_POINT('Ctrl Pts',(0.364893764354408,0.906795910405157,
-7.74067940423168));
#34952=CARTESIAN_POINT('Ctrl Pts',(0.602552308657543,0.774392065697426,
-7.76078092887998));
#34953=CARTESIAN_POINT('Ctrl Pts',(0.694580298594965,0.685114787931247,
-7.77006362922804));
#34954=CARTESIAN_POINT('Ctrl Pts',(0.837537470686194,0.502943306898377,
-7.78715621316132));
#34955=CARTESIAN_POINT('Ctrl Pts',(0.895666672303433,0.39143709728767,-7.79626984527518));
#34956=CARTESIAN_POINT('Ctrl Pts',(0.973351297906596,0.128895529785619,
-7.81651098819627));
#34957=CARTESIAN_POINT('Ctrl Pts',(0.974893322586702,-0.0019847928045931,
-7.82597019693368));
#34958=CARTESIAN_POINT('Ctrl Pts',(0.950357105839006,-0.225512712002595,
-7.84256438020254));
#34959=CARTESIAN_POINT('Ctrl Pts',(0.915137957151007,-0.343555912182618,
-7.85150366301155));
#34960=CARTESIAN_POINT('Ctrl Pts',(0.79895709032177,-0.565039921665155,
-7.86999754200814));
#34961=CARTESIAN_POINT('Ctrl Pts',(0.715226511460408,-0.666609469197207,
-7.87952665675726));
#34962=CARTESIAN_POINT('Ctrl Pts',(0.536741391990988,-0.813719169033563,
-7.89659574416654));
#34963=CARTESIAN_POINT('Ctrl Pts',(0.430157431758474,-0.881619871693293,
-7.90574434095616));
#34964=CARTESIAN_POINT('Ctrl Pts',(0.169879893219252,-0.963177221783432,
-7.92590779534851));
#34965=CARTESIAN_POINT('Ctrl Pts',(0.0397241532021394,-0.976746905277044,
-7.93537724319687));
#34966=CARTESIAN_POINT('Ctrl Pts',(-0.215567824952798,-0.954110740313475,
-7.95429743954781));
#34967=CARTESIAN_POINT('Ctrl Pts',(-0.335772498328983,-0.919014836607859,
-7.96338078352852));
#34968=CARTESIAN_POINT('Ctrl Pts',(-0.560640566968571,-0.800756976907155,
-7.98215056834433));
#34969=CARTESIAN_POINT('Ctrl Pts',(-0.661335943120196,-0.719769058763693,
-7.99150330602323));
#34970=CARTESIAN_POINT('Ctrl Pts',(-0.844482510173841,-0.502763426800802,
-8.01247835748223));
#34971=CARTESIAN_POINT('Ctrl Pts',(-0.895835357602949,-0.383242232620365,
-8.02187999800142));
#34972=CARTESIAN_POINT('Ctrl Pts',(-0.961546949955464,-0.173650789240346,
-8.03809694137713));
#34973=CARTESIAN_POINT('Ctrl Pts',(-0.976299127968145,-0.0474944798539713,
-8.04729710662085));
#34974=CARTESIAN_POINT('Ctrl Pts',(-0.955530645539919,0.224147261598761,
-8.06743276001601));
#34975=CARTESIAN_POINT('Ctrl Pts',(-0.911883259972712,0.345947006970901,
-8.07679308703859));
#34976=CARTESIAN_POINT('Ctrl Pts',(-0.80759222572764,0.549546991928824,
-8.09367559884552));
#34977=CARTESIAN_POINT('Ctrl Pts',(-0.731634438299219,0.648219317689523,
-8.10270570758665));
#34978=CARTESIAN_POINT('Ctrl Pts',(-0.519253362836709,0.835147785103093,
-8.12362513174581));
#34979=CARTESIAN_POINT('Ctrl Pts',(-0.394382545000837,0.890311605080876,
-8.13346376213966));
#34980=CARTESIAN_POINT('Ctrl Pts',(-0.22948769620124,0.945169712744923,
-8.14628763376929));
#34981=CARTESIAN_POINT('Ctrl Pts',(-0.10344025351597,0.977763677308026,
-8.15567354070393));
#34982=CARTESIAN_POINT('Ctrl Pts',(0.184189748428152,0.960792073154366,
-8.1769774940639));
#34983=CARTESIAN_POINT('Ctrl Pts',(0.311040850131799,0.926823882769418,
-8.18648132694537));
#34984=CARTESIAN_POINT('Ctrl Pts',(0.522317084702463,0.82373430143044,-8.20383254532107));
#34985=CARTESIAN_POINT('Ctrl Pts',(0.627925007800294,0.753621699865986,
-8.21301334868246));
#34986=CARTESIAN_POINT('Ctrl Pts',(0.808291869592365,0.550140906266646,
-8.23310786347754));
#34987=CARTESIAN_POINT('Ctrl Pts',(0.87394342749214,0.437853235013805,-8.2425203987734));
#34988=CARTESIAN_POINT('Ctrl Pts',(0.958431878966911,0.196473510716754,
-8.26140532400548));
#34989=CARTESIAN_POINT('Ctrl Pts',(0.975880231838361,0.0702848706249534,
-8.27064732836836));
#34990=CARTESIAN_POINT('Ctrl Pts',(0.959947904054335,-0.183126801657153,
-8.28939844178708));
#34991=CARTESIAN_POINT('Ctrl Pts',(0.9279613149587,-0.307075814244947,-8.29866694348103));
#34992=CARTESIAN_POINT('Ctrl Pts',(0.810836783038452,-0.552574182082263,
-8.31876610146149));
#34993=CARTESIAN_POINT('Ctrl Pts',(0.727428616466514,-0.650090720524161,
-8.32805586355408));
#34994=CARTESIAN_POINT('Ctrl Pts',(0.554830637668132,-0.804089741468125,
-8.34512936045986));
#34995=CARTESIAN_POINT('Ctrl Pts',(0.447347381110083,-0.869095961842081,
-8.35423363278207));
#34996=CARTESIAN_POINT('Ctrl Pts',(0.190085901191506,-0.963314868905316,
-8.37448821792598));
#34997=CARTESIAN_POINT('Ctrl Pts',(0.0593773685688153,-0.973041258364987,
-8.38395933661561));
#34998=CARTESIAN_POINT('Ctrl Pts',(-0.164812872673331,-0.962733764741733,
-8.40052072541264));
#34999=CARTESIAN_POINT('Ctrl Pts',(-0.284713736492386,-0.935119778603541,
-8.40945016383226));
#35000=CARTESIAN_POINT('Ctrl Pts',(-0.505500848301031,-0.836647957297407,
-8.42732628037607));
#35001=CARTESIAN_POINT('Ctrl Pts',(-0.606159982100895,-0.765891415849571,
-8.43625571879569));
#35002=CARTESIAN_POINT('Ctrl Pts',(-0.763625880418339,-0.605978941163821,
-8.45281710759272));
#35003=CARTESIAN_POINT('Ctrl Pts',(-0.843724779454851,-0.502231702523653,
-8.46228822628236));
#35004=CARTESIAN_POINT('Ctrl Pts',(-0.945519248298759,-0.247872591008094,
-8.48254281142633));
#35005=CARTESIAN_POINT('Ctrl Pts',(-0.968971023406308,-0.124468890204753,
-8.49164708374858));
#35006=CARTESIAN_POINT('Ctrl Pts',(-0.969718982672264,0.106843023223741,
-8.50872058065439));
#35007=CARTESIAN_POINT('Ctrl Pts',(-0.952896543688451,0.23405702822005,
-8.51801034274699));
#35008=CARTESIAN_POINT('Ctrl Pts',(-0.848502485829636,0.485233231854171,
-8.53810950072742));
#35009=CARTESIAN_POINT('Ctrl Pts',(-0.777655722913491,0.591850471490924,
-8.54737800242134));
#35010=CARTESIAN_POINT('Ctrl Pts',(-0.599760572964984,0.773026160649792,
-8.56612911584002));
#35011=CARTESIAN_POINT('Ctrl Pts',(-0.494216597850723,0.844359793833638,
-8.57537112020285));
#35012=CARTESIAN_POINT('Ctrl Pts',(-0.258175251552619,0.94278211128278,
-8.59425604543487));
#35013=CARTESIAN_POINT('Ctrl Pts',(-0.130765826826689,0.968963911470145,
-8.6036685807307));
#35014=CARTESIAN_POINT('Ctrl Pts',(0.141141368764911,0.970728899308695,
-8.62376309552574));
#35015=CARTESIAN_POINT('Ctrl Pts',(0.263869764194383,0.939002707061656,
-8.63294389888712));
#35016=CARTESIAN_POINT('Ctrl Pts',(0.48173765663666,0.850692512192601,-8.6502951172628));
#35017=CARTESIAN_POINT('Ctrl Pts',(0.59176831279852,0.779010613040475,-8.65979895014427));
#35018=CARTESIAN_POINT('Ctrl Pts',(0.796580869189747,0.576351120022339,
-8.68110290350424));
#35019=CARTESIAN_POINT('Ctrl Pts',(0.85655168261402,0.460792364963848,-8.69048881043887));
#35020=CARTESIAN_POINT('Ctrl Pts',(0.925914408979296,0.301454562392536,
-8.7033126820685));
#35021=CARTESIAN_POINT('Ctrl Pts',(0.96830685546231,0.171690743618838,-8.71315131246233));
#35022=CARTESIAN_POINT('Ctrl Pts',(0.97113684240774,-0.111222607635871,
-8.73407073662165));
#35023=CARTESIAN_POINT('Ctrl Pts',(0.948476372601596,-0.233665722796318,
-8.74310084536292));
#35024=CARTESIAN_POINT('Ctrl Pts',(0.866680152751085,-0.447298473368202,
-8.75998335717));
#35025=CARTESIAN_POINT('Ctrl Pts',(0.805223850365118,-0.561155379775387,
-8.76934368419274));
#35026=CARTESIAN_POINT('Ctrl Pts',(0.616996729226077,-0.758109984772489,
-8.78947933758782));
#35027=CARTESIAN_POINT('Ctrl Pts',(0.513278309612569,-0.831427994749491,
-8.79867950283134));
#35028=CARTESIAN_POINT('Ctrl Pts',(0.31343386006222,-0.922580517982861,
-8.81489644620692));
#35029=CARTESIAN_POINT('Ctrl Pts',(0.190196585754656,-0.964233909424807,
-8.82429808672594));
#35030=CARTESIAN_POINT('Ctrl Pts',(-0.0936305289987633,-0.972967651905942,
-8.84527313818489));
#35031=CARTESIAN_POINT('Ctrl Pts',(-0.221167848283893,-0.952162992497406,
-8.8546258758639));
#35032=CARTESIAN_POINT('Ctrl Pts',(-0.459402726619715,-0.863875323940818,
-8.87339566067979));
#35033=CARTESIAN_POINT('Ctrl Pts',(-0.565831472897797,-0.797891932666687,
-8.88247900466054));
#35034=CARTESIAN_POINT('Ctrl Pts',(-0.753251241861668,-0.623077115572175,
-8.90139920101144));
#35035=CARTESIAN_POINT('Ctrl Pts',(-0.830121335358713,-0.517173188849596,
-8.91086864885978));
#35036=CARTESIAN_POINT('Ctrl Pts',(-0.943351358027897,-0.269030164792746,
-8.93103210325212));
#35037=CARTESIAN_POINT('Ctrl Pts',(-0.964048729229666,-0.144361544739941,
-8.94018070004174));
#35038=CARTESIAN_POINT('Ctrl Pts',(-0.973856013903567,0.0867272235402916,
-8.95724978745104));
#35039=CARTESIAN_POINT('Ctrl Pts',(-0.954233524433084,0.216889202356323,
-8.96677890220017));
#35040=CARTESIAN_POINT('Ctrl Pts',(-0.867075844584165,0.451317654377401,
-8.98527278119678));
#35041=CARTESIAN_POINT('Ctrl Pts',(-0.802782957983991,0.556393866127067,
-8.9942120640058));
#35042=CARTESIAN_POINT('Ctrl Pts',(-0.652870452434927,0.724003523585268,
-9.01080624727465));
#35043=CARTESIAN_POINT('Ctrl Pts',(-0.554463941404066,0.81030645092931,
-9.02026545601205));
#35044=CARTESIAN_POINT('Ctrl Pts',(-0.307224094184924,0.927930571195957,
-9.0405065989331));
#35045=CARTESIAN_POINT('Ctrl Pts',(-0.18542229140729,0.959186925789853,
-9.04962023104691));
#35046=CARTESIAN_POINT('Ctrl Pts',(0.0456345727863304,0.974546843206883,
-9.06671281498016));
#35047=CARTESIAN_POINT('Ctrl Pts',(0.173547971727258,0.965729495041201,
-9.07599551532821));
#35048=CARTESIAN_POINT('Ctrl Pts',(0.430853797139275,0.877377505913246,
-9.09609703997657));
#35049=CARTESIAN_POINT('Ctrl Pts',(0.541843176296526,0.813335765249628,
-9.10537448865406));
#35050=CARTESIAN_POINT('Ctrl Pts',(0.733843091802084,0.647133684351997,
-9.12412857887477));
#35051=CARTESIAN_POINT('Ctrl Pts',(0.811550342016078,0.546324878994267,
-9.13336308316049));
#35052=CARTESIAN_POINT('Ctrl Pts',(0.924606730993034,0.317066970465827,
-9.1522376077533));
#35053=CARTESIAN_POINT('Ctrl Pts',(0.958807608424655,0.191445444025974,
-9.16165830678668));
#35054=CARTESIAN_POINT('Ctrl Pts',(0.97752676026398,-0.0776682060790321,
-9.18159750234122));
#35055=CARTESIAN_POINT('Ctrl Pts',(0.954466464728092,-0.200390318016599,
-9.19065177707848));
#35056=CARTESIAN_POINT('Ctrl Pts',(0.921755948798206,-0.300215476427702,
-9.19840833793598));
#35057=CARTESIAN_POINT('Ctrl Pts',(0.921755949557376,-0.300215476483715,
-9.1984083383494));
#35058=CARTESIAN_POINT('Ctrl Pts',(0.966258812022516,-0.314710037724431,
-9.22544687004147));
#35059=CARTESIAN_POINT('Ctrl Pts',(1.01076167448854,-0.329204598962977,
-9.25248540173324));
#35060=CARTESIAN_POINT('Ctrl Pts',(1.09965630787658,-0.358157538981693,
-9.30649496940931));
#35061=CARTESIAN_POINT('Ctrl Pts',(1.14404807879862,-0.372615917761862,
-9.33346600539358));
#35062=CARTESIAN_POINT('Ctrl Pts',(1.18843984972142,-0.387074296539831,
-9.36043704137777));
#35063=CARTESIAN_POINT('Ctrl Pts',(-1.259505999833,0.1118215653306,-7.310493359005));
#35064=CARTESIAN_POINT('Ctrl Pts',(-1.233119488752,0.4090269292851,-7.327393450197));
#35065=CARTESIAN_POINT('Ctrl Pts',(-0.9611624434191,0.9824414050051,-7.361193632581));
#35066=CARTESIAN_POINT('Ctrl Pts',(-0.09123625710912,1.371574306486,-7.411893906157));
#35067=CARTESIAN_POINT('Ctrl Pts',(0.8225070640451,1.101289504301,-7.462594179733));
#35068=CARTESIAN_POINT('Ctrl Pts',(1.340998453597,0.3018564915754,-7.513294453309));
#35069=CARTESIAN_POINT('Ctrl Pts',(1.215065651604,-0.6426565758875,-7.563994726885));
#35070=CARTESIAN_POINT('Ctrl Pts',(0.5052286202678,-1.278332598092,-7.614695000461));
#35071=CARTESIAN_POINT('Ctrl Pts',(-0.4473982195291,-1.299702243498,-7.665395274037));
#35072=CARTESIAN_POINT('Ctrl Pts',(-1.185025986569,-0.6964942675707,-7.716095547613));
#35073=CARTESIAN_POINT('Ctrl Pts',(-1.353184701554,0.2414167522021,-7.766795821189));
#35074=CARTESIAN_POINT('Ctrl Pts',(-0.8710649968543,1.063313998875,-7.817496094765));
#35075=CARTESIAN_POINT('Ctrl Pts',(0.02964853739914,1.374231366706,-7.868196368341));
#35076=CARTESIAN_POINT('Ctrl Pts',(0.9161143464999,1.024756259044,-7.918896641917));
#35077=CARTESIAN_POINT('Ctrl Pts',(1.362337676919,0.1828303588308,-7.969596915493));
#35078=CARTESIAN_POINT('Ctrl Pts',(1.153884090754,-0.7469554144499,-8.020297189069));
#35079=CARTESIAN_POINT('Ctrl Pts',(0.3909268074144,-1.31778872257,-8.070997462645));
#35080=CARTESIAN_POINT('Ctrl Pts',(-0.5598919446549,-1.255353295447,-8.121697736221));
#35081=CARTESIAN_POINT('Ctrl Pts',(-1.241652343453,-0.5896527317712,-8.172398009797));
#35082=CARTESIAN_POINT('Ctrl Pts',(-1.326731653941,0.3594078525894,-8.223098283373));
#35083=CARTESIAN_POINT('Ctrl Pts',(-0.7742446671504,1.13575353024,-8.273798556949));
#35084=CARTESIAN_POINT('Ctrl Pts',(0.1503087464258,1.366308225497,-8.324498830525));
#35085=CARTESIAN_POINT('Ctrl Pts',(1.002630679619,0.940277940449,-8.375199104101));
#35086=CARTESIAN_POINT('Ctrl Pts',(1.373134359574,0.0623932649103,-8.425899377677));
#35087=CARTESIAN_POINT('Ctrl Pts',(1.083772727633,-0.8454747539721,-8.476599651253));
#35088=CARTESIAN_POINT('Ctrl Pts',(0.273599719997,-1.347046415986,-8.527299924829));
#35089=CARTESIAN_POINT('Ctrl Pts',(-0.6680528234323,-1.201289521179,-8.578000198405));
#35090=CARTESIAN_POINT('Ctrl Pts',(-1.288669577293,-0.4782477502744,-8.628700471981));
#35091=CARTESIAN_POINT('Ctrl Pts',(-1.290011985917,0.4746167806014,-8.679400745557));
#35092=CARTESIAN_POINT('Ctrl Pts',(-0.67142990411,1.199406552392,-8.730101019133));
#35093=CARTESIAN_POINT('Ctrl Pts',(0.2697957013361,1.347800698259,-8.780801292709));
#35094=CARTESIAN_POINT('Ctrl Pts',(1.081425305565,0.8485631628267,-8.831501566285));
#35095=CARTESIAN_POINT('Ctrl Pts',(1.373164741435,-0.05867665453186,-8.882201839861));
#35096=CARTESIAN_POINT('Ctrl Pts',(1.128252374438,-0.6441531510397,-8.916002022245));
#35097=CARTESIAN_POINT('Ctrl Pts',(0.9247594743852,-0.8623684483003,-8.932902113437));
#35098=CARTESIAN_POINT('Ctrl Pts',(-1.156936026367,0.1027151895051,-7.369945091634));
#35099=CARTESIAN_POINT('Ctrl Pts',(-1.13269834486,0.3757171385502,-7.386845182826));
#35100=CARTESIAN_POINT('Ctrl Pts',(-0.882888575465,0.9024346492954,-7.42064536521));
#35101=CARTESIAN_POINT('Ctrl Pts',(-0.0838062802197,1.259877863402,-7.471345638786));
#35102=CARTESIAN_POINT('Ctrl Pts',(0.7555248283541,1.011604155244,-7.522045912362));
#35103=CARTESIAN_POINT('Ctrl Pts',(1.231792006131,0.2772743043245,-7.572746185938));
#35104=CARTESIAN_POINT('Ctrl Pts',(1.116114752076,-0.5903207649065,-7.623446459514));
#35105=CARTESIAN_POINT('Ctrl Pts',(0.4640844842477,-1.174229449172,-7.67414673309));
#35106=CARTESIAN_POINT('Ctrl Pts',(-0.4109635987238,-1.193858821833,-7.724847006666));
#35107=CARTESIAN_POINT('Ctrl Pts',(-1.088521417305,-0.6397740943015,-7.775547280242));
#35108=CARTESIAN_POINT('Ctrl Pts',(-1.242985846645,0.2217565760132,-7.826247553818));
#35109=CARTESIAN_POINT('Ctrl Pts',(-0.8001283648521,0.9767212484911,-7.876947827394));
#35110=CARTESIAN_POINT('Ctrl Pts',(0.02723405926664,1.262318541488,-7.92764810097));
#35111=CARTESIAN_POINT('Ctrl Pts',(0.8415090455128,0.9413035225634,-7.978348374546));
#35112=CARTESIAN_POINT('Ctrl Pts',(1.251393434183,0.1679412633786,-8.029048648122));
#35113=CARTESIAN_POINT('Ctrl Pts',(1.059915613758,-0.6861258534547,-8.079748921698));
#35114=CARTESIAN_POINT('Ctrl Pts',(0.3590910303168,-1.210472398292,-8.130449195274));
#35115=CARTESIAN_POINT('Ctrl Pts',(-0.5142962095692,-1.153121504394,-8.18114946885));
#35116=CARTESIAN_POINT('Ctrl Pts',(-1.140536312295,-0.54163337731,-8.231849742426));
#35117=CARTESIAN_POINT('Ctrl Pts',(-1.218687047119,0.3301388741895,-8.282550016002));
#35118=CARTESIAN_POINT('Ctrl Pts',(-0.7111927603103,1.043261545703,-8.333250289578));
#35119=CARTESIAN_POINT('Ctrl Pts',(0.1380681027649,1.255040634509,-8.383950563154));
#35120=CARTESIAN_POINT('Ctrl Pts',(0.9209797766311,0.8637048368548,-8.43465083673));
#35121=CARTESIAN_POINT('Ctrl Pts',(1.261310870964,0.05731216523537,-8.485351110306));
#35122=CARTESIAN_POINT('Ctrl Pts',(0.9955138865225,-0.7766221061142,-8.536051383882));
#35123=CARTESIAN_POINT('Ctrl Pts',(0.2513186701059,-1.237347442608,-8.586751657458));
#35124=CARTESIAN_POINT('Ctrl Pts',(-0.613648826641,-1.103460503827,-8.637451931034));
#35125=CARTESIAN_POINT('Ctrl Pts',(-1.183724619217,-0.4393008464388,-8.68815220461));
#35126=CARTESIAN_POINT('Ctrl Pts',(-1.184957706554,0.4359655708419,-8.738852478186));
#35127=CARTESIAN_POINT('Ctrl Pts',(-0.6167508891167,1.101730877747,-8.789552751762));
#35128=CARTESIAN_POINT('Ctrl Pts',(0.2478244380543,1.238040298645,-8.840253025338));
#35129=CARTESIAN_POINT('Ctrl Pts',(0.9933576306892,0.7794590052386,-8.890953298914));
#35130=CARTESIAN_POINT('Ctrl Pts',(1.261338778627,-0.05389822322687,-8.94165357249));
#35131=CARTESIAN_POINT('Ctrl Pts',(1.036371259045,-0.5916954639631,-8.975453754874));
#35132=CARTESIAN_POINT('Ctrl Pts',(0.8494501429783,-0.7921400342458,-8.992353846066));
#35133=CARTESIAN_POINT('Ctrl Pts',(-1.054366052901,0.09360881367962,-7.429396824262));
#35134=CARTESIAN_POINT('Ctrl Pts',(-1.032277200968,0.3424073478153,-7.446296915454));
#35135=CARTESIAN_POINT('Ctrl Pts',(-0.8046147075109,0.8224278935856,-7.480097097838));
#35136=CARTESIAN_POINT('Ctrl Pts',(-0.07637630333028,1.148181420319,-7.530797371414));
#35137=CARTESIAN_POINT('Ctrl Pts',(0.6885425926632,0.9219188061864,-7.58149764499));
#35138=CARTESIAN_POINT('Ctrl Pts',(1.122585558665,0.2526921170736,-7.632197918566));
#35139=CARTESIAN_POINT('Ctrl Pts',(1.017163852547,-0.5379849539255,-7.682898192142));
#35140=CARTESIAN_POINT('Ctrl Pts',(0.4229403482276,-1.070126300251,-7.733598465718));
#35141=CARTESIAN_POINT('Ctrl Pts',(-0.3745289779184,-1.088015400168,-7.784298739294));
#35142=CARTESIAN_POINT('Ctrl Pts',(-0.9920168480411,-0.5830539210323,-7.83499901287));
#35143=CARTESIAN_POINT('Ctrl Pts',(-1.132786991735,0.2020963998243,-7.885699286446));
#35144=CARTESIAN_POINT('Ctrl Pts',(-0.7291917328499,0.8901284981069,-7.936399560022));
#35145=CARTESIAN_POINT('Ctrl Pts',(0.02481958113415,1.150405716271,-7.987099833598));
#35146=CARTESIAN_POINT('Ctrl Pts',(0.7669037445257,0.857850786083,-8.037800107174));
#35147=CARTESIAN_POINT('Ctrl Pts',(1.140449191446,0.1530521679265,-8.08850038075));
#35148=CARTESIAN_POINT('Ctrl Pts',(0.9659471367619,-0.6252962924595,-8.139200654326));
#35149=CARTESIAN_POINT('Ctrl Pts',(0.3272552532192,-1.103156074014,-8.189900927902));
#35150=CARTESIAN_POINT('Ctrl Pts',(-0.4687004744835,-1.050889713341,-8.240601201478));
#35151=CARTESIAN_POINT('Ctrl Pts',(-1.039420281137,-0.4936140228487,-8.291301475054));
#35152=CARTESIAN_POINT('Ctrl Pts',(-1.110642440297,0.3008698957896,-8.34200174863));
#35153=CARTESIAN_POINT('Ctrl Pts',(-0.6481408534701,0.9507695611661,-8.392702022206));
#35154=CARTESIAN_POINT('Ctrl Pts',(0.1258274591041,1.143773043521,-8.443402295782));
#35155=CARTESIAN_POINT('Ctrl Pts',(0.8393288736432,0.7871317332605,-8.494102569358));
#35156=CARTESIAN_POINT('Ctrl Pts',(1.149487382353,0.05223106556044,-8.544802842934));
#35157=CARTESIAN_POINT('Ctrl Pts',(0.9072550454121,-0.7077694582564,-8.59550311651));
#35158=CARTESIAN_POINT('Ctrl Pts',(0.2290376202147,-1.127648469229,-8.646203390086));
#35159=CARTESIAN_POINT('Ctrl Pts',(-0.5592448298497,-1.005631486475,-8.696903663662));
#35160=CARTESIAN_POINT('Ctrl Pts',(-1.07877966114,-0.4003539426031,-8.747603937238));
#35161=CARTESIAN_POINT('Ctrl Pts',(-1.07990342719,0.3973143610824,-8.798304210814));
#35162=CARTESIAN_POINT('Ctrl Pts',(-0.5620718741233,1.004055203101,-8.84900448439));
#35163=CARTESIAN_POINT('Ctrl Pts',(0.2258531747725,1.128279899031,-8.899704757966));
#35164=CARTESIAN_POINT('Ctrl Pts',(0.9052899558132,0.7103548476505,-8.950405031542));
#35165=CARTESIAN_POINT('Ctrl Pts',(1.149512815819,-0.04911979192188,-9.001105305118));
#35166=CARTESIAN_POINT('Ctrl Pts',(0.9444901436511,-0.5392377768865,-9.034905487502));
#35167=CARTESIAN_POINT('Ctrl Pts',(0.7741408115714,-0.7219116201914,-9.051805578694));
#35168=CARTESIAN_POINT('Ctrl Pts',(-0.9517960794344,0.08450243785415,-7.48884855689));
#35169=CARTESIAN_POINT('Ctrl Pts',(-0.9318560570757,0.3090975570804,-7.505748648082));
#35170=CARTESIAN_POINT('Ctrl Pts',(-0.7263408395568,0.7424211378759,-7.539548830466));
#35171=CARTESIAN_POINT('Ctrl Pts',(-0.06894632644086,1.036484977236,-7.590249104042));
#35172=CARTESIAN_POINT('Ctrl Pts',(0.6215603569723,0.832233457129,-7.640949377618));
#35173=CARTESIAN_POINT('Ctrl Pts',(1.013379111199,0.2281099298227,-7.691649651194));
#35174=CARTESIAN_POINT('Ctrl Pts',(0.9182129530188,-0.4856491429445,-7.74234992477));
#35175=CARTESIAN_POINT('Ctrl Pts',(0.3817962122075,-0.9660231513296,-7.793050198346));
#35176=CARTESIAN_POINT('Ctrl Pts',(-0.3380943571131,-0.9821719785035,-7.843750471922));
#35177=CARTESIAN_POINT('Ctrl Pts',(-0.8955122787772,-0.5263337477631,-7.894450745498));
#35178=CARTESIAN_POINT('Ctrl Pts',(-1.022588136825,0.1824362236354,-7.945151019074));
#35179=CARTESIAN_POINT('Ctrl Pts',(-0.6582551008476,0.8035357477226,-7.99585129265));
#35180=CARTESIAN_POINT('Ctrl Pts',(0.02240510300165,1.038492891054,-8.046551566226));
#35181=CARTESIAN_POINT('Ctrl Pts',(0.6922984435386,0.7743980496026,-8.097251839802));
#35182=CARTESIAN_POINT('Ctrl Pts',(1.029504948709,0.1381630724743,-8.147952113378));
#35183=CARTESIAN_POINT('Ctrl Pts',(0.8719786597657,-0.5644667314643,-8.198652386954));
#35184=CARTESIAN_POINT('Ctrl Pts',(0.2954194761216,-0.9958397497356,-8.24935266053));
#35185=CARTESIAN_POINT('Ctrl Pts',(-0.4231047393978,-0.948657922288,-8.300052934106));
#35186=CARTESIAN_POINT('Ctrl Pts',(-0.9383042499798,-0.4455946683874,-8.350753207682));
#35187=CARTESIAN_POINT('Ctrl Pts',(-1.002597833476,0.2716009173896,-8.401453481258));
#35188=CARTESIAN_POINT('Ctrl Pts',(-0.58508894663,0.8582775766289,-8.452153754834));
#35189=CARTESIAN_POINT('Ctrl Pts',(0.1135868154433,1.032505452534,-8.50285402841));
#35190=CARTESIAN_POINT('Ctrl Pts',(0.7576779706553,0.7105586296663,-8.553554301986));
#35191=CARTESIAN_POINT('Ctrl Pts',(1.037663893743,0.04714996588551,-8.604254575562));
#35192=CARTESIAN_POINT('Ctrl Pts',(0.8189962043018,-0.6389168103985,-8.654954849138));
#35193=CARTESIAN_POINT('Ctrl Pts',(0.2067565703236,-1.017949495851,-8.705655122714));
#35194=CARTESIAN_POINT('Ctrl Pts',(-0.5048408330584,-0.9078024691232,-8.75635539629));
#35195=CARTESIAN_POINT('Ctrl Pts',(-0.9738347030632,-0.3614070387674,-8.807055669866));
#35196=CARTESIAN_POINT('Ctrl Pts',(-0.9748491478262,0.3586631513228,-8.857755943442));
#35197=CARTESIAN_POINT('Ctrl Pts',(-0.50739285913,0.9063795284549,-8.908456217018));
#35198=CARTESIAN_POINT('Ctrl Pts',(0.2038819114907,1.018519499416,-8.959156490594));
#35199=CARTESIAN_POINT('Ctrl Pts',(0.8172222809373,0.6412506900624,-9.00985676417));
#35200=CARTESIAN_POINT('Ctrl Pts',(1.037686853011,-0.04434136061689,-9.060557037746));
#35201=CARTESIAN_POINT('Ctrl Pts',(0.8526090282577,-0.4867800898099,-9.09435722013));
#35202=CARTESIAN_POINT('Ctrl Pts',(0.6988314801645,-0.6516832061369,-9.111257311322));
#35203=CARTESIAN_POINT('',(-1.08160102925865,0.625310431755989,-7.35041766696342));
#35204=CARTESIAN_POINT('Ctrl Pts',(-1.08141633891441,0.625226119210898,
-7.35008360873745));
#35205=CARTESIAN_POINT('Ctrl Pts',(-1.03390357444464,0.707597454903937,
-7.35557558080133));
#35206=CARTESIAN_POINT('Ctrl Pts',(-0.977165735444024,0.784700022705665,
-7.36105287658457));
#35207=CARTESIAN_POINT('Ctrl Pts',(-0.847428073212402,0.923895031085402,
-7.37187595599759));
#35208=CARTESIAN_POINT('Ctrl Pts',(-0.775218330200545,0.985002391821968,
-7.37715175724076));
#35209=CARTESIAN_POINT('Ctrl Pts',(-0.562372240877458,1.12689746391015,
-7.39180025301249));
#35210=CARTESIAN_POINT('Ctrl Pts',(-0.41080462578532,1.19043897709064,-7.40119985709024));
#35211=CARTESIAN_POINT('Ctrl Pts',(-0.0629664710684568,1.26354084983809,
-7.42162303400616));
#35212=CARTESIAN_POINT('Ctrl Pts',(0.103488374627705,1.25272346457742,-7.43077732184325));
#35213=CARTESIAN_POINT('Ctrl Pts',(0.393137413675227,1.19617600750093,-7.44776934087969));
#35214=CARTESIAN_POINT('Ctrl Pts',(0.544669237975361,1.13566521348015,-7.45708958155269));
#35215=CARTESIAN_POINT('Ctrl Pts',(0.74071771238418,1.00950579684395,-7.47039494437775));
#35216=CARTESIAN_POINT('Ctrl Pts',(0.798229981102956,0.964762914809237,
-7.4744740161231));
#35217=CARTESIAN_POINT('Ctrl Pts',(0.91161970049166,0.858715269389297,-7.48330419809846));
#35218=CARTESIAN_POINT('Ctrl Pts',(0.96585170887338,0.796699343698819,-7.48801878934439));
#35219=CARTESIAN_POINT('Ctrl Pts',(1.1051564507755,0.602515358859405,-7.50180807576398));
#35220=CARTESIAN_POINT('Ctrl Pts',(1.17325445808129,0.457773604427091,-7.51093744662193));
#35221=CARTESIAN_POINT('Ctrl Pts',(1.23173628114455,0.227803586493787,-7.52442350173589));
#35222=CARTESIAN_POINT('Ctrl Pts',(1.24360254337297,0.148809050123005,-7.52889719445281));
#35223=CARTESIAN_POINT('Ctrl Pts',(1.25210926732186,-0.0141296717769907,
-7.53823147511025));
#35224=CARTESIAN_POINT('Ctrl Pts',(1.24810293985508,-0.0976312140262272,
-7.54303303614898));
#35225=CARTESIAN_POINT('Ctrl Pts',(1.21512425843464,-0.32325358963531,-7.55620697967317));
#35226=CARTESIAN_POINT('Ctrl Pts',(1.16817801989322,-0.475178802142458,
-7.56524490596786));
#35227=CARTESIAN_POINT('Ctrl Pts',(1.0010569163738,-0.767448246501332,-7.5842773720152));
#35228=CARTESIAN_POINT('Ctrl Pts',(0.893699212068381,-0.883883124181553,
-7.59326625011072));
#35229=CARTESIAN_POINT('Ctrl Pts',(0.719401219493123,-1.02453980494428,
-7.60620759270894));
#35230=CARTESIAN_POINT('Ctrl Pts',(0.649553479442821,-1.07048344305116,
-7.6110122144122));
#35231=CARTESIAN_POINT('Ctrl Pts',(0.43533477113506,-1.18255361353768,-7.62485720834406));
#35232=CARTESIAN_POINT('Ctrl Pts',(0.284651569813539,-1.22753999642643,
-7.63351977150539));
#35233=CARTESIAN_POINT('Ctrl Pts',(-0.0378877950936454,-1.25878616455311,
-7.65219720012196));
#35234=CARTESIAN_POINT('Ctrl Pts',(-0.202527294014996,-1.24354442983782,
-7.66163547117351));
#35235=CARTESIAN_POINT('Ctrl Pts',(-0.432645253811083,-1.17535719485944,
-7.67529850407763));
#35236=CARTESIAN_POINT('Ctrl Pts',(-0.5044565720885,-1.14630075345231,-7.67963067502684));
#35237=CARTESIAN_POINT('Ctrl Pts',(-0.715088231070164,-1.03676845987327,
-7.69318388762178));
#35238=CARTESIAN_POINT('Ctrl Pts',(-0.842583200977805,-0.935593103413969,
-7.7024820512621));
#35239=CARTESIAN_POINT('Ctrl Pts',(-1.05492365451986,-0.690166554091875,
-7.72116588890207));
#35240=CARTESIAN_POINT('Ctrl Pts',(-1.13607731155066,-0.547058816969546,
-7.73020867810678));
#35241=CARTESIAN_POINT('Ctrl Pts',(-1.23686100235198,-0.236561521351647,
-7.74896782912686));
#35242=CARTESIAN_POINT('Ctrl Pts',(-1.25722144982577,-0.0738463772980785,
-7.75834693922323));
#35243=CARTESIAN_POINT('Ctrl Pts',(-1.24034494211375,0.18082038036121,-7.77296132059527));
#35244=CARTESIAN_POINT('Ctrl Pts',(-1.22343274900602,0.273643041743944,
-7.77822353566137));
#35245=CARTESIAN_POINT('Ctrl Pts',(-1.16761229453482,0.455287656065107,
-7.789032216188));
#35246=CARTESIAN_POINT('Ctrl Pts',(-1.12910782046682,0.542922433132975,
-7.79450905932452));
#35247=CARTESIAN_POINT('Ctrl Pts',(-1.08143574407104,0.625192553810161,
-7.80000057583712));
#35248=CARTESIAN_POINT('',(0.921755949135472,-0.300215476273863,-9.07172448818857));
#35249=CARTESIAN_POINT('Ctrl Pts',(1.18807733836104,-0.386956226761339,
-8.90991603565015));
#35250=CARTESIAN_POINT('Ctrl Pts',(1.14381077010285,-0.372538626432016,
-8.93681100245566));
#35251=CARTESIAN_POINT('Ctrl Pts',(1.09954420184343,-0.358121026106439,
-8.96370596926116));
#35252=CARTESIAN_POINT('Ctrl Pts',(1.01077040547201,-0.329207442646842,
-9.01764212018779));
#35253=CARTESIAN_POINT('Ctrl Pts',(0.96626317735999,-0.314711459512787,
-9.04468330430887));
#35254=CARTESIAN_POINT('Ctrl Pts',(0.921755949246852,-0.300215476382577,
-9.07172448843017));
#35255=CARTESIAN_POINT('',(-0.83975938535873,0.485493530516545,-7.51170016756324));
#35256=CARTESIAN_POINT('Ctrl Pts',(-0.839251224062929,0.485201762564704,
-7.51168438601709));
#35257=CARTESIAN_POINT('Ctrl Pts',(-0.78683913480634,0.576233911347829,
-7.51944053895476));
#35258=CARTESIAN_POINT('Ctrl Pts',(-0.710942002712494,0.675391308566732,
-7.52849482973451));
#35259=CARTESIAN_POINT('Ctrl Pts',(-0.498208577115371,0.841279740454846,
-7.54843428816774));
#35260=CARTESIAN_POINT('Ctrl Pts',(-0.381893017926296,0.899770411614537,
-7.55785498720109));
#35261=CARTESIAN_POINT('Ctrl Pts',(-0.135782197717577,0.968838493154299,
-7.57672951179386));
#35262=CARTESIAN_POINT('Ctrl Pts',(-0.00885791301167244,0.978380920800163,
-7.58596401607956));
#35263=CARTESIAN_POINT('Ctrl Pts',(0.243086422407639,0.946582318646723,
-7.60471810630025));
#35264=CARTESIAN_POINT('Ctrl Pts',(0.364893764354414,0.906795910405155,
-7.61399555497774));
#35265=CARTESIAN_POINT('Ctrl Pts',(0.602552308657548,0.774392065697422,
-7.63409707962608));
#35266=CARTESIAN_POINT('Ctrl Pts',(0.69458029859497,0.685114787931242,-7.64337977997413));
#35267=CARTESIAN_POINT('Ctrl Pts',(0.837537470686198,0.502943306898371,
-7.66047236390738));
#35268=CARTESIAN_POINT('Ctrl Pts',(0.895666672303435,0.391437097287665,
-7.6695859960212));
#35269=CARTESIAN_POINT('Ctrl Pts',(0.973351297906597,0.128895529785616,
-7.68982713894225));
#35270=CARTESIAN_POINT('Ctrl Pts',(0.974893322586701,-0.00198479280459631,
-7.69928634767966));
#35271=CARTESIAN_POINT('Ctrl Pts',(0.950357105839005,-0.225512712002599,
-7.71588053094852));
#35272=CARTESIAN_POINT('Ctrl Pts',(0.915137957151005,-0.343555912182622,
-7.72481981375755));
#35273=CARTESIAN_POINT('Ctrl Pts',(0.798957090321767,-0.56503992166516,
-7.74331369275417));
#35274=CARTESIAN_POINT('Ctrl Pts',(0.715226511460403,-0.666609469197212,
-7.75284280750332));
#35275=CARTESIAN_POINT('Ctrl Pts',(0.536741391990981,-0.813719169033567,
-7.76991189491262));
#35276=CARTESIAN_POINT('Ctrl Pts',(0.430157431758467,-0.881619871693296,
-7.77906049170225));
#35277=CARTESIAN_POINT('Ctrl Pts',(0.169879893219243,-0.963177221783434,
-7.79922394609459));
#35278=CARTESIAN_POINT('Ctrl Pts',(0.0397241532021311,-0.976746905277045,
-7.80869339394293));
#35279=CARTESIAN_POINT('Ctrl Pts',(-0.215567824952813,-0.954110740313473,
-7.82761359029387));
#35280=CARTESIAN_POINT('Ctrl Pts',(-0.335772498328998,-0.919014836607853,
-7.83669693427461));
#35281=CARTESIAN_POINT('Ctrl Pts',(-0.560640566968575,-0.800756976907151,
-7.85546671909044));
#35282=CARTESIAN_POINT('Ctrl Pts',(-0.661335943120198,-0.719769058763691,
-7.86481945676939));
#35283=CARTESIAN_POINT('Ctrl Pts',(-0.844482510173831,-0.502763426800814,
-7.88579450822828));
#35284=CARTESIAN_POINT('Ctrl Pts',(-0.89583535760294,-0.383242232620388,
-7.89519614874726));
#35285=CARTESIAN_POINT('Ctrl Pts',(-0.96154694995546,-0.173650789240365,
-7.91141309212273));
#35286=CARTESIAN_POINT('Ctrl Pts',(-0.976299127968143,-0.0474944798539945,
-7.92061325736621));
#35287=CARTESIAN_POINT('Ctrl Pts',(-0.955530645539925,0.224147261598739,
-7.94074891076125));
#35288=CARTESIAN_POINT('Ctrl Pts',(-0.91188325997272,0.34594700697088,-7.95010923778401));
#35289=CARTESIAN_POINT('Ctrl Pts',(-0.807592225727651,0.54954699192881,
-7.96699174959113));
#35290=CARTESIAN_POINT('Ctrl Pts',(-0.731634438299227,0.648219317689515,
-7.97602185833242));
#35291=CARTESIAN_POINT('Ctrl Pts',(-0.519253362836699,0.835147785103102,
-7.99694128249182));
#35292=CARTESIAN_POINT('Ctrl Pts',(-0.394382545000818,0.890311605080883,
-8.00677991288573));
#35293=CARTESIAN_POINT('Ctrl Pts',(-0.229487696201209,0.945169712744932,
-8.01960378451543));
#35294=CARTESIAN_POINT('Ctrl Pts',(-0.103440253515942,0.977763677308026,
-8.02898969145012));
#35295=CARTESIAN_POINT('Ctrl Pts',(0.184189748428156,0.960792073154365,
-8.0502936448101));
#35296=CARTESIAN_POINT('Ctrl Pts',(0.311040850131801,0.926823882769417,
-8.0597974776915));
#35297=CARTESIAN_POINT('Ctrl Pts',(0.522317084702464,0.82373430143044,-8.07714869606713));
#35298=CARTESIAN_POINT('Ctrl Pts',(0.627925007800295,0.753621699865985,
-8.08632949942849));
#35299=CARTESIAN_POINT('Ctrl Pts',(0.808291869592366,0.550140906266646,
-8.10642401422356));
#35300=CARTESIAN_POINT('Ctrl Pts',(0.87394342749214,0.437853235013805,-8.11583654951944));
#35301=CARTESIAN_POINT('Ctrl Pts',(0.958431878966911,0.196473510716756,
-8.13472147475153));
#35302=CARTESIAN_POINT('Ctrl Pts',(0.975880231838361,0.0702848706249561,
-8.14396347911438));
#35303=CARTESIAN_POINT('Ctrl Pts',(0.959947904054336,-0.183126801657149,
-8.16271459253308));
#35304=CARTESIAN_POINT('Ctrl Pts',(0.927961314958701,-0.307075814244942,
-8.17198309422699));
#35305=CARTESIAN_POINT('Ctrl Pts',(0.810836783038454,-0.55257418208226,
-8.19208225220743));
#35306=CARTESIAN_POINT('Ctrl Pts',(0.727428616466516,-0.650090720524158,
-8.20137201430004));
#35307=CARTESIAN_POINT('Ctrl Pts',(0.554830637668136,-0.804089741468123,
-8.21844551120585));
#35308=CARTESIAN_POINT('Ctrl Pts',(0.447347381110085,-0.869095961842079,
-8.22754978352812));
#35309=CARTESIAN_POINT('Ctrl Pts',(0.190085901191508,-0.963314868905315,
-8.24780436867206));
#35310=CARTESIAN_POINT('Ctrl Pts',(0.0593773685688175,-0.973041258364987,
-8.25727548736166));
#35311=CARTESIAN_POINT('Ctrl Pts',(-0.164812872673331,-0.962733764741733,
-8.27383687615867));
#35312=CARTESIAN_POINT('Ctrl Pts',(-0.284713736492387,-0.935119778603541,
-8.28276631457827));
#35313=CARTESIAN_POINT('Ctrl Pts',(-0.50550084830103,-0.836647957297407,
-8.30064243112206));
#35314=CARTESIAN_POINT('Ctrl Pts',(-0.606159982100893,-0.765891415849572,
-8.3095718695417));
#35315=CARTESIAN_POINT('Ctrl Pts',(-0.763625880418338,-0.605978941163823,
-8.32613325833872));
#35316=CARTESIAN_POINT('Ctrl Pts',(-0.843724779454849,-0.502231702523655,
-8.33560437702835));
#35317=CARTESIAN_POINT('Ctrl Pts',(-0.945519248298758,-0.2478725910081,
-8.35585896217228));
#35318=CARTESIAN_POINT('Ctrl Pts',(-0.968971023406307,-0.124468890204761,
-8.36496323449451));
#35319=CARTESIAN_POINT('Ctrl Pts',(-0.969718982672265,0.106843023223732,
-8.3820367314003));
#35320=CARTESIAN_POINT('Ctrl Pts',(-0.952896543688453,0.234057028220043,
-8.39132649349289));
#35321=CARTESIAN_POINT('Ctrl Pts',(-0.848502485829639,0.485233231854166,
-8.41142565147333));
#35322=CARTESIAN_POINT('Ctrl Pts',(-0.777655722913494,0.59185047149092,
-8.42069415316726));
#35323=CARTESIAN_POINT('Ctrl Pts',(-0.599760572964985,0.773026160649791,
-8.43944526658599));
#35324=CARTESIAN_POINT('Ctrl Pts',(-0.494216597850722,0.844359793833639,
-8.44868727094887));
#35325=CARTESIAN_POINT('Ctrl Pts',(-0.258175251552615,0.942782111282781,
-8.46757219618098));
#35326=CARTESIAN_POINT('Ctrl Pts',(-0.130765826826681,0.968963911470147,
-8.4769847314769));
#35327=CARTESIAN_POINT('Ctrl Pts',(0.141141368764922,0.970728899308694,
-8.49707924627199));
#35328=CARTESIAN_POINT('Ctrl Pts',(0.263869764194396,0.939002707061653,
-8.50626004963336));
#35329=CARTESIAN_POINT('Ctrl Pts',(0.481737656636674,0.850692512192593,
-8.52361126800899));
#35330=CARTESIAN_POINT('Ctrl Pts',(0.59176831279853,0.779010613040467,-8.53311510089038));
#35331=CARTESIAN_POINT('Ctrl Pts',(0.79658086918973,0.576351120022354,-8.55441905425033));
#35332=CARTESIAN_POINT('Ctrl Pts',(0.85655168261401,0.460792364963875,-8.56380496118504));
#35333=CARTESIAN_POINT('Ctrl Pts',(0.925914408979285,0.30145456239256,-8.57662883281474));
#35334=CARTESIAN_POINT('Ctrl Pts',(0.968306855462314,0.171690743618857,
-8.5864674632087));
#35335=CARTESIAN_POINT('Ctrl Pts',(0.971136842407738,-0.111222607635891,
-8.607386887368));
#35336=CARTESIAN_POINT('Ctrl Pts',(0.948476372601592,-0.233665722796339,
-8.61641699610915));
#35337=CARTESIAN_POINT('Ctrl Pts',(0.866680152751073,-0.447298473368225,
-8.63329950791612));
#35338=CARTESIAN_POINT('Ctrl Pts',(0.805223850365105,-0.561155379775405,
-8.64265983493872));
#35339=CARTESIAN_POINT('Ctrl Pts',(0.616996729226062,-0.758109984772501,
-8.66279548833384));
#35340=CARTESIAN_POINT('Ctrl Pts',(0.513278309612551,-0.831427994749503,
-8.6719956535775));
#35341=CARTESIAN_POINT('Ctrl Pts',(0.313433860062192,-0.922580517982871,
-8.68821259695317));
#35342=CARTESIAN_POINT('Ctrl Pts',(0.190196585754628,-0.964233909424812,
-8.69761423747229));
#35343=CARTESIAN_POINT('Ctrl Pts',(-0.0936305289987827,-0.972967651905939,
-8.71858928893115));
#35344=CARTESIAN_POINT('Ctrl Pts',(-0.221167848283909,-0.952162992497402,
-8.72794202661001));
#35345=CARTESIAN_POINT('Ctrl Pts',(-0.459402726619743,-0.863875323940806,
-8.74671181142578));
#35346=CARTESIAN_POINT('Ctrl Pts',(-0.565831472897816,-0.79789193266667,
-8.75579515540647));
#35347=CARTESIAN_POINT('Ctrl Pts',(-0.753251241861667,-0.623077115572176,
-8.77471535175737));
#35348=CARTESIAN_POINT('Ctrl Pts',(-0.830121335358711,-0.517173188849598,
-8.78418479960575));
#35349=CARTESIAN_POINT('Ctrl Pts',(-0.943351358027896,-0.269030164792749,
-8.80434825399811));
#35350=CARTESIAN_POINT('Ctrl Pts',(-0.964048729229666,-0.144361544739943,
-8.81349685078773));
#35351=CARTESIAN_POINT('Ctrl Pts',(-0.973856013903567,0.0867272235402903,
-8.830565938197));
#35352=CARTESIAN_POINT('Ctrl Pts',(-0.954233524433085,0.21688920235632,
-8.84009505294611));
#35353=CARTESIAN_POINT('Ctrl Pts',(-0.867075844584167,0.451317654377397,
-8.85858893194271));
#35354=CARTESIAN_POINT('Ctrl Pts',(-0.802782957983994,0.556393866127063,
-8.86752821475173));
#35355=CARTESIAN_POINT('Ctrl Pts',(-0.652870452434931,0.724003523585264,
-8.8841223980206));
#35356=CARTESIAN_POINT('Ctrl Pts',(-0.55446394140407,0.810306450929307,
-8.89358160675802));
#35357=CARTESIAN_POINT('Ctrl Pts',(-0.307224094184925,0.927930571195957,
-8.91382274967911));
#35358=CARTESIAN_POINT('Ctrl Pts',(-0.185422291407291,0.959186925789853,
-8.92293638179297));
#35359=CARTESIAN_POINT('Ctrl Pts',(0.0456345727863289,0.974546843206883,
-8.94002896572626));
#35360=CARTESIAN_POINT('Ctrl Pts',(0.173547971727256,0.965729495041201,
-8.94931166607434));
#35361=CARTESIAN_POINT('Ctrl Pts',(0.430853797139274,0.877377505913247,
-8.96941319072267));
#35362=CARTESIAN_POINT('Ctrl Pts',(0.541843176296524,0.813335765249629,
-8.9786906394001));
#35363=CARTESIAN_POINT('Ctrl Pts',(0.73384309180208,0.647133684352001,-8.99744472962074));
#35364=CARTESIAN_POINT('Ctrl Pts',(0.811550342016074,0.546324878994273,
-9.00667923390641));
#35365=CARTESIAN_POINT('Ctrl Pts',(0.924606730993031,0.317066970465836,
-9.02555375849916));
#35366=CARTESIAN_POINT('Ctrl Pts',(0.958807608424653,0.191445444025986,
-9.03497445753251));
#35367=CARTESIAN_POINT('Ctrl Pts',(0.977526763343717,-0.0776682503544696,
-9.05491365636751));
#35368=CARTESIAN_POINT('Ctrl Pts',(0.95446645028955,-0.200390361982081,
-9.06396793124116));
#35369=CARTESIAN_POINT('Ctrl Pts',(0.921755948887285,-0.300215476155852,
-9.07172448866066));
#35370=CARTESIAN_POINT('',(-1.082164275363,0.6256360612436,-7.350042088616));
#35371=CARTESIAN_POINT('Ctrl Pts',(0.9134609739509,-0.2804380286241,-6.038826865909));
#35372=CARTESIAN_POINT('Ctrl Pts',(0.8472860717472,-0.4959872211307,-6.055726957101));
#35373=CARTESIAN_POINT('Ctrl Pts',(0.5562136135091,-0.8771468390869,-6.089527139485));
#35374=CARTESIAN_POINT('Ctrl Pts',(-0.1479368148011,-1.028187435632,-6.140227413061));
#35375=CARTESIAN_POINT('Ctrl Pts',(-0.7809283426593,-0.6849092846179,-6.190927686637));
#35376=CARTESIAN_POINT('Ctrl Pts',(-1.038659599125,-0.01255389358613,-6.241627960213));
#35377=CARTESIAN_POINT('Ctrl Pts',(-0.7972539277561,0.6658500520475,-6.292328233789));
#35378=CARTESIAN_POINT('Ctrl Pts',(-0.1727259298309,1.024272829731,-6.343028507365));
#35379=CARTESIAN_POINT('Ctrl Pts',(0.5348065635462,0.8904782587224,-6.393728780941));
#35380=CARTESIAN_POINT('Ctrl Pts',(0.9853354927582,0.3287604328168,-6.444429054517));
#35381=CARTESIAN_POINT('Ctrl Pts',(0.962357464606,-0.3909444763488,-6.495129328093));
#35382=CARTESIAN_POINT('Ctrl Pts',(0.4769146324961,-0.9227794476316,-6.545829601669));
#35383=CARTESIAN_POINT('Ctrl Pts',(-0.2377114659494,-1.011168992981,-6.596529875245));
#35384=CARTESIAN_POINT('Ctrl Pts',(-0.8381043522096,-0.6136371639345,-6.647230148821));
#35385=CARTESIAN_POINT('Ctrl Pts',(-1.035742780039,0.07878050272052,-6.697930422397));
#35386=CARTESIAN_POINT('Ctrl Pts',(-0.7356507985394,0.7333398779728,-6.748630695973));
#35387=CARTESIAN_POINT('Ctrl Pts',(-0.08203883102345,1.035489789534,-6.799330969549));
#35388=CARTESIAN_POINT('Ctrl Pts',(0.6109972307107,0.8400308673404,-6.850031243125));
#35389=CARTESIAN_POINT('Ctrl Pts',(1.010416085914,0.240891692159,-6.900731516701));
#35390=CARTESIAN_POINT('Ctrl Pts',(0.9242753777111,-0.4740089663433,-6.951431790277));
#35391=CARTESIAN_POINT('Ctrl Pts',(0.3939703741324,-0.9611226864031,-7.002132063853));
#35392=CARTESIAN_POINT('Ctrl Pts',(-0.3256586966498,-0.9863649869347,-7.052832337429));
#35393=CARTESIAN_POINT('Ctrl Pts',(-0.8887911546714,-0.5376055773403,-7.103532611005));
#35394=CARTESIAN_POINT('Ctrl Pts',(-1.024811406463,0.169502380053,-7.154232884581));
#35395=CARTESIAN_POINT('Ctrl Pts',(-0.668354359975,0.7951552821763,-7.204933158157));
#35396=CARTESIAN_POINT('Ctrl Pts',(0.009283076393916,1.038693063406,-7.255633431733));
#35397=CARTESIAN_POINT('Ctrl Pts',(0.682459562086,0.7830827132473,-7.306333705309));
#35398=CARTESIAN_POINT('Ctrl Pts',(1.027677067702,0.151158595784,-7.357033978885));
#35399=CARTESIAN_POINT('Ctrl Pts',(0.8790411425118,-0.5534047225185,-7.407734252461));
#35400=CARTESIAN_POINT('Ctrl Pts',(0.3079748064376,-0.9920296778312,-7.458434526037));
#35401=CARTESIAN_POINT('Ctrl Pts',(-0.41107659886,-0.9539212936056,-7.509134799613));
#35402=CARTESIAN_POINT('Ctrl Pts',(-0.9326337707599,-0.4574373767019,-7.559835073189));
#35403=CARTESIAN_POINT('Ctrl Pts',(-1.005822266638,0.2590014075395,-7.610535346765));
#35404=CARTESIAN_POINT('Ctrl Pts',(-0.7328469964043,0.6533240319803,-7.644335529149));
#35405=CARTESIAN_POINT('Ctrl Pts',(-0.548159772547,0.7826731773806,-7.661235620341));
#35406=CARTESIAN_POINT('Ctrl Pts',(1.011899778108,-0.3106593352427,-6.098278598537));
#35407=CARTESIAN_POINT('Ctrl Pts',(0.9385935605836,-0.5494371115119,-6.115178689729));
#35408=CARTESIAN_POINT('Ctrl Pts',(0.6161537801183,-0.9716722631302,-6.148978872113));
#35409=CARTESIAN_POINT('Ctrl Pts',(-0.1638791741958,-1.138989697031,-6.199679145689));
#35410=CARTESIAN_POINT('Ctrl Pts',(-0.8650848138998,-0.7587182954638,-6.250379419265));
#35411=CARTESIAN_POINT('Ctrl Pts',(-1.150590389579,-0.0139067595622,-6.301079692841));
#35412=CARTESIAN_POINT('Ctrl Pts',(-0.8831697199965,0.7376051513243,-6.351779966417));
#35413=CARTESIAN_POINT('Ctrl Pts',(-0.1913396795852,1.134653234986,-6.402480239993));
#35414=CARTESIAN_POINT('Ctrl Pts',(0.5924398068615,0.9864403385659,-6.453180513569));
#35415=CARTESIAN_POINT('Ctrl Pts',(1.091519829436,0.3641891865167,-6.503880787145));
#35416=CARTESIAN_POINT('Ctrl Pts',(1.066065582072,-0.4330744718724,-6.554581060721));
#35417=CARTESIAN_POINT('Ctrl Pts',(0.5283091719965,-1.022222453864,-6.605281334297));
#35418=CARTESIAN_POINT('Ctrl Pts',(-0.2633283594015,-1.120137267826,-6.655981607873));
#35419=CARTESIAN_POINT('Ctrl Pts',(-0.9284223762335,-0.6797655594833,-6.706681881449));
#35420=CARTESIAN_POINT('Ctrl Pts',(-1.1473592405,0.0872702561964,-6.757382155025));
#35421=CARTESIAN_POINT('Ctrl Pts',(-0.8149279509853,0.8123679948675,-6.808082428601));
#35422=CARTESIAN_POINT('Ctrl Pts',(-0.09087971711565,1.147078986561,-6.858782702177));
#35423=CARTESIAN_POINT('Ctrl Pts',(0.6768411347738,0.9305565015973,-6.909482975753));
#35424=CARTESIAN_POINT('Ctrl Pts',(1.119303223991,0.2668513015826,-6.960183249329));
#35425=CARTESIAN_POINT('Ctrl Pts',(1.023879592328,-0.5250903777413,-7.010883522905));
#35426=CARTESIAN_POINT('Ctrl Pts',(0.4364264544781,-1.064697738426,-7.061583796481));
#35427=CARTESIAN_POINT('Ctrl Pts',(-0.3607531928305,-1.092660266695,-7.112284070057));
#35428=CARTESIAN_POINT('Ctrl Pts',(-0.9845714243337,-0.5955404554036,-7.162984343633));
#35429=CARTESIAN_POINT('Ctrl Pts',(-1.135249851252,0.1877687450866,-7.213684617209));
#35430=CARTESIAN_POINT('Ctrl Pts',(-0.7403793351246,0.8808449146057,-7.264384890785));
#35431=CARTESIAN_POINT('Ctrl Pts',(0.01028346389286,1.150627460127,-7.315085164361));
#35432=CARTESIAN_POINT('Ctrl Pts',(0.7560045794353,0.8674713494848,-7.365785437937));
#35433=CARTESIAN_POINT('Ctrl Pts',(1.138424329478,0.1674481492858,-7.416485711513));
#35434=CARTESIAN_POINT('Ctrl Pts',(0.9737707055048,-0.613042189967,-7.467185985089));
#35435=CARTESIAN_POINT('Ctrl Pts',(0.34116360434,-1.098935411036,-7.517886258665));
#35436=CARTESIAN_POINT('Ctrl Pts',(-0.455376125564,-1.056720290038,-7.568586532241));
#35437=CARTESIAN_POINT('Ctrl Pts',(-1.033138724697,-0.5067329565058,-7.619286805817));
#35438=CARTESIAN_POINT('Ctrl Pts',(-1.114214353379,0.2869126041425,-7.669987079393));
#35439=CARTESIAN_POINT('Ctrl Pts',(-0.8118219980882,0.7237292690611,-7.703787261777));
#35440=CARTESIAN_POINT('Ctrl Pts',(-0.607232019786,0.867017680128,-7.720687352969));
#35441=CARTESIAN_POINT('Ctrl Pts',(1.110338582265,-0.3408806418612,-6.157730331166));
#35442=CARTESIAN_POINT('Ctrl Pts',(1.02990104942,-0.6028870018931,-6.174630422358));
#35443=CARTESIAN_POINT('Ctrl Pts',(0.6760939467275,-1.066197687173,-6.208430604742));
#35444=CARTESIAN_POINT('Ctrl Pts',(-0.1798215335905,-1.249791958429,-6.259130878318));
#35445=CARTESIAN_POINT('Ctrl Pts',(-0.9492412851402,-0.8325273063098,-6.309831151894));
#35446=CARTESIAN_POINT('Ctrl Pts',(-1.262521180034,-0.01525962553827,-6.36053142547));
#35447=CARTESIAN_POINT('Ctrl Pts',(-0.9690855122368,0.8093602506011,-6.411231699046));
#35448=CARTESIAN_POINT('Ctrl Pts',(-0.2099534293395,1.24503364024,-6.461931972622));
#35449=CARTESIAN_POINT('Ctrl Pts',(0.6500730501767,1.08240241841,-6.512632246198));
#35450=CARTESIAN_POINT('Ctrl Pts',(1.197704166115,0.3996179402166,-6.563332519774));
#35451=CARTESIAN_POINT('Ctrl Pts',(1.169773699538,-0.475204467396,-6.61403279335));
#35452=CARTESIAN_POINT('Ctrl Pts',(0.5797037114969,-1.121665460096,-6.664733066926));
#35453=CARTESIAN_POINT('Ctrl Pts',(-0.2889452528537,-1.22910554267,-6.715433340502));
#35454=CARTESIAN_POINT('Ctrl Pts',(-1.018740400257,-0.7458939550322,-6.766133614078));
#35455=CARTESIAN_POINT('Ctrl Pts',(-1.25897570096,0.09576000967229,-6.816833887654));
#35456=CARTESIAN_POINT('Ctrl Pts',(-0.8942051034311,0.8913961117622,-6.86753416123));
#35457=CARTESIAN_POINT('Ctrl Pts',(-0.09972060320785,1.258668183588,-6.918234434806));
#35458=CARTESIAN_POINT('Ctrl Pts',(0.742685038837,1.021082135854,-6.968934708382));
#35459=CARTESIAN_POINT('Ctrl Pts',(1.228190362067,0.2928109110062,-7.019634981958));
#35460=CARTESIAN_POINT('Ctrl Pts',(1.123483806945,-0.5761717891393,-7.070335255534));
#35461=CARTESIAN_POINT('Ctrl Pts',(0.4788825348239,-1.168272790448,-7.12103552911));
#35462=CARTESIAN_POINT('Ctrl Pts',(-0.3958476890111,-1.198955546455,-7.171735802686));
#35463=CARTESIAN_POINT('Ctrl Pts',(-1.080351693996,-0.6534753334669,-7.222436076262));
#35464=CARTESIAN_POINT('Ctrl Pts',(-1.245688296041,0.2060351101202,-7.273136349838));
#35465=CARTESIAN_POINT('Ctrl Pts',(-0.8124043102742,0.966534547035,-7.323836623414));
#35466=CARTESIAN_POINT('Ctrl Pts',(0.0112838513918,1.262561856849,-7.37453689699));
#35467=CARTESIAN_POINT('Ctrl Pts',(0.8295495967846,0.9518599857224,-7.425237170566));
#35468=CARTESIAN_POINT('Ctrl Pts',(1.249171591254,0.1837377027876,-7.475937444142));
#35469=CARTESIAN_POINT('Ctrl Pts',(1.068500268498,-0.6726796574155,-7.526637717718));
#35470=CARTESIAN_POINT('Ctrl Pts',(0.3743524022424,-1.20584114424,-7.577337991294));
#35471=CARTESIAN_POINT('Ctrl Pts',(-0.499675652268,-1.15951928647,-7.62803826487));
#35472=CARTESIAN_POINT('Ctrl Pts',(-1.133643678633,-0.5560285363098,-7.678738538446));
#35473=CARTESIAN_POINT('Ctrl Pts',(-1.222606440119,0.3148238007455,-7.729438812022));
#35474=CARTESIAN_POINT('Ctrl Pts',(-0.8907969997721,0.7941345061418,-7.763238994406));
#35475=CARTESIAN_POINT('Ctrl Pts',(-0.666304267025,0.9513621828753,-7.780139085598));
#35476=CARTESIAN_POINT('Ctrl Pts',(1.208777386421,-0.3711019484798,-6.217182063794));
#35477=CARTESIAN_POINT('Ctrl Pts',(1.121208538256,-0.6563368922743,-6.234082154986));
#35478=CARTESIAN_POINT('Ctrl Pts',(0.7360341133366,-1.160723111217,-6.26788233737));
#35479=CARTESIAN_POINT('Ctrl Pts',(-0.1957638929852,-1.360594219827,-6.318582610946));
#35480=CARTESIAN_POINT('Ctrl Pts',(-1.033397756381,-0.9063363171557,-6.369282884522));
#35481=CARTESIAN_POINT('Ctrl Pts',(-1.374451970489,-0.01661249151435,-6.419983158098));
#35482=CARTESIAN_POINT('Ctrl Pts',(-1.055001304477,0.8811153498779,-6.470683431674));
#35483=CARTESIAN_POINT('Ctrl Pts',(-0.2285671790938,1.355414045495,-6.52138370525));
#35484=CARTESIAN_POINT('Ctrl Pts',(0.707706293492,1.178364498253,-6.572083978826));
#35485=CARTESIAN_POINT('Ctrl Pts',(1.303888502793,0.4350466939165,-6.622784252402));
#35486=CARTESIAN_POINT('Ctrl Pts',(1.273481817004,-0.5173344629195,-6.673484525978));
#35487=CARTESIAN_POINT('Ctrl Pts',(0.6310982509973,-1.221108466328,-6.724184799554));
#35488=CARTESIAN_POINT('Ctrl Pts',(-0.3145621463059,-1.338073817515,-6.77488507313));
#35489=CARTESIAN_POINT('Ctrl Pts',(-1.109058424281,-0.8120223505811,-6.825585346706));
#35490=CARTESIAN_POINT('Ctrl Pts',(-1.370592161421,0.1042497631482,-6.876285620282));
#35491=CARTESIAN_POINT('Ctrl Pts',(-0.973482255877,0.9704242286569,-6.926985893858));
#35492=CARTESIAN_POINT('Ctrl Pts',(-0.1085614893,1.370257380614,-6.977686167434));
#35493=CARTESIAN_POINT('Ctrl Pts',(0.8085289429002,1.111607770111,-7.02838644101));
#35494=CARTESIAN_POINT('Ctrl Pts',(1.337077500144,0.3187705204298,-7.079086714586));
#35495=CARTESIAN_POINT('Ctrl Pts',(1.223088021562,-0.6272532005374,-7.129786988162));
#35496=CARTESIAN_POINT('Ctrl Pts',(0.5213386151697,-1.271847842471,-7.180487261738));
#35497=CARTESIAN_POINT('Ctrl Pts',(-0.4309421851917,-1.305250826215,-7.231187535314));
#35498=CARTESIAN_POINT('Ctrl Pts',(-1.176131963658,-0.7114102115302,-7.28188780889));
#35499=CARTESIAN_POINT('Ctrl Pts',(-1.35612674083,0.2243014751538,-7.332588082466));
#35500=CARTESIAN_POINT('Ctrl Pts',(-0.8844292854238,1.052224179464,-7.383288356042));
#35501=CARTESIAN_POINT('Ctrl Pts',(0.01228423889075,1.37449625357,-7.433988629618));
#35502=CARTESIAN_POINT('Ctrl Pts',(0.9030946141339,1.03624862196,-7.484688903194));
#35503=CARTESIAN_POINT('Ctrl Pts',(1.359918853029,0.2000272562895,-7.53538917677));
#35504=CARTESIAN_POINT('Ctrl Pts',(1.163229831491,-0.732317124864,-7.586089450346));
#35505=CARTESIAN_POINT('Ctrl Pts',(0.4075412001447,-1.312746877444,-7.636789723922));
#35506=CARTESIAN_POINT('Ctrl Pts',(-0.5439751789721,-1.262318282903,-7.687489997498));
#35507=CARTESIAN_POINT('Ctrl Pts',(-1.23414863257,-0.6053241161137,-7.738190271074));
#35508=CARTESIAN_POINT('Ctrl Pts',(-1.330998526859,0.3427349973485,-7.78889054465));
#35509=CARTESIAN_POINT('Ctrl Pts',(-0.9697720014561,0.8645397432226,-7.822690727034));
#35510=CARTESIAN_POINT('Ctrl Pts',(-0.725376514264,1.035706685623,-7.839590818226));
#35511=CARTESIAN_POINT('',(0.9280544183911,-0.8364143225921,-6.23965809256072));
#35512=CARTESIAN_POINT('Ctrl Pts',(-1.08144091415521,0.625238554653748,
-7.35009940962399));
#35513=CARTESIAN_POINT('Ctrl Pts',(-1.13845941588873,0.526794183586659,
-7.34364665860282));
#35514=CARTESIAN_POINT('Ctrl Pts',(-1.19439067109551,0.400143823427812,
-7.33585368731547));
#35515=CARTESIAN_POINT('Ctrl Pts',(-1.25119108729651,0.118585425996973,
-7.31907932790072));
#35516=CARTESIAN_POINT('Ctrl Pts',(-1.25593947156391,-0.0140855441947595,
-7.31159686950582));
#35517=CARTESIAN_POINT('Ctrl Pts',(-1.22529757201621,-0.276529705002004,
-7.29662426640538));
#35518=CARTESIAN_POINT('Ctrl Pts',(-1.18906778938012,-0.406719794981607,
-7.28908149497592));
#35519=CARTESIAN_POINT('Ctrl Pts',(-1.10137406144739,-0.595950494314858,
-7.27699564285035));
#35520=CARTESIAN_POINT('Ctrl Pts',(-1.06370367262132,-0.660673233860386,
-7.27262032993749));
#35521=CARTESIAN_POINT('Ctrl Pts',(-0.971992258317847,-0.789531566420169,
-7.26351469895125));
#35522=CARTESIAN_POINT('Ctrl Pts',(-0.917017581242872,-0.852353804178172,
-7.2587927042533));
#35523=CARTESIAN_POINT('Ctrl Pts',(-0.756971603418245,-1.00285400129472,
-7.24633659192418));
#35524=CARTESIAN_POINT('Ctrl Pts',(-0.642298996377849,-1.08057458876947,
-7.23860555019741));
#35525=CARTESIAN_POINT('Ctrl Pts',(-0.453827957240571,-1.16684560048204,
-7.22658638206331));
#35526=CARTESIAN_POINT('Ctrl Pts',(-0.387529057819546,-1.19043933362089,
-7.22247029669801));
#35527=CARTESIAN_POINT('Ctrl Pts',(-0.238834653791269,-1.22930303428804,
-7.21360777094392));
#35528=CARTESIAN_POINT('Ctrl Pts',(-0.156340711699991,-1.24219522029809,
-7.20888047579269));
#35529=CARTESIAN_POINT('Ctrl Pts',(0.0641921503111542,-1.25493503764991,
-7.19635390921882));
#35530=CARTESIAN_POINT('Ctrl Pts',(0.203231193855402,-1.24059849399102,
-7.1885643218617));
#35531=CARTESIAN_POINT('Ctrl Pts',(0.400249068389142,-1.18604301244094,
-7.17672562103673));
#35532=CARTESIAN_POINT('Ctrl Pts',(0.462519894877283,-1.16315139144511,
-7.17284152673707));
#35533=CARTESIAN_POINT('Ctrl Pts',(0.669055230915653,-1.06741042621854,
-7.15968337989695));
#35534=CARTESIAN_POINT('Ctrl Pts',(0.801914381946556,-0.970913148856214,
-7.15062451754881));
#35535=CARTESIAN_POINT('Ctrl Pts',(1.01686078903117,-0.742279077871929,
-7.13276658058505));
#35536=CARTESIAN_POINT('Ctrl Pts',(1.0968524668718,-0.617844041552233,-7.12420955314268));
#35537=CARTESIAN_POINT('Ctrl Pts',(1.18530342790498,-0.403842745066263,
-7.11088809527967));
#35538=CARTESIAN_POINT('Ctrl Pts',(1.20932189186302,-0.32388207356038,-7.10616843028997));
#35539=CARTESIAN_POINT('Ctrl Pts',(1.25150036893193,-0.109861760058388,
-7.09380383094239));
#35540=CARTESIAN_POINT('Ctrl Pts',(1.2566190093772,0.0269369245505145,-7.08615896767945));
#35541=CARTESIAN_POINT('Ctrl Pts',(1.23004537676662,0.23457038514643,-7.074016349761));
#35542=CARTESIAN_POINT('Ctrl Pts',(1.213950499144,0.306782464954891,-7.06969350282979));
#35543=CARTESIAN_POINT('Ctrl Pts',(1.16603740630127,0.456571322769034,-7.06063903711535));
#35544=CARTESIAN_POINT('Ctrl Pts',(1.13276358119362,0.533151262793348,-7.05591658816548));
#35545=CARTESIAN_POINT('Ctrl Pts',(1.02636194887124,0.724653732998469,-7.0434971171023));
#35546=CARTESIAN_POINT('Ctrl Pts',(0.941242131519351,0.833109088899172,
-7.03580329128069));
#35547=CARTESIAN_POINT('Ctrl Pts',(0.788394273768947,0.972607904358993,
-7.0238063653535));
#35548=CARTESIAN_POINT('Ctrl Pts',(0.732231243339065,1.015483219647,-7.019673727507));
#35549=CARTESIAN_POINT('Ctrl Pts',(0.60222128539102,1.09797945750687,-7.01079519081006));
#35550=CARTESIAN_POINT('Ctrl Pts',(0.527586212742716,1.13540556649639,-7.00606801275208));
#35551=CARTESIAN_POINT('Ctrl Pts',(0.321385388788767,1.21478868557968,-6.99353817344243));
#35552=CARTESIAN_POINT('Ctrl Pts',(0.184535948543945,1.24352468862241,-6.98574504666367));
#35553=CARTESIAN_POINT('Ctrl Pts',(-0.0198864739890845,1.25160529301129,
-6.97389700631672));
#35554=CARTESIAN_POINT('Ctrl Pts',(-0.0862656311501007,1.24876529684857,
-6.97000742825624));
#35555=CARTESIAN_POINT('Ctrl Pts',(-0.312234498867914,1.22045076352206,
-6.95684511453382));
#35556=CARTESIAN_POINT('Ctrl Pts',(-0.46816438855612,1.16899975646828,-6.94778687483531));
#35557=CARTESIAN_POINT('Ctrl Pts',(-0.741904897123531,1.01702921803696,
-6.92996880361027));
#35558=CARTESIAN_POINT('Ctrl Pts',(-0.855594423444135,0.923368273219295,
-6.92144739328836));
#35559=CARTESIAN_POINT('Ctrl Pts',(-1.00491474173641,0.747120993151983,
-6.90815669347837));
#35560=CARTESIAN_POINT('Ctrl Pts',(-1.05224489991832,0.678340844485654,
-6.90343656893941));
#35561=CARTESIAN_POINT('Ctrl Pts',(-1.15794237658074,0.48736397670007,-6.89106390268326));
#35562=CARTESIAN_POINT('Ctrl Pts',(-1.20469386492157,0.358548019629921,
-6.88341191542826));
#35563=CARTESIAN_POINT('Ctrl Pts',(-1.24277040598387,0.153182356417834,
-6.87129720714745));
#35564=CARTESIAN_POINT('Ctrl Pts',(-1.24951852581418,0.0801083073668442,
-6.86700856005424));
#35565=CARTESIAN_POINT('Ctrl Pts',(-1.24990423010732,-0.076565829009687,
-6.85798576654047));
#35566=CARTESIAN_POINT('Ctrl Pts',(-1.24174330493025,-0.159663077316491,
-6.85326245846073));
#35567=CARTESIAN_POINT('Ctrl Pts',(-1.19919680323486,-0.374893580986194,
-6.84082429682175));
#35568=CARTESIAN_POINT('Ctrl Pts',(-1.15131189136542,-0.504534513233835,
-6.8331136881208));
#35569=CARTESIAN_POINT('Ctrl Pts',(-1.04881278268726,-0.68366199337213,
-6.82115117111684));
#35570=CARTESIAN_POINT('Ctrl Pts',(-1.00904387182181,-0.74100695815593,
-6.81706860902981));
#35571=CARTESIAN_POINT('Ctrl Pts',(-0.911352540719992,-0.858895892747815,
-6.80823628859876));
#35572=CARTESIAN_POINT('Ctrl Pts',(-0.851888287296867,-0.91749957652705,
-6.80350789605541));
#35573=CARTESIAN_POINT('Ctrl Pts',(-0.668265026613998,-1.06622345316516,
-6.79010655339088));
#35574=CARTESIAN_POINT('Ctrl Pts',(-0.524441825712136,-1.14729178292643,
-6.78096206157405));
#35575=CARTESIAN_POINT('Ctrl Pts',(-0.286619386009769,-1.2191432792449,
-6.76647656088353));
#35576=CARTESIAN_POINT('Ctrl Pts',(-0.2106650741897,-1.23429105046874,-6.76199825471631));
#35577=CARTESIAN_POINT('Ctrl Pts',(0.0254923040591906,-1.25902399119274,
-6.74840675794588));
#35578=CARTESIAN_POINT('Ctrl Pts',(0.188210080940334,-1.24518018289136,
-6.73941201231742));
#35579=CARTESIAN_POINT('Ctrl Pts',(0.533113525267708,-1.14801824337071,
-6.718874944052));
#35580=CARTESIAN_POINT('Ctrl Pts',(0.670006874045706,-1.06151480982223,
-6.70956035198521));
#35581=CARTESIAN_POINT('Ctrl Pts',(0.891167699619736,-0.889705845031928,
-6.69361240794748));
#35582=CARTESIAN_POINT('Ctrl Pts',(0.999690126438071,-0.766475194873538,
-6.68455777859975));
#35583=CARTESIAN_POINT('Ctrl Pts',(1.11677488123714,-0.565928020540905,
-6.67115191316097));
#35584=CARTESIAN_POINT('Ctrl Pts',(1.14705574486821,-0.50181209517784,-6.66700163097715));
#35585=CARTESIAN_POINT('Ctrl Pts',(1.2170828887025,-0.311952024704957,-6.65528522804467));
#35586=CARTESIAN_POINT('Ctrl Pts',(1.24269004423336,-0.181621278522362,
-6.64786488682457));
#35587=CARTESIAN_POINT('Ctrl Pts',(1.2515385009026,0.0325279813153482,-6.63571498520908));
#35588=CARTESIAN_POINT('Ctrl Pts',(1.24685187992131,0.116008148491328,-6.63098694881452));
#35589=CARTESIAN_POINT('Ctrl Pts',(1.21062276726679,0.345659149496376,-6.61760475355315));
#35590=CARTESIAN_POINT('Ctrl Pts',(1.16157099219993,0.485157474530085,-6.60905675358139));
#35591=CARTESIAN_POINT('Ctrl Pts',(1.0063728134479,0.756970110543001,-6.59124987992135));
#35592=CARTESIAN_POINT('Ctrl Pts',(0.89959439455553,0.881959799323835,-6.58217933370859));
#35593=CARTESIAN_POINT('Ctrl Pts',(0.719369820494962,1.02452385547995,-6.56888886194693));
#35594=CARTESIAN_POINT('Ctrl Pts',(0.662440624582576,1.06222165136825,-6.56489101070615));
#35595=CARTESIAN_POINT('Ctrl Pts',(0.48485220812677,1.15936247999066,-6.55318361156413));
#35596=CARTESIAN_POINT('Ctrl Pts',(0.356900686552398,1.20438281988483,-6.54561797582988));
#35597=CARTESIAN_POINT('Ctrl Pts',(0.144393426698886,1.24358475220579,-6.53336382990338));
#35598=CARTESIAN_POINT('Ctrl Pts',(0.0620477895094899,1.25068971498076,
-6.52868408387922));
#35599=CARTESIAN_POINT('Ctrl Pts',(-0.0936680948074589,1.24858819902552,
-6.51970677548154));
#35600=CARTESIAN_POINT('Ctrl Pts',(-0.166508017661877,1.24104336575588,
-6.51542333541335));
#35601=CARTESIAN_POINT('Ctrl Pts',(-0.365628590584132,1.20189232020038,
-6.50366515590112));
#35602=CARTESIAN_POINT('Ctrl Pts',(-0.488609145957327,1.15677135627177,
-6.49633876007959));
#35603=CARTESIAN_POINT('Ctrl Pts',(-0.674921949564665,1.0544298326615,-6.48429081890586));
#35604=CARTESIAN_POINT('Ctrl Pts',(-0.743941992643752,1.00724740684214,
-6.47956668412178));
#35605=CARTESIAN_POINT('Ctrl Pts',(-0.925097327137965,0.85473233049542,
-6.46595196737));
#35606=CARTESIAN_POINT('Ctrl Pts',(-1.02191142899692,0.736327243566084,
-6.45711337782292));
#35607=CARTESIAN_POINT('Ctrl Pts',(-1.17389129062308,0.455826182550516,
-6.43896668114914));
#35608=CARTESIAN_POINT('Ctrl Pts',(-1.22379685651126,0.299157012952662,
-6.42989288930313));
#35609=CARTESIAN_POINT('Ctrl Pts',(-1.24980716087092,0.0712298930941525,
-6.41662001494264));
#35610=CARTESIAN_POINT('Ctrl Pts',(-1.25182415933548,0.003398592608898,
-6.41264668251563));
#35611=CARTESIAN_POINT('Ctrl Pts',(-1.24088522508175,-0.198759275666808,
-6.40094010361306));
#35612=CARTESIAN_POINT('Ctrl Pts',(-1.21161252387838,-0.331695448278339,
-6.39335019059184));
#35613=CARTESIAN_POINT('Ctrl Pts',(-1.13265884776994,-0.53334288847137,
-6.38106921400184));
#35614=CARTESIAN_POINT('Ctrl Pts',(-1.09525941863046,-0.607048262681095,
-6.37638841497169));
#35615=CARTESIAN_POINT('Ctrl Pts',(-1.01180373953895,-0.737481050653887,
-6.36745862467547));
#35616=CARTESIAN_POINT('Ctrl Pts',(-0.967570521889716,-0.794721975412659,
-6.36322624106468));
#35617=CARTESIAN_POINT('Ctrl Pts',(-0.829606230581431,-0.943504132115711,
-6.35146920984007));
#35618=CARTESIAN_POINT('Ctrl Pts',(-0.725782883999061,-1.02485139482369,
-6.34409347751394));
#35619=CARTESIAN_POINT('Ctrl Pts',(-0.539826516001505,-1.12958576426288,
-6.33199527779046));
#35620=CARTESIAN_POINT('Ctrl Pts',(-0.463351068505991,-1.16333510483609,
-6.32727081415333));
#35621=CARTESIAN_POINT('Ctrl Pts',(-0.236432299447394,-1.23737660634955,
-6.31354543564448));
#35622=CARTESIAN_POINT('Ctrl Pts',(-0.083838606894931,-1.25671070950491,
-6.30466986447607));
#35623=CARTESIAN_POINT('Ctrl Pts',(0.234319781210057,-1.23724994774721,
-6.28655599010737));
#35624=CARTESIAN_POINT('Ctrl Pts',(0.393564405146679,-1.19675981713808,
-6.27748794480623));
#35625=CARTESIAN_POINT('Ctrl Pts',(0.611700856771692,-1.09306215307407,
-6.26349273975741));
#35626=CARTESIAN_POINT('Ctrl Pts',(0.680192833559366,-1.05171705293845,
-6.25880773384765));
#35627=CARTESIAN_POINT('Ctrl Pts',(0.810992282165546,-0.954164575612996,
-6.24939904171304));
#35628=CARTESIAN_POINT('Ctrl Pts',(0.872476840637322,-0.897918805592539,
-6.2446792108443));
#35629=CARTESIAN_POINT('Ctrl Pts',(0.927936718582964,-0.836284130747026,
-6.23997634988408));
#35630=CARTESIAN_POINT('',(0.720545178071692,-0.649395442066378,-6.07837558621596));
#35631=CARTESIAN_POINT('',(0.7205452572168,-0.6493955129983,-6.078375595519));
#35632=CARTESIAN_POINT('Ctrl Pts',(0.720108814885489,-0.649004361933079,
-6.07835980896107));
#35633=CARTESIAN_POINT('Ctrl Pts',(0.649924585346467,-0.727158430109657,
-6.08611596373328));
#35634=CARTESIAN_POINT('Ctrl Pts',(0.555079528159261,-0.80838028401483,
-6.09517025738535));
#35635=CARTESIAN_POINT('Ctrl Pts',(0.312518521341734,-0.926442422296045,
-6.11510971969884));
#35636=CARTESIAN_POINT('Ctrl Pts',(0.186587724758927,-0.959486368703356,
-6.12453041873231));
#35637=CARTESIAN_POINT('Ctrl Pts',(-0.0685031170829461,-0.975905812045906,
-6.14340494332513));
#35638=CARTESIAN_POINT('Ctrl Pts',(-0.194639787589674,-0.958865497291617,
-6.15263944761075));
#35639=CARTESIAN_POINT('Ctrl Pts',(-0.434477044399925,-0.875407786476393,
-6.17139353783132));
#35640=CARTESIAN_POINT('Ctrl Pts',(-0.545358094112512,-0.811178668098797,
-6.18067098650868));
#35641=CARTESIAN_POINT('Ctrl Pts',(-0.750315949779605,-0.63228026348299,
-6.2007725111569));
#35642=CARTESIAN_POINT('Ctrl Pts',(-0.82178362970336,-0.525828612563066,
-6.21005521150494));
#35643=CARTESIAN_POINT('Ctrl Pts',(-0.92376570001596,-0.317927532987132,
-6.22714779543817));
#35644=CARTESIAN_POINT('Ctrl Pts',(-0.957455434114765,-0.196776219833821,
-6.23626142755198));
#35645=CARTESIAN_POINT('Ctrl Pts',(-0.978889084396869,0.076177209082542,
-6.25650257047306));
#35646=CARTESIAN_POINT('Ctrl Pts',(-0.953200947514868,0.204521107671369,
-6.26596177921051));
#35647=CARTESIAN_POINT('Ctrl Pts',(-0.882751937182648,0.418071320821551,
-6.2825559624794));
#35648=CARTESIAN_POINT('Ctrl Pts',(-0.82377256068534,0.52621945391236,-6.29149524528844));
#35649=CARTESIAN_POINT('Ctrl Pts',(-0.664104034634088,0.718726913669791,
-6.30998912428504));
#35650=CARTESIAN_POINT('Ctrl Pts',(-0.561095305033122,0.800680464223247,
-6.31951823903411));
#35651=CARTESIAN_POINT('Ctrl Pts',(-0.35593723957073,0.90749043488932,-6.33658732644336));
#35652=CARTESIAN_POINT('Ctrl Pts',(-0.237570247179751,0.95176120530112,
-6.34573592323295));
#35653=CARTESIAN_POINT('Ctrl Pts',(0.0339733113907493,0.977453504160468,
-6.36589937762531));
#35654=CARTESIAN_POINT('Ctrl Pts',(0.16410775167376,0.963681052608347,-6.37536882547371));
#35655=CARTESIAN_POINT('Ctrl Pts',(0.409123503410254,0.888490152389851,
-6.39428902182473));
#35656=CARTESIAN_POINT('Ctrl Pts',(0.519411539030056,0.829182183637508,
-6.40337236580551));
#35657=CARTESIAN_POINT('Ctrl Pts',(0.714797598489669,0.666778804844548,
-6.42214215062138));
#35658=CARTESIAN_POINT('Ctrl Pts',(0.79646597496153,0.566634519196591,-6.43149488830038));
#35659=CARTESIAN_POINT('Ctrl Pts',(0.930521764899172,0.316308422852225,
-6.45246993975933));
#35660=CARTESIAN_POINT('Ctrl Pts',(0.955917571323847,0.188725180169855,
-6.46187158027833));
#35661=CARTESIAN_POINT('Ctrl Pts',(0.97664239769674,-0.0299459612263952,
-6.47808852365388));
#35662=CARTESIAN_POINT('Ctrl Pts',(0.964857697793123,-0.156413988815773,
-6.48728868889742));
#35663=CARTESIAN_POINT('Ctrl Pts',(0.888096285138142,-0.417810720029666,
-6.50742434229249));
#35664=CARTESIAN_POINT('Ctrl Pts',(0.820092045273133,-0.527882040545075,
-6.51678466931517));
#35665=CARTESIAN_POINT('Ctrl Pts',(0.675770062615426,-0.705366515980331,
-6.53366718112217));
#35666=CARTESIAN_POINT('Ctrl Pts',(0.5809664933872,-0.786101245828098,-6.54269728986336));
#35667=CARTESIAN_POINT('Ctrl Pts',(0.334378142358148,-0.924817352612472,
-6.56361671402265));
#35668=CARTESIAN_POINT('Ctrl Pts',(0.200770139829655,-0.95282931152194,
-6.57345534441649));
#35669=CARTESIAN_POINT('Ctrl Pts',(0.0280752756794515,-0.972225368674033,
-6.58627921604608));
#35670=CARTESIAN_POINT('Ctrl Pts',(-0.101993726346509,-0.977915627493418,
-6.59566512298073));
#35671=CARTESIAN_POINT('Ctrl Pts',(-0.37981870565778,-0.901545906814718,
-6.61696907634072));
#35672=CARTESIAN_POINT('Ctrl Pts',(-0.49684242670466,-0.841959929657246,
-6.62647290922221));
#35673=CARTESIAN_POINT('Ctrl Pts',(-0.682085252789105,-0.697218075104707,
-6.64382412759795));
#35674=CARTESIAN_POINT('Ctrl Pts',(-0.77081880044234,-0.606690908795046,
-6.65300493095937));
#35675=CARTESIAN_POINT('Ctrl Pts',(-0.904965977547019,-0.370172044703089,
-6.67309944575452));
#35676=CARTESIAN_POINT('Ctrl Pts',(-0.945851484996125,-0.246693206634984,
-6.68251198105045));
#35677=CARTESIAN_POINT('Ctrl Pts',(-0.978337809142477,0.00697411187024545,
-6.70139690628255));
#35678=CARTESIAN_POINT('Ctrl Pts',(-0.969183713860661,0.134034020754471,
-6.71063891064538));
#35679=CARTESIAN_POINT('Ctrl Pts',(-0.900941041069729,0.378603545282209,
-6.72939002406403));
#35680=CARTESIAN_POINT('Ctrl Pts',(-0.843896455480788,0.493200294182256,
-6.73865852575791));
#35681=CARTESIAN_POINT('Ctrl Pts',(-0.678314757631577,0.709001837100137,
-6.7587576837383));
#35682=CARTESIAN_POINT('Ctrl Pts',(-0.576463604726424,0.787057843739473,
-6.76804744583087));
#35683=CARTESIAN_POINT('Ctrl Pts',(-0.375632597250351,0.901830084169005,
-6.78512094273665));
#35684=CARTESIAN_POINT('Ctrl Pts',(-0.256987402283606,0.943082682135299,
-6.79422521505888));
#35685=CARTESIAN_POINT('Ctrl Pts',(0.0142369621639247,0.981786888990614,
-6.81447980020282));
#35686=CARTESIAN_POINT('Ctrl Pts',(0.144113504802178,0.964140166216503,
-6.82395091889248));
#35687=CARTESIAN_POINT('Ctrl Pts',(0.361268264905602,0.907471666524345,
-6.8405123076895));
#35688=CARTESIAN_POINT('Ctrl Pts',(0.472813840474943,0.855545430902499,
-6.84944174610912));
#35689=CARTESIAN_POINT('Ctrl Pts',(0.668319496067421,0.713344210924143,
-6.86731786265288));
#35690=CARTESIAN_POINT('Ctrl Pts',(0.752078467845626,0.623215502836168,
-6.87624730107246));
#35691=CARTESIAN_POINT('Ctrl Pts',(0.872877916954441,0.43407269491594,-6.89280868986945));
#35692=CARTESIAN_POINT('Ctrl Pts',(0.929670083339895,0.315945758997088,
-6.90227980855905));
#35693=CARTESIAN_POINT('Ctrl Pts',(0.976387595491632,0.0459862332221396,
-6.92253439370301));
#35694=CARTESIAN_POINT('Ctrl Pts',(0.97368458119012,-0.0795970174180683,
-6.9316386660253));
#35695=CARTESIAN_POINT('Ctrl Pts',(0.926350356148606,-0.306015284960221,
-6.94871216293115));
#35696=CARTESIAN_POINT('Ctrl Pts',(0.883460463339687,-0.426956818832671,
-6.95800192502379));
#35697=CARTESIAN_POINT('Ctrl Pts',(0.729151523474463,-0.650957612728575,
-6.97810108300424));
#35698=CARTESIAN_POINT('Ctrl Pts',(0.637696488394232,-0.740525889266283,
-6.98736958469814));
#35699=CARTESIAN_POINT('Ctrl Pts',(0.426036713628733,-0.880780851615593,
-7.00612069811684));
#35700=CARTESIAN_POINT('Ctrl Pts',(0.307973653875435,-0.928625724149746,
-7.0153627024797));
#35701=CARTESIAN_POINT('Ctrl Pts',(0.0566327757125236,-0.975851063730747,
-7.03424762771179));
#35702=CARTESIAN_POINT('Ctrl Pts',(-0.0734360522994339,-0.974986107295992,
-7.0436601630077));
#35703=CARTESIAN_POINT('Ctrl Pts',(-0.339774824632758,-0.920211144507616,
-7.06375467780277));
#35704=CARTESIAN_POINT('Ctrl Pts',(-0.453231709580488,-0.863674912079865,
-7.07293548116414));
#35705=CARTESIAN_POINT('Ctrl Pts',(-0.647993419123852,-0.732020115088863,
-7.09028669953976));
#35706=CARTESIAN_POINT('Ctrl Pts',(-0.740727065661021,-0.639038876328688,
-7.09979053242116));
#35707=CARTESIAN_POINT('Ctrl Pts',(-0.898957001061358,-0.398243650235556,
-7.12109448578108));
#35708=CARTESIAN_POINT('Ctrl Pts',(-0.933606042652205,-0.27274556957179,
-7.1304803927157));
#35709=CARTESIAN_POINT('Ctrl Pts',(-0.968344848134613,-0.102472440362377,
-7.14330426434533));
#35710=CARTESIAN_POINT('Ctrl Pts',(-0.982847457133258,0.0332679092532401,
-7.15314289473918));
#35711=CARTESIAN_POINT('Ctrl Pts',(-0.926827203591237,0.310593898546053,
-7.1740623188985));
#35712=CARTESIAN_POINT('Ctrl Pts',(-0.879218087597563,0.425655557739472,
-7.18309242763976));
#35713=CARTESIAN_POINT('Ctrl Pts',(-0.754815127384698,0.617628152630065,
-7.19997493944684));
#35714=CARTESIAN_POINT('Ctrl Pts',(-0.671041199110333,0.716229375650086,
-7.20933526646956));
#35715=CARTESIAN_POINT('Ctrl Pts',(-0.445996172083125,0.869771882377502,
-7.22947091986463));
#35716=CARTESIAN_POINT('Ctrl Pts',(-0.329306472663791,0.91993716124174,
-7.23867108510816));
#35717=CARTESIAN_POINT('Ctrl Pts',(-0.114883025917202,0.967572988022602,
-7.25488802848372));
#35718=CARTESIAN_POINT('Ctrl Pts',(0.0143196672288365,0.982708868611547,
-7.26428966900275));
#35719=CARTESIAN_POINT('Ctrl Pts',(0.293766255479787,0.932273626548167,
-7.28526472046171));
#35720=CARTESIAN_POINT('Ctrl Pts',(0.414196553987357,0.885421253450072,
-7.29461745814069));
#35721=CARTESIAN_POINT('Ctrl Pts',(0.628885360373169,0.749556298117646,
-7.31338724295661));
#35722=CARTESIAN_POINT('Ctrl Pts',(0.719279850675252,0.662897645454415,
-7.3224705869374));
#35723=CARTESIAN_POINT('Ctrl Pts',(0.866282680323135,0.45295346680244,-7.34139078328843));
#35724=CARTESIAN_POINT('Ctrl Pts',(0.91946836671907,0.33338785413682,-7.35086023113688));
#35725=CARTESIAN_POINT('Ctrl Pts',(0.978663500387982,0.0671324606298182,
-7.37102368552925));
#35726=CARTESIAN_POINT('Ctrl Pts',(0.973003359148487,-0.0591157425322254,
-7.38017228231881));
#35727=CARTESIAN_POINT('Ctrl Pts',(0.934577081667824,-0.287198233874419,
-7.397241369728));
#35728=CARTESIAN_POINT('Ctrl Pts',(0.888335678485908,-0.410441551965415,
-7.40677048447703));
#35729=CARTESIAN_POINT('Ctrl Pts',(0.75436700942129,-0.621641826545463,
-7.42526436347355));
#35730=CARTESIAN_POINT('Ctrl Pts',(0.669643013392061,-0.71106458673487,
-7.43420364628256));
#35731=CARTESIAN_POINT('Ctrl Pts',(0.488174055667406,-0.843864338148941,
-7.45079782955139));
#35732=CARTESIAN_POINT('Ctrl Pts',(0.373982093359788,-0.90783489720384,
-7.4602570382888));
#35733=CARTESIAN_POINT('Ctrl Pts',(0.107697083087079,-0.971515891430713,
-7.4804981812099));
#35734=CARTESIAN_POINT('Ctrl Pts',(-0.0179410017595397,-0.976779967655474,
-7.48961181332377));
#35735=CARTESIAN_POINT('Ctrl Pts',(-0.247146104311301,-0.943791749784903,
-7.50670439725705));
#35736=CARTESIAN_POINT('Ctrl Pts',(-0.370435197427262,-0.90858688114603,
-7.51598709760512));
#35737=CARTESIAN_POINT('Ctrl Pts',(-0.603765305235316,-0.768696128900332,
-7.53608862225344));
#35738=CARTESIAN_POINT('Ctrl Pts',(-0.699024347697691,-0.682989059985113,
-7.54536607093089));
#35739=CARTESIAN_POINT('Ctrl Pts',(-0.852297046956421,-0.480517879540376,
-7.56412016115156));
#35740=CARTESIAN_POINT('Ctrl Pts',(-0.90736036616704,-0.365762213662909,
-7.57335466543725));
#35741=CARTESIAN_POINT('Ctrl Pts',(-0.97030992135747,-0.118015792472393,
-7.59222919003006));
#35742=CARTESIAN_POINT('Ctrl Pts',(-0.977660521401202,0.0119705014249978,
-7.60164988906344));
#35743=CARTESIAN_POINT('Ctrl Pts',(-0.940049641385491,0.279103247274372,
-7.62158934749669));
#35744=CARTESIAN_POINT('Ctrl Pts',(-0.891989890508622,0.394354383619942,
-7.63064363827625));
#35745=CARTESIAN_POINT('Ctrl Pts',(-0.839252972699874,0.48519873794285,
-7.63839979121393));
#35746=CARTESIAN_POINT('Ctrl Pts',(1.208777386421,-0.3711019484798,-5.750484941282));
#35747=CARTESIAN_POINT('Ctrl Pts',(1.121208538256,-0.6563368922743,-5.767385032474));
#35748=CARTESIAN_POINT('Ctrl Pts',(0.7360341133366,-1.160723111217,-5.801185214858));
#35749=CARTESIAN_POINT('Ctrl Pts',(-0.1957638929852,-1.360594219827,-5.851885488434));
#35750=CARTESIAN_POINT('Ctrl Pts',(-1.033397756381,-0.9063363171557,-5.90258576201));
#35751=CARTESIAN_POINT('Ctrl Pts',(-1.374451970489,-0.01661249151435,-5.953286035586));
#35752=CARTESIAN_POINT('Ctrl Pts',(-1.055001304477,0.8811153498779,-6.003986309162));
#35753=CARTESIAN_POINT('Ctrl Pts',(-0.2285671790938,1.355414045495,-6.054686582738));
#35754=CARTESIAN_POINT('Ctrl Pts',(0.707706293492,1.178364498253,-6.105386856314));
#35755=CARTESIAN_POINT('Ctrl Pts',(1.303888502793,0.4350466939165,-6.15608712989));
#35756=CARTESIAN_POINT('Ctrl Pts',(1.273481817004,-0.5173344629195,-6.206787403466));
#35757=CARTESIAN_POINT('Ctrl Pts',(0.6310982509973,-1.221108466328,-6.257487677042));
#35758=CARTESIAN_POINT('Ctrl Pts',(-0.3145621463059,-1.338073817515,-6.308187950618));
#35759=CARTESIAN_POINT('Ctrl Pts',(-1.109058424281,-0.8120223505811,-6.358888224194));
#35760=CARTESIAN_POINT('Ctrl Pts',(-1.370592161421,0.1042497631482,-6.40958849777));
#35761=CARTESIAN_POINT('Ctrl Pts',(-0.973482255877,0.9704242286569,-6.460288771346));
#35762=CARTESIAN_POINT('Ctrl Pts',(-0.1085614893001,1.370257380614,-6.510989044922));
#35763=CARTESIAN_POINT('Ctrl Pts',(0.8085289429002,1.111607770111,-6.561689318498));
#35764=CARTESIAN_POINT('Ctrl Pts',(1.337077500144,0.3187705204298,-6.612389592074));
#35765=CARTESIAN_POINT('Ctrl Pts',(1.223088021562,-0.6272532005374,-6.66308986565));
#35766=CARTESIAN_POINT('Ctrl Pts',(0.5213386151697,-1.271847842471,-6.713790139226));
#35767=CARTESIAN_POINT('Ctrl Pts',(-0.4309421851917,-1.305250826215,-6.764490412802));
#35768=CARTESIAN_POINT('Ctrl Pts',(-1.176131963658,-0.7114102115302,-6.815190686378));
#35769=CARTESIAN_POINT('Ctrl Pts',(-1.35612674083,0.2243014751538,-6.865890959954));
#35770=CARTESIAN_POINT('Ctrl Pts',(-0.8844292854238,1.052224179464,-6.91659123353));
#35771=CARTESIAN_POINT('Ctrl Pts',(0.01228423889075,1.37449625357,-6.967291507106));
#35772=CARTESIAN_POINT('Ctrl Pts',(0.9030946141339,1.03624862196,-7.017991780682));
#35773=CARTESIAN_POINT('Ctrl Pts',(1.359918853029,0.2000272562895,-7.068692054258));
#35774=CARTESIAN_POINT('Ctrl Pts',(1.163229831491,-0.732317124864,-7.119392327834));
#35775=CARTESIAN_POINT('Ctrl Pts',(0.4075412001447,-1.312746877444,-7.17009260141));
#35776=CARTESIAN_POINT('Ctrl Pts',(-0.5439751789721,-1.262318282903,-7.220792874986));
#35777=CARTESIAN_POINT('Ctrl Pts',(-1.23414863257,-0.6053241161137,-7.271493148562));
#35778=CARTESIAN_POINT('Ctrl Pts',(-1.330998526859,0.3427349973485,-7.322193422138));
#35779=CARTESIAN_POINT('Ctrl Pts',(-0.9697720014561,0.8645397432226,-7.355993604522));
#35780=CARTESIAN_POINT('Ctrl Pts',(-0.725376514264,1.035706685623,-7.372893695714));
#35781=CARTESIAN_POINT('Ctrl Pts',(1.110338582265,-0.3408806418612,-5.80993667391));
#35782=CARTESIAN_POINT('Ctrl Pts',(1.02990104942,-0.6028870018931,-5.826836765102));
#35783=CARTESIAN_POINT('Ctrl Pts',(0.6760939467275,-1.066197687173,-5.860636947486));
#35784=CARTESIAN_POINT('Ctrl Pts',(-0.1798215335905,-1.249791958429,-5.911337221062));
#35785=CARTESIAN_POINT('Ctrl Pts',(-0.9492412851402,-0.8325273063098,-5.962037494638));
#35786=CARTESIAN_POINT('Ctrl Pts',(-1.262521180034,-0.01525962553827,-6.012737768214));
#35787=CARTESIAN_POINT('Ctrl Pts',(-0.9690855122368,0.8093602506011,-6.06343804179));
#35788=CARTESIAN_POINT('Ctrl Pts',(-0.2099534293395,1.24503364024,-6.114138315366));
#35789=CARTESIAN_POINT('Ctrl Pts',(0.6500730501767,1.08240241841,-6.164838588942));
#35790=CARTESIAN_POINT('Ctrl Pts',(1.197704166115,0.3996179402166,-6.215538862518));
#35791=CARTESIAN_POINT('Ctrl Pts',(1.169773699538,-0.475204467396,-6.266239136094));
#35792=CARTESIAN_POINT('Ctrl Pts',(0.5797037114969,-1.121665460096,-6.31693940967));
#35793=CARTESIAN_POINT('Ctrl Pts',(-0.2889452528537,-1.22910554267,-6.367639683246));
#35794=CARTESIAN_POINT('Ctrl Pts',(-1.018740400257,-0.7458939550322,-6.418339956822));
#35795=CARTESIAN_POINT('Ctrl Pts',(-1.25897570096,0.09576000967229,-6.469040230398));
#35796=CARTESIAN_POINT('Ctrl Pts',(-0.8942051034311,0.8913961117622,-6.519740503974));
#35797=CARTESIAN_POINT('Ctrl Pts',(-0.09972060320785,1.258668183588,-6.57044077755));
#35798=CARTESIAN_POINT('Ctrl Pts',(0.742685038837,1.021082135854,-6.621141051126));
#35799=CARTESIAN_POINT('Ctrl Pts',(1.228190362067,0.2928109110062,-6.671841324702));
#35800=CARTESIAN_POINT('Ctrl Pts',(1.123483806945,-0.5761717891393,-6.722541598278));
#35801=CARTESIAN_POINT('Ctrl Pts',(0.4788825348239,-1.168272790448,-6.773241871854));
#35802=CARTESIAN_POINT('Ctrl Pts',(-0.3958476890111,-1.198955546455,-6.82394214543));
#35803=CARTESIAN_POINT('Ctrl Pts',(-1.080351693996,-0.6534753334669,-6.874642419006));
#35804=CARTESIAN_POINT('Ctrl Pts',(-1.245688296041,0.2060351101202,-6.925342692582));
#35805=CARTESIAN_POINT('Ctrl Pts',(-0.8124043102742,0.966534547035,-6.976042966158));
#35806=CARTESIAN_POINT('Ctrl Pts',(0.0112838513918,1.262561856849,-7.026743239734));
#35807=CARTESIAN_POINT('Ctrl Pts',(0.8295495967846,0.9518599857224,-7.07744351331));
#35808=CARTESIAN_POINT('Ctrl Pts',(1.249171591254,0.1837377027876,-7.128143786886));
#35809=CARTESIAN_POINT('Ctrl Pts',(1.068500268498,-0.6726796574155,-7.178844060462));
#35810=CARTESIAN_POINT('Ctrl Pts',(0.3743524022424,-1.20584114424,-7.229544334038));
#35811=CARTESIAN_POINT('Ctrl Pts',(-0.499675652268,-1.15951928647,-7.280244607614));
#35812=CARTESIAN_POINT('Ctrl Pts',(-1.133643678633,-0.5560285363098,-7.33094488119));
#35813=CARTESIAN_POINT('Ctrl Pts',(-1.222606440119,0.3148238007455,-7.381645154766));
#35814=CARTESIAN_POINT('Ctrl Pts',(-0.8907969997721,0.7941345061418,-7.415445337151));
#35815=CARTESIAN_POINT('Ctrl Pts',(-0.666304267025,0.9513621828753,-7.432345428343));
#35816=CARTESIAN_POINT('Ctrl Pts',(1.011899778108,-0.3106593352427,-5.869388406539));
#35817=CARTESIAN_POINT('Ctrl Pts',(0.9385935605836,-0.5494371115119,-5.886288497731));
#35818=CARTESIAN_POINT('Ctrl Pts',(0.6161537801183,-0.9716722631302,-5.920088680115));
#35819=CARTESIAN_POINT('Ctrl Pts',(-0.1638791741958,-1.138989697031,-5.970788953691));
#35820=CARTESIAN_POINT('Ctrl Pts',(-0.8650848138998,-0.7587182954638,-6.021489227267));
#35821=CARTESIAN_POINT('Ctrl Pts',(-1.150590389579,-0.0139067595622,-6.072189500843));
#35822=CARTESIAN_POINT('Ctrl Pts',(-0.8831697199965,0.7376051513243,-6.122889774419));
#35823=CARTESIAN_POINT('Ctrl Pts',(-0.1913396795852,1.134653234986,-6.173590047995));
#35824=CARTESIAN_POINT('Ctrl Pts',(0.5924398068615,0.9864403385659,-6.224290321571));
#35825=CARTESIAN_POINT('Ctrl Pts',(1.091519829436,0.3641891865167,-6.274990595147));
#35826=CARTESIAN_POINT('Ctrl Pts',(1.066065582072,-0.4330744718724,-6.325690868723));
#35827=CARTESIAN_POINT('Ctrl Pts',(0.5283091719965,-1.022222453864,-6.376391142299));
#35828=CARTESIAN_POINT('Ctrl Pts',(-0.2633283594015,-1.120137267826,-6.427091415875));
#35829=CARTESIAN_POINT('Ctrl Pts',(-0.9284223762335,-0.6797655594833,-6.477791689451));
#35830=CARTESIAN_POINT('Ctrl Pts',(-1.1473592405,0.0872702561964,-6.528491963027));
#35831=CARTESIAN_POINT('Ctrl Pts',(-0.8149279509853,0.8123679948675,-6.579192236603));
#35832=CARTESIAN_POINT('Ctrl Pts',(-0.09087971711565,1.147078986561,-6.629892510179));
#35833=CARTESIAN_POINT('Ctrl Pts',(0.6768411347738,0.9305565015973,-6.680592783755));
#35834=CARTESIAN_POINT('Ctrl Pts',(1.119303223991,0.2668513015826,-6.731293057331));
#35835=CARTESIAN_POINT('Ctrl Pts',(1.023879592328,-0.5250903777413,-6.781993330907));
#35836=CARTESIAN_POINT('Ctrl Pts',(0.4364264544781,-1.064697738426,-6.832693604483));
#35837=CARTESIAN_POINT('Ctrl Pts',(-0.3607531928305,-1.092660266695,-6.883393878059));
#35838=CARTESIAN_POINT('Ctrl Pts',(-0.9845714243337,-0.5955404554036,-6.934094151635));
#35839=CARTESIAN_POINT('Ctrl Pts',(-1.135249851252,0.1877687450866,-6.984794425211));
#35840=CARTESIAN_POINT('Ctrl Pts',(-0.7403793351246,0.8808449146057,-7.035494698787));
#35841=CARTESIAN_POINT('Ctrl Pts',(0.01028346389286,1.150627460127,-7.086194972363));
#35842=CARTESIAN_POINT('Ctrl Pts',(0.7560045794353,0.8674713494848,-7.136895245939));
#35843=CARTESIAN_POINT('Ctrl Pts',(1.138424329478,0.1674481492858,-7.187595519515));
#35844=CARTESIAN_POINT('Ctrl Pts',(0.9737707055048,-0.613042189967,-7.238295793091));
#35845=CARTESIAN_POINT('Ctrl Pts',(0.34116360434,-1.098935411036,-7.288996066667));
#35846=CARTESIAN_POINT('Ctrl Pts',(-0.455376125564,-1.056720290038,-7.339696340243));
#35847=CARTESIAN_POINT('Ctrl Pts',(-1.033138724697,-0.5067329565058,-7.390396613819));
#35848=CARTESIAN_POINT('Ctrl Pts',(-1.114214353379,0.2869126041425,-7.441096887395));
#35849=CARTESIAN_POINT('Ctrl Pts',(-0.8118219980882,0.7237292690611,-7.474897069779));
#35850=CARTESIAN_POINT('Ctrl Pts',(-0.607232019786,0.867017680128,-7.491797160971));
#35851=CARTESIAN_POINT('Ctrl Pts',(0.9134609739509,-0.2804380286241,-5.928840139167));
#35852=CARTESIAN_POINT('Ctrl Pts',(0.8472860717472,-0.4959872211307,-5.945740230359));
#35853=CARTESIAN_POINT('Ctrl Pts',(0.5562136135091,-0.8771468390869,-5.979540412743));
#35854=CARTESIAN_POINT('Ctrl Pts',(-0.1479368148011,-1.028187435632,-6.030240686319));
#35855=CARTESIAN_POINT('Ctrl Pts',(-0.7809283426593,-0.6849092846179,-6.080940959895));
#35856=CARTESIAN_POINT('Ctrl Pts',(-1.038659599125,-0.01255389358613,-6.131641233471));
#35857=CARTESIAN_POINT('Ctrl Pts',(-0.7972539277561,0.6658500520475,-6.182341507047));
#35858=CARTESIAN_POINT('Ctrl Pts',(-0.1727259298309,1.024272829731,-6.233041780623));
#35859=CARTESIAN_POINT('Ctrl Pts',(0.5348065635462,0.8904782587224,-6.283742054199));
#35860=CARTESIAN_POINT('Ctrl Pts',(0.9853354927582,0.3287604328168,-6.334442327775));
#35861=CARTESIAN_POINT('Ctrl Pts',(0.962357464606,-0.3909444763488,-6.385142601351));
#35862=CARTESIAN_POINT('Ctrl Pts',(0.4769146324961,-0.9227794476316,-6.435842874927));
#35863=CARTESIAN_POINT('Ctrl Pts',(-0.2377114659494,-1.011168992981,-6.486543148503));
#35864=CARTESIAN_POINT('Ctrl Pts',(-0.8381043522096,-0.6136371639345,-6.537243422079));
#35865=CARTESIAN_POINT('Ctrl Pts',(-1.035742780039,0.07878050272052,-6.587943695655));
#35866=CARTESIAN_POINT('Ctrl Pts',(-0.7356507985394,0.7333398779728,-6.638643969231));
#35867=CARTESIAN_POINT('Ctrl Pts',(-0.08203883102345,1.035489789534,-6.689344242807));
#35868=CARTESIAN_POINT('Ctrl Pts',(0.6109972307107,0.8400308673404,-6.740044516383));
#35869=CARTESIAN_POINT('Ctrl Pts',(1.010416085914,0.240891692159,-6.790744789959));
#35870=CARTESIAN_POINT('Ctrl Pts',(0.9242753777111,-0.4740089663433,-6.841445063535));
#35871=CARTESIAN_POINT('Ctrl Pts',(0.3939703741324,-0.9611226864031,-6.892145337111));
#35872=CARTESIAN_POINT('Ctrl Pts',(-0.3256586966498,-0.9863649869346,-6.942845610687));
#35873=CARTESIAN_POINT('Ctrl Pts',(-0.8887911546714,-0.5376055773403,-6.993545884263));
#35874=CARTESIAN_POINT('Ctrl Pts',(-1.024811406463,0.169502380053,-7.044246157839));
#35875=CARTESIAN_POINT('Ctrl Pts',(-0.668354359975,0.7951552821763,-7.094946431415));
#35876=CARTESIAN_POINT('Ctrl Pts',(0.009283076393917,1.038693063406,-7.145646704991));
#35877=CARTESIAN_POINT('Ctrl Pts',(0.682459562086,0.7830827132473,-7.196346978567));
#35878=CARTESIAN_POINT('Ctrl Pts',(1.027677067702,0.151158595784,-7.247047252143));
#35879=CARTESIAN_POINT('Ctrl Pts',(0.8790411425118,-0.5534047225185,-7.297747525719));
#35880=CARTESIAN_POINT('Ctrl Pts',(0.3079748064376,-0.9920296778312,-7.348447799295));
#35881=CARTESIAN_POINT('Ctrl Pts',(-0.41107659886,-0.9539212936056,-7.399148072871));
#35882=CARTESIAN_POINT('Ctrl Pts',(-0.9326337707599,-0.4574373767019,-7.449848346447));
#35883=CARTESIAN_POINT('Ctrl Pts',(-1.005822266638,0.2590014075395,-7.500548620023));
#35884=CARTESIAN_POINT('Ctrl Pts',(-0.7328469964043,0.6533240319803,-7.534348802407));
#35885=CARTESIAN_POINT('Ctrl Pts',(-0.548159772547,0.7826731773806,-7.551248893599));
#35886=CARTESIAN_POINT('',(0.928054415751644,-0.836414325535831,-5.79040924924187));
#35887=CARTESIAN_POINT('Ctrl Pts',(0.92789124572231,-0.836293509745428,
-5.79007519368924));
#35888=CARTESIAN_POINT('Ctrl Pts',(0.864371518669428,-0.90691332511516,
-5.79556091081753));
#35889=CARTESIAN_POINT('Ctrl Pts',(0.792940913081216,-0.970478590785472,
-5.80103199531844));
#35890=CARTESIAN_POINT('Ctrl Pts',(0.637425660624765,-1.07951704358424,
-5.81183551894919));
#35891=CARTESIAN_POINT('Ctrl Pts',(0.554333481303023,-1.1242195195087,-5.81709774994574));
#35892=CARTESIAN_POINT('Ctrl Pts',(0.316929185470185,-1.21890506887434,
-5.83173271154793));
#35893=CARTESIAN_POINT('Ctrl Pts',(0.155475401581182,-1.24969237459365,
-5.84113306986631));
#35894=CARTESIAN_POINT('Ctrl Pts',(-0.199054089558224,-1.2492012766419,
-5.86150526396104));
#35895=CARTESIAN_POINT('Ctrl Pts',(-0.359646947934741,-1.20454904675112,
-5.87065369581061));
#35896=CARTESIAN_POINT('Ctrl Pts',(-0.632160151649209,-1.08893348546595,
-5.88769715376775));
#35897=CARTESIAN_POINT('Ctrl Pts',(-0.767902086473319,-0.99835874169403,
-5.89701866654246));
#35898=CARTESIAN_POINT('Ctrl Pts',(-0.933329311671832,-0.834622917109364,
-5.91030361631294));
#35899=CARTESIAN_POINT('Ctrl Pts',(-0.980121164363449,-0.779260291825079,
-5.91436218117752));
#35900=CARTESIAN_POINT('Ctrl Pts',(-1.06900391284112,-0.65245114369523,
-5.92316811919274));
#35901=CARTESIAN_POINT('Ctrl Pts',(-1.10928952019647,-0.580596899049868,
-5.92788168288861));
#35902=CARTESIAN_POINT('Ctrl Pts',(-1.20570785544617,-0.361601373980931,
-5.94168728141064));
#35903=CARTESIAN_POINT('Ctrl Pts',(-1.24253207170567,-0.205605311439727,
-5.95083527081061));
#35904=CARTESIAN_POINT('Ctrl Pts',(-1.25221879358022,0.0317429523925532,
-5.964337522886));
#35905=CARTESIAN_POINT('Ctrl Pts',(-1.24750844541546,0.111429598253442,
-5.96880751915366));
#35906=CARTESIAN_POINT('Ctrl Pts',(-1.22216876165356,0.272568462527646,
-5.97813844804283));
#35907=CARTESIAN_POINT('Ctrl Pts',(-1.20099175532748,0.353439666303131,
-5.98293973961609));
#35908=CARTESIAN_POINT('Ctrl Pts',(-1.12195753346685,0.567748349892674,
-5.99613650557584));
#35909=CARTESIAN_POINT('Ctrl Pts',(-1.04444831027652,0.706761633037904,
-6.00518390553283));
#35910=CARTESIAN_POINT('Ctrl Pts',(-0.820493665574736,0.95807855509362,
-6.02421369458117));
#35911=CARTESIAN_POINT('Ctrl Pts',(-0.691465108533078,1.04962810774492,
-6.03319175461902));
#35912=CARTESIAN_POINT('Ctrl Pts',(-0.492229169061597,1.15105288157756,
-6.04610966506214));
#35913=CARTESIAN_POINT('Ctrl Pts',(-0.414398218128557,1.18157328874261,
-6.0509144337977));
#35914=CARTESIAN_POINT('Ctrl Pts',(-0.181971563564285,1.24688313303702,
-6.06474168436814));
#35915=CARTESIAN_POINT('Ctrl Pts',(-0.0251387762637779,1.25994099328009,
-6.0734095518453));
#35916=CARTESIAN_POINT('Ctrl Pts',(0.297440616610082,1.22372522263434,-6.09211825370061));
#35917=CARTESIAN_POINT('Ctrl Pts',(0.455350712066313,1.17475757835444,-6.1015560033069));
#35918=CARTESIAN_POINT('Ctrl Pts',(0.666423373946411,1.06043904118231,-6.11522248205187));
#35919=CARTESIAN_POINT('Ctrl Pts',(0.730710728774875,1.01713258649561,-6.11955696212495));
#35920=CARTESIAN_POINT('Ctrl Pts',(0.914149524679502,0.866358631852595,
-6.13311138351778));
#35921=CARTESIAN_POINT('Ctrl Pts',(1.01793347598042,0.741001899059063,-6.14240830870793));
#35922=CARTESIAN_POINT('Ctrl Pts',(1.16083313914051,0.48240175293223,-6.15941888380699));
#35923=CARTESIAN_POINT('Ctrl Pts',(1.22181971482467,0.327451104671911,-6.16855859432356));
#35924=CARTESIAN_POINT('Ctrl Pts',(1.25904048842782,-0.0245884022575979,
-6.18890019477955));
#35925=CARTESIAN_POINT('Ctrl Pts',(1.24527503627133,-0.187976080808616,
-6.19827840885629));
#35926=CARTESIAN_POINT('Ctrl Pts',(1.17601279473243,-0.433788014109638,
-6.21290291514525));
#35927=CARTESIAN_POINT('Ctrl Pts',(1.14016946501633,-0.521266518177868,
-6.21817569961738));
#35928=CARTESIAN_POINT('Ctrl Pts',(1.04771956613206,-0.687695788509239,
-6.22900408748747));
#35929=CARTESIAN_POINT('Ctrl Pts',(0.99175891804555,-0.765569396789959,
-6.23449075487895));
#35930=CARTESIAN_POINT('Ctrl Pts',(0.927917233057705,-0.836264674901695,
-6.23999215811417));
#35931=CARTESIAN_POINT('',(0.720545177924135,-0.649395441962508,-5.95169174984025));
#35932=CARTESIAN_POINT('Ctrl Pts',(0.720108737182204,-0.649004448460025,
-5.95167596829406));
#35933=CARTESIAN_POINT('Ctrl Pts',(0.649924515094261,-0.727158489828415,
-5.95943212123172));
#35934=CARTESIAN_POINT('Ctrl Pts',(0.555079480957704,-0.808380306989316,
-5.96848641201143));
#35935=CARTESIAN_POINT('Ctrl Pts',(0.312518521341791,-0.926442422296025,
-5.98842587044456));
#35936=CARTESIAN_POINT('Ctrl Pts',(0.186587724758989,-0.959486368703343,
-5.99784656947781));
#35937=CARTESIAN_POINT('Ctrl Pts',(-0.0685031170828884,-0.975905812045911,
-6.01672109407051));
#35938=CARTESIAN_POINT('Ctrl Pts',(-0.194639787589624,-0.958865497291628,
-6.02595559835624));
#35939=CARTESIAN_POINT('Ctrl Pts',(-0.434477044399887,-0.875407786476413,
-6.04470968857699));
#35940=CARTESIAN_POINT('Ctrl Pts',(-0.545358094112484,-0.811178668098817,
-6.05398713725455));
#35941=CARTESIAN_POINT('Ctrl Pts',(-0.750315949779591,-0.632280263483006,
-6.07408866190298));
#35942=CARTESIAN_POINT('Ctrl Pts',(-0.821783629703353,-0.525828612563079,
-6.08337136225105));
#35943=CARTESIAN_POINT('Ctrl Pts',(-0.923765700015957,-0.31792753298714,
-6.10046394618437));
#35944=CARTESIAN_POINT('Ctrl Pts',(-0.957455434114764,-0.196776219833828,
-6.10957757829825));
#35945=CARTESIAN_POINT('Ctrl Pts',(-0.978889084396869,0.0761772090825361,
-6.12981872121936));
#35946=CARTESIAN_POINT('Ctrl Pts',(-0.953200947514869,0.204521107671363,
-6.13927792995675));
#35947=CARTESIAN_POINT('Ctrl Pts',(-0.882751937182649,0.418071320821548,
-6.1558721132256));
#35948=CARTESIAN_POINT('Ctrl Pts',(-0.823772560685341,0.526219453912358,
-6.16481139603458));
#35949=CARTESIAN_POINT('Ctrl Pts',(-0.664104034634087,0.718726913669793,
-6.18330527503119));
#35950=CARTESIAN_POINT('Ctrl Pts',(-0.561095305033117,0.800680464223251,
-6.19283438978037));
#35951=CARTESIAN_POINT('Ctrl Pts',(-0.355937239570725,0.907490434889322,
-6.2099034771897));
#35952=CARTESIAN_POINT('Ctrl Pts',(-0.237570247179744,0.951761205301122,
-6.21905207397936));
#35953=CARTESIAN_POINT('Ctrl Pts',(0.0339733113907507,0.977453504160467,
-6.23921552837171));
#35954=CARTESIAN_POINT('Ctrl Pts',(0.164107751673757,0.963681052608347,
-6.24868497622005));
#35955=CARTESIAN_POINT('Ctrl Pts',(0.409123503410246,0.888490152389854,
-6.26760517257095));
#35956=CARTESIAN_POINT('Ctrl Pts',(0.519411539030041,0.829182183637515,
-6.27668851655165));
#35957=CARTESIAN_POINT('Ctrl Pts',(0.714797598489648,0.66677880484457,-6.29545830136734));
#35958=CARTESIAN_POINT('Ctrl Pts',(0.79646597496151,0.566634519196618,-6.30481103904617));
#35959=CARTESIAN_POINT('Ctrl Pts',(0.930521764899155,0.316308422852269,
-6.32578609050498));
#35960=CARTESIAN_POINT('Ctrl Pts',(0.955917571323838,0.188725180169905,
-6.33518773102405));
#35961=CARTESIAN_POINT('Ctrl Pts',(0.976642397696742,-0.0299459612263604,
-6.35140467439967));
#35962=CARTESIAN_POINT('Ctrl Pts',(0.964857697793128,-0.156413988815745,
-6.36060483964335));
#35963=CARTESIAN_POINT('Ctrl Pts',(0.888096285138152,-0.417810720029647,
-6.38074049303855));
#35964=CARTESIAN_POINT('Ctrl Pts',(0.820092045273143,-0.52788204054506,
-6.39010082006124));
#35965=CARTESIAN_POINT('Ctrl Pts',(0.675770062615433,-0.705366515980325,
-6.4069833318683));
#35966=CARTESIAN_POINT('Ctrl Pts',(0.580966493387205,-0.786101245828095,
-6.4160134406095));
#35967=CARTESIAN_POINT('Ctrl Pts',(0.334378142358139,-0.924817352612478,
-6.43693286476891));
#35968=CARTESIAN_POINT('Ctrl Pts',(0.200770139829639,-0.952829311521942,
-6.44677149516289));
#35969=CARTESIAN_POINT('Ctrl Pts',(0.0280752756794855,-0.972225368674028,
-6.45959536679255));
#35970=CARTESIAN_POINT('Ctrl Pts',(-0.101993726346479,-0.977915627493428,
-6.46898127372728));
#35971=CARTESIAN_POINT('Ctrl Pts',(-0.379818705657778,-0.901545906814717,
-6.49028522708722));
#35972=CARTESIAN_POINT('Ctrl Pts',(-0.496842426704654,-0.841959929657249,
-6.49978905996859));
#35973=CARTESIAN_POINT('Ctrl Pts',(-0.682085252789091,-0.697218075104719,
-6.51714027834417));
#35974=CARTESIAN_POINT('Ctrl Pts',(-0.770818800442323,-0.606690908795065,
-6.52632108170549));
#35975=CARTESIAN_POINT('Ctrl Pts',(-0.904965977547005,-0.370172044703121,
-6.54641559650045));
#35976=CARTESIAN_POINT('Ctrl Pts',(-0.945851484996115,-0.24669320663502,
-6.55582813179624));
#35977=CARTESIAN_POINT('Ctrl Pts',(-0.978337809142478,0.00697411187020937,
-6.57471305702824));
#35978=CARTESIAN_POINT('Ctrl Pts',(-0.969183713860666,0.134034020754438,
-6.58395506139111));
#35979=CARTESIAN_POINT('Ctrl Pts',(-0.900941041069741,0.378603545282184,
-6.60270617480985));
#35980=CARTESIAN_POINT('Ctrl Pts',(-0.8438964554808,0.493200294182236,-6.61197467650383));
#35981=CARTESIAN_POINT('Ctrl Pts',(-0.678314757631588,0.709001837100127,
-6.63207383448436));
#35982=CARTESIAN_POINT('Ctrl Pts',(-0.576463604726434,0.787057843739467,
-6.64136359657699));
#35983=CARTESIAN_POINT('Ctrl Pts',(-0.375632597250357,0.901830084169003,
-6.65843709348284));
#35984=CARTESIAN_POINT('Ctrl Pts',(-0.256987402283611,0.943082682135298,
-6.66754136580511));
#35985=CARTESIAN_POINT('Ctrl Pts',(0.0142369621639232,0.981786888990614,
-6.68779595094908));
#35986=CARTESIAN_POINT('Ctrl Pts',(0.144113504802177,0.964140166216503,
-6.69726706963869));
#35987=CARTESIAN_POINT('Ctrl Pts',(0.361268264905602,0.907471666524346,
-6.71382845843568));
#35988=CARTESIAN_POINT('Ctrl Pts',(0.472813840474943,0.855545430902499,
-6.72275789685528));
#35989=CARTESIAN_POINT('Ctrl Pts',(0.668319496067421,0.713344210924142,
-6.74063401339906));
#35990=CARTESIAN_POINT('Ctrl Pts',(0.752078467845626,0.623215502836167,
-6.7495634518187));
#35991=CARTESIAN_POINT('Ctrl Pts',(0.872877916954441,0.43407269491594,-6.76612484061573));
#35992=CARTESIAN_POINT('Ctrl Pts',(0.929670083339896,0.315945758997087,
-6.7755959593054));
#35993=CARTESIAN_POINT('Ctrl Pts',(0.976387595491632,0.045986233222139,
-6.79585054444934));
#35994=CARTESIAN_POINT('Ctrl Pts',(0.97368458119012,-0.0795970174180682,
-6.80495481677156));
#35995=CARTESIAN_POINT('Ctrl Pts',(0.926350356148606,-0.30601528496022,
-6.82202831367734));
#35996=CARTESIAN_POINT('Ctrl Pts',(0.883460463339688,-0.426956818832668,
-6.8313180757699));
#35997=CARTESIAN_POINT('Ctrl Pts',(0.729151523474468,-0.650957612728569,
-6.85141723375034));
#35998=CARTESIAN_POINT('Ctrl Pts',(0.637696488394238,-0.740525889266277,
-6.8606857354443));
#35999=CARTESIAN_POINT('Ctrl Pts',(0.426036713628743,-0.880780851615588,
-6.87943684886301));
#36000=CARTESIAN_POINT('Ctrl Pts',(0.307973653875445,-0.928625724149743,
-6.88867885322587));
#36001=CARTESIAN_POINT('Ctrl Pts',(0.0566327757125344,-0.975851063730746,
-6.90756377845789));
#36002=CARTESIAN_POINT('Ctrl Pts',(-0.0734360522994191,-0.974986107295992,
-6.91697631375371));
#36003=CARTESIAN_POINT('Ctrl Pts',(-0.339774824632742,-0.920211144507622,
-6.93707082854873));
#36004=CARTESIAN_POINT('Ctrl Pts',(-0.453231709580473,-0.863674912079873,
-6.9462516319101));
#36005=CARTESIAN_POINT('Ctrl Pts',(-0.64799341912384,-0.732020115088874,
-6.96360285028577));
#36006=CARTESIAN_POINT('Ctrl Pts',(-0.74072706566101,-0.6390388763287,-6.97310668316723));
#36007=CARTESIAN_POINT('Ctrl Pts',(-0.89895700106135,-0.398243650235574,
-6.99441063652728));
#36008=CARTESIAN_POINT('Ctrl Pts',(-0.933606042652201,-0.272745569571806,
-7.00379654346201));
#36009=CARTESIAN_POINT('Ctrl Pts',(-0.968344848134609,-0.102472440362395,
-7.01662041509172));
#36010=CARTESIAN_POINT('Ctrl Pts',(-0.982847457133263,0.0332679092532288,
-7.02645904548568));
#36011=CARTESIAN_POINT('Ctrl Pts',(-0.926827203591233,0.310593898546063,
-7.04737846964495));
#36012=CARTESIAN_POINT('Ctrl Pts',(-0.879218087597559,0.425655557739481,
-7.0564085783861));
#36013=CARTESIAN_POINT('Ctrl Pts',(-0.75481512738469,0.617628152630076,
-7.07329109019308));
#36014=CARTESIAN_POINT('Ctrl Pts',(-0.671041199110324,0.716229375650094,
-7.08265141721569));
#36015=CARTESIAN_POINT('Ctrl Pts',(-0.445996172083117,0.869771882377507,
-7.10278707061082));
#36016=CARTESIAN_POINT('Ctrl Pts',(-0.329306472663781,0.919937161241744,
-7.11198723585447));
#36017=CARTESIAN_POINT('Ctrl Pts',(-0.114883025917167,0.967572988022609,
-7.12820417923012));
#36018=CARTESIAN_POINT('Ctrl Pts',(0.0143196672288667,0.982708868611544,
-7.13760581974923));
#36019=CARTESIAN_POINT('Ctrl Pts',(0.293766255479796,0.932273626548164,
-7.15858087120812));
#36020=CARTESIAN_POINT('Ctrl Pts',(0.414196553987364,0.885421253450069,
-7.16793360888701));
#36021=CARTESIAN_POINT('Ctrl Pts',(0.628885360373163,0.749556298117649,
-7.18670339370275));
#36022=CARTESIAN_POINT('Ctrl Pts',(0.719279850675244,0.662897645454425,
-7.19578673768343));
#36023=CARTESIAN_POINT('Ctrl Pts',(0.866282680323126,0.452953466802456,
-7.21470693403423));
#36024=CARTESIAN_POINT('Ctrl Pts',(0.919468366719059,0.333387854136846,
-7.22417638188249));
#36025=CARTESIAN_POINT('Ctrl Pts',(0.978663500387979,0.0671324606298572,
-7.24433983627477));
#36026=CARTESIAN_POINT('Ctrl Pts',(0.973003359148489,-0.0591157425321842,
-7.2534884330644));
#36027=CARTESIAN_POINT('Ctrl Pts',(0.934577081667836,-0.287198233874384,
-7.27055752047376));
#36028=CARTESIAN_POINT('Ctrl Pts',(0.888335678485921,-0.410441551965388,
-7.28008663522298));
#36029=CARTESIAN_POINT('Ctrl Pts',(0.754367009421304,-0.621641826545447,
-7.29858051421967));
#36030=CARTESIAN_POINT('Ctrl Pts',(0.669643013392075,-0.711064586734859,
-7.30751979702871));
#36031=CARTESIAN_POINT('Ctrl Pts',(0.488174055667416,-0.843864338148935,
-7.32411398029761));
#36032=CARTESIAN_POINT('Ctrl Pts',(0.373982093359797,-0.907834897203836,
-7.33357318903505));
#36033=CARTESIAN_POINT('Ctrl Pts',(0.107697083087087,-0.971515891430713,
-7.35381433195615));
#36034=CARTESIAN_POINT('Ctrl Pts',(-0.0179410017595324,-0.976779967655474,
-7.36292796406999));
#36035=CARTESIAN_POINT('Ctrl Pts',(-0.247146104311293,-0.943791749784905,
-7.38002054800323));
#36036=CARTESIAN_POINT('Ctrl Pts',(-0.370435197427253,-0.908586881146033,
-7.38930324835126));
#36037=CARTESIAN_POINT('Ctrl Pts',(-0.603765305235306,-0.76869612890034,
-7.40940477299955));
#36038=CARTESIAN_POINT('Ctrl Pts',(-0.699024347697681,-0.682989059985123,
-7.41868222167699));
#36039=CARTESIAN_POINT('Ctrl Pts',(-0.852297046956413,-0.480517879540391,
-7.43743631189764));
#36040=CARTESIAN_POINT('Ctrl Pts',(-0.907360366167034,-0.365762213662926,
-7.44667081618334));
#36041=CARTESIAN_POINT('Ctrl Pts',(-0.970309921357468,-0.118015792472412,
-7.46554534077611));
#36042=CARTESIAN_POINT('Ctrl Pts',(-0.977660521401202,0.0119705014249765,
-7.47496603980946));
#36043=CARTESIAN_POINT('Ctrl Pts',(-0.940049634066545,0.2791032992575,-7.49490550212285));
#36044=CARTESIAN_POINT('Ctrl Pts',(-0.891989855331675,0.394354468850662,
-7.50395979577473));
#36045=CARTESIAN_POINT('Ctrl Pts',(-0.839252914313109,0.48519883851959,
-7.51171595054694));
#36046=CARTESIAN_POINT('',(0.928537702599,-0.8368498878844,-5.790033670893));
#36047=CARTESIAN_POINT('Ctrl Pts',(-0.8352478720641,0.4641308339706,-4.478818448186));
#36048=CARTESIAN_POINT('Ctrl Pts',(-0.7257270174981,0.6612240973944,-4.495718539378));
#36049=CARTESIAN_POINT('Ctrl Pts',(-0.3618043599731,0.973579871545,-4.529518721762));
#36050=CARTESIAN_POINT('Ctrl Pts',(0.3583616355052,0.9750034062319,-4.580218995338));
#36051=CARTESIAN_POINT('Ctrl Pts',(0.9062041683878,0.5076847542727,-4.630919268914));
#36052=CARTESIAN_POINT('Ctrl Pts',(1.018596427125,-0.203550194661,-4.68161954249));
#36053=CARTESIAN_POINT('Ctrl Pts',(0.6414900337905,-0.8169826520078,-4.732319816066));
#36054=CARTESIAN_POINT('Ctrl Pts',(-0.0438848651729,-1.037806916131,-4.783020089642));
#36055=CARTESIAN_POINT('Ctrl Pts',(-0.7081712873547,-0.759909874548,-4.833720363218));
#36056=CARTESIAN_POINT('Ctrl Pts',(-1.032142960739,-0.1168347725255,-4.884420636794));
#36057=CARTESIAN_POINT('Ctrl Pts',(-0.8601141737781,0.5823856809165,-4.93512091037));
#36058=CARTESIAN_POINT('Ctrl Pts',(-0.2747540081207,1.00173834442,-4.985821183946));
#36059=CARTESIAN_POINT('Ctrl Pts',(0.4426403116802,0.9397015632025,-5.036521457522));
#36060=CARTESIAN_POINT('Ctrl Pts',(0.9473220285466,0.4260873717732,-5.087221731098));
#36061=CARTESIAN_POINT('Ctrl Pts',(0.9967642879194,-0.2922848411075,-5.137922004674));
#36062=CARTESIAN_POINT('Ctrl Pts',(0.5672074110512,-0.8701983836261,-5.18862227825));
#36063=CARTESIAN_POINT('Ctrl Pts',(-0.1349232962637,-1.029934550421,-5.239322551826));
#36064=CARTESIAN_POINT('Ctrl Pts',(-0.7722160642937,-0.694731476232,-5.290022825402));
#36065=CARTESIAN_POINT('Ctrl Pts',(-1.038417259008,-0.02567236295293,-5.340723098978));
#36066=CARTESIAN_POINT('Ctrl Pts',(-0.8056028125943,0.6557237088569,-5.391423372554));
#36067=CARTESIAN_POINT('Ctrl Pts',(-0.1856526550803,1.022009082971,-5.44212364613));
#36068=CARTESIAN_POINT('Ctrl Pts',(0.5235136417157,0.897163831801,-5.492823919706));
#36069=CARTESIAN_POINT('Ctrl Pts',(0.9811033264056,0.3411828488149,-5.543524193282));
#36070=CARTESIAN_POINT('Ctrl Pts',(0.9672198151093,-0.3787549404562,-5.594224466858));
#36071=CARTESIAN_POINT('Ctrl Pts',(0.4885348785918,-0.9166805035943,-5.644924740434));
#36072=CARTESIAN_POINT('Ctrl Pts',(-0.2249174616962,-1.014091510121,-5.69562501401));
#36073=CARTESIAN_POINT('Ctrl Pts',(-0.8302848782164,-0.6241767463422,-5.746325287586));
#36074=CARTESIAN_POINT('Ctrl Pts',(-1.036655225136,0.0656888176107,-5.797025561162));
#36075=CARTESIAN_POINT('Ctrl Pts',(-0.74485777085,0.7239868909991,-5.847725834738));
#36076=CARTESIAN_POINT('Ctrl Pts',(-0.09511182443393,1.034371840274,-5.898426108314));
#36077=CARTESIAN_POINT('Ctrl Pts',(0.6003253513746,0.8476787581516,-5.94912638189));
#36078=CARTESIAN_POINT('Ctrl Pts',(1.007330257735,0.2536542052052,-5.999826655466));
#36079=CARTESIAN_POINT('Ctrl Pts',(0.9300475649187,-0.4623545048573,-6.050526929042));
#36080=CARTESIAN_POINT('Ctrl Pts',(0.5810918409035,-0.7913465001737,-6.084327111426));
#36081=CARTESIAN_POINT('Ctrl Pts',(0.3735576354296,-0.8794948162679,-6.101227202618));
#36082=CARTESIAN_POINT('Ctrl Pts',(-0.9252580684986,0.5141477318691,-4.538270180814));
#36083=CARTESIAN_POINT('Ctrl Pts',(-0.8039347371316,0.7324806822769,-4.555170272006));
#36084=CARTESIAN_POINT('Ctrl Pts',(-0.4007940809903,1.078497367792,-4.58897045439));
#36085=CARTESIAN_POINT('Ctrl Pts',(0.3969803525175,1.080074309199,-4.639670727966));
#36086=CARTESIAN_POINT('Ctrl Pts',(1.003860945417,0.5623952252446,-4.690371001542));
#36087=CARTESIAN_POINT('Ctrl Pts',(1.128365116827,-0.225485710594,-4.741071275118));
#36088=CARTESIAN_POINT('Ctrl Pts',(0.7106199841722,-0.9050245033555,-4.791771548694));
#36089=CARTESIAN_POINT('Ctrl Pts',(-0.04861410240514,-1.1496458175,-4.84247182227));
#36090=CARTESIAN_POINT('Ctrl Pts',(-0.7844871198351,-0.8418012978826,-4.893172095846));
#36091=CARTESIAN_POINT('Ctrl Pts',(-1.143371487925,-0.1294254311517,-4.943872369422));
#36092=CARTESIAN_POINT('Ctrl Pts',(-0.9528040785683,0.6451462712671,-4.994572642998));
#36093=CARTESIAN_POINT('Ctrl Pts',(-0.3043627782466,1.109690328703,-5.045272916574));
#36094=CARTESIAN_POINT('Ctrl Pts',(0.4903412909185,1.040968175334,-5.09597319015));
#36095=CARTESIAN_POINT('Ctrl Pts',(1.049409857475,0.4720045291995,-5.146673463726));
#36096=CARTESIAN_POINT('Ctrl Pts',(1.104180244733,-0.323782815353,-5.197373737302));
#36097=CARTESIAN_POINT('Ctrl Pts',(0.6283323204288,-0.9639750097833,-5.248074010878));
#36098=CARTESIAN_POINT('Ctrl Pts',(-0.1494632583593,-1.140925089037,-5.298774284454));
#36099=CARTESIAN_POINT('Ctrl Pts',(-0.8554336598862,-0.7695989721411,-5.34947455803));
#36100=CARTESIAN_POINT('Ctrl Pts',(-1.150321933764,-0.02843893621772,-5.400174831606));
#36101=CARTESIAN_POINT('Ctrl Pts',(-0.8924183195055,0.7263875462816,-5.450875105182));
#36102=CARTESIAN_POINT('Ctrl Pts',(-0.2056594488852,1.132145536343,-5.501575378758));
#36103=CARTESIAN_POINT('Ctrl Pts',(0.5799299072375,0.9938463801022,-5.552275652334));
#36104=CARTESIAN_POINT('Ctrl Pts',(1.086831585149,0.3779502998543,-5.60297592591));
#36105=CARTESIAN_POINT('Ctrl Pts',(1.071451922086,-0.4195713348838,-5.653676199486));
#36106=CARTESIAN_POINT('Ctrl Pts',(0.5411816698712,-1.015466259243,-5.704376473062));
#36107=CARTESIAN_POINT('Ctrl Pts',(-0.2491556137298,-1.123374729009,-5.755076746638));
#36108=CARTESIAN_POINT('Ctrl Pts',(-0.919760239345,-0.6914409363236,-5.805777020214));
#36109=CARTESIAN_POINT('Ctrl Pts',(-1.148370014925,0.072767750194,-5.85647729379));
#36110=CARTESIAN_POINT('Ctrl Pts',(-0.8251271094647,0.8020070865056,-5.907177567366));
#36111=CARTESIAN_POINT('Ctrl Pts',(-0.1053615171142,1.145840561887,-5.957877840942));
#36112=CARTESIAN_POINT('Ctrl Pts',(0.6650192040728,0.9390285647018,-6.008578114518));
#36113=CARTESIAN_POINT('Ctrl Pts',(1.115884852611,0.2809891624084,-6.059278388094));
#36114=CARTESIAN_POINT('Ctrl Pts',(1.030273817282,-0.5121799772668,-6.10997866167));
#36115=CARTESIAN_POINT('Ctrl Pts',(0.6437130010352,-0.8766256805353,-6.143778844054));
#36116=CARTESIAN_POINT('Ctrl Pts',(0.4138139440886,-0.9742732692555,-6.160678935246));
#36117=CARTESIAN_POINT('Ctrl Pts',(-1.015268264933,0.5641646297676,-4.597721913443));
#36118=CARTESIAN_POINT('Ctrl Pts',(-0.882142456765,0.8037372671594,-4.614622004635));
#36119=CARTESIAN_POINT('Ctrl Pts',(-0.4397838020076,1.183414864038,-4.648422187019));
#36120=CARTESIAN_POINT('Ctrl Pts',(0.4355990695298,1.185145212166,-4.699122460595));
#36121=CARTESIAN_POINT('Ctrl Pts',(1.101517722446,0.6171056962164,-4.749822734171));
#36122=CARTESIAN_POINT('Ctrl Pts',(1.238133806529,-0.2474212265271,-4.800523007747));
#36123=CARTESIAN_POINT('Ctrl Pts',(0.7797499345539,-0.9930663547032,-4.851223281323));
#36124=CARTESIAN_POINT('Ctrl Pts',(-0.05334333963738,-1.261484718868,-4.901923554899));
#36125=CARTESIAN_POINT('Ctrl Pts',(-0.8608029523155,-0.9236927212173,-4.952623828475));
#36126=CARTESIAN_POINT('Ctrl Pts',(-1.254600015111,-0.1420160897778,-5.003324102051));
#36127=CARTESIAN_POINT('Ctrl Pts',(-1.045493983358,0.7079068616178,-5.054024375627));
#36128=CARTESIAN_POINT('Ctrl Pts',(-0.3339715483725,1.217642312985,-5.104724649203));
#36129=CARTESIAN_POINT('Ctrl Pts',(0.5380422701567,1.142234787465,-5.155424922779));
#36130=CARTESIAN_POINT('Ctrl Pts',(1.151497686404,0.5179216866258,-5.206125196355));
#36131=CARTESIAN_POINT('Ctrl Pts',(1.211596201547,-0.3552807895985,-5.256825469931));
#36132=CARTESIAN_POINT('Ctrl Pts',(0.6894572298064,-1.05775163594,-5.307525743507));
#36133=CARTESIAN_POINT('Ctrl Pts',(-0.164003220455,-1.251915627652,-5.358226017083));
#36134=CARTESIAN_POINT('Ctrl Pts',(-0.9386512554787,-0.8444664680501,-5.408926290659));
#36135=CARTESIAN_POINT('Ctrl Pts',(-1.262226608521,-0.03120550948252,-5.459626564235));
#36136=CARTESIAN_POINT('Ctrl Pts',(-0.9792338264167,0.7970513837064,-5.510326837811));
#36137=CARTESIAN_POINT('Ctrl Pts',(-0.2256662426901,1.242281989715,-5.561027111387));
#36138=CARTESIAN_POINT('Ctrl Pts',(0.6363461727594,1.090528928403,-5.611727384963));
#36139=CARTESIAN_POINT('Ctrl Pts',(1.192559843892,0.4147177508937,-5.662427658539));
#36140=CARTESIAN_POINT('Ctrl Pts',(1.175684029063,-0.4603877293114,-5.713127932115));
#36141=CARTESIAN_POINT('Ctrl Pts',(0.5938284611506,-1.114252014892,-5.763828205691));
#36142=CARTESIAN_POINT('Ctrl Pts',(-0.2733937657633,-1.232657947897,-5.814528479267));
#36143=CARTESIAN_POINT('Ctrl Pts',(-1.009235600474,-0.758705126305,-5.865228752843));
#36144=CARTESIAN_POINT('Ctrl Pts',(-1.260084804714,0.0798466827773,-5.915929026419));
#36145=CARTESIAN_POINT('Ctrl Pts',(-0.9053964480795,0.8800272820121,-5.966629299995));
#36146=CARTESIAN_POINT('Ctrl Pts',(-0.1156112097945,1.2573092835,-6.017329573571));
#36147=CARTESIAN_POINT('Ctrl Pts',(0.729713056771,1.030378371252,-6.068029847147));
#36148=CARTESIAN_POINT('Ctrl Pts',(1.224439447487,0.3083241196116,-6.118730120723));
#36149=CARTESIAN_POINT('Ctrl Pts',(1.130500069646,-0.5620054496762,-6.169430394299));
#36150=CARTESIAN_POINT('Ctrl Pts',(0.7063341611668,-0.9619048608968,-6.203230576683));
#36151=CARTESIAN_POINT('Ctrl Pts',(0.4540702527476,-1.069051722243,-6.220130667875));
#36152=CARTESIAN_POINT('Ctrl Pts',(-1.105278461367,0.6141815276661,-4.657173646071));
#36153=CARTESIAN_POINT('Ctrl Pts',(-0.9603501763984,0.8749938520419,-4.674073737263));
#36154=CARTESIAN_POINT('Ctrl Pts',(-0.4787735230248,1.288332360285,-4.707873919647));
#36155=CARTESIAN_POINT('Ctrl Pts',(0.4742177865421,1.290216115133,-4.758574193223));
#36156=CARTESIAN_POINT('Ctrl Pts',(1.199174499476,0.6718161671883,-4.809274466799));
#36157=CARTESIAN_POINT('Ctrl Pts',(1.347902496231,-0.2693567424601,-4.859974740375));
#36158=CARTESIAN_POINT('Ctrl Pts',(0.8488798849356,-1.081108206051,-4.910675013951));
#36159=CARTESIAN_POINT('Ctrl Pts',(-0.05807257686961,-1.373323620236,-4.961375287527));
#36160=CARTESIAN_POINT('Ctrl Pts',(-0.9371187847959,-1.005584144552,-5.012075561103));
#36161=CARTESIAN_POINT('Ctrl Pts',(-1.365828542296,-0.154606748404,-5.062775834679));
#36162=CARTESIAN_POINT('Ctrl Pts',(-1.138183888149,0.7706674519685,-5.113476108255));
#36163=CARTESIAN_POINT('Ctrl Pts',(-0.3635803184984,1.325594297268,-5.164176381831));
#36164=CARTESIAN_POINT('Ctrl Pts',(0.585743249395,1.243501399596,-5.214876655407));
#36165=CARTESIAN_POINT('Ctrl Pts',(1.253585515332,0.563838844052,-5.265576928983));
#36166=CARTESIAN_POINT('Ctrl Pts',(1.319012158361,-0.386778763844,-5.316277202559));
#36167=CARTESIAN_POINT('Ctrl Pts',(0.7505821391841,-1.151528262098,-5.366977476135));
#36168=CARTESIAN_POINT('Ctrl Pts',(-0.1785431825506,-1.362906166268,-5.417677749711));
#36169=CARTESIAN_POINT('Ctrl Pts',(-1.021868851071,-0.9193339639592,-5.468378023287));
#36170=CARTESIAN_POINT('Ctrl Pts',(-1.374131283277,-0.03397208274731,-5.519078296863));
#36171=CARTESIAN_POINT('Ctrl Pts',(-1.066049333328,0.8677152211312,-5.569778570439));
#36172=CARTESIAN_POINT('Ctrl Pts',(-0.245673036495,1.352418443088,-5.620478844015));
#36173=CARTESIAN_POINT('Ctrl Pts',(0.6927624382813,1.187211476704,-5.671179117591));
#36174=CARTESIAN_POINT('Ctrl Pts',(1.298288102635,0.4514852019331,-5.721879391167));
#36175=CARTESIAN_POINT('Ctrl Pts',(1.27991613604,-0.501204123739,-5.772579664743));
#36176=CARTESIAN_POINT('Ctrl Pts',(0.64647525243,-1.213037770542,-5.823279938319));
#36177=CARTESIAN_POINT('Ctrl Pts',(-0.2976319177969,-1.341941166785,-5.873980211895));
#36178=CARTESIAN_POINT('Ctrl Pts',(-1.098710961602,-0.8259693162864,-5.924680485471));
#36179=CARTESIAN_POINT('Ctrl Pts',(-1.371799594503,0.0869256153606,-5.975380759047));
#36180=CARTESIAN_POINT('Ctrl Pts',(-0.9856657866942,0.9580474775185,-6.026081032623));
#36181=CARTESIAN_POINT('Ctrl Pts',(-0.1258609024749,1.368778005114,-6.076781306199));
#36182=CARTESIAN_POINT('Ctrl Pts',(0.7944069094692,1.121728177802,-6.127481579775));
#36183=CARTESIAN_POINT('Ctrl Pts',(1.332994042363,0.3356590768148,-6.178181853351));
#36184=CARTESIAN_POINT('Ctrl Pts',(1.23072632201,-0.6118309220856,-6.228882126927));
#36185=CARTESIAN_POINT('Ctrl Pts',(0.7689553212985,-1.047184041258,-6.262682309311));
#36186=CARTESIAN_POINT('Ctrl Pts',(0.4943265614066,-1.16383017523,-6.279582400503));
#36187=CARTESIAN_POINT('',(-0.733992718634193,1.01100376434735,-4.67964967483772));
#36188=CARTESIAN_POINT('Ctrl Pts',(0.927912398543726,-0.83631111477366,
-5.79009102008202));
#36189=CARTESIAN_POINT('Ctrl Pts',(0.984303033291466,-0.773842119781296,
-5.78531766274095));
#36190=CARTESIAN_POINT('Ctrl Pts',(1.03452888871054,-0.705774985620509,
-5.78052678031108));
#36191=CARTESIAN_POINT('Ctrl Pts',(1.11910171243664,-0.562755852325079,
-5.7709425432084));
#36192=CARTESIAN_POINT('Ctrl Pts',(1.15345589545556,-0.488641509593253,
-5.76615705971969));
#36193=CARTESIAN_POINT('Ctrl Pts',(1.2328253590026,-0.258988426301621,-5.75209196287802));
#36194=CARTESIAN_POINT('Ctrl Pts',(1.25550476406795,-0.0965386012710815,
-5.74304269490003));
#36195=CARTESIAN_POINT('Ctrl Pts',(1.24008869637804,0.217686148614962,-5.72515730558005));
#36196=CARTESIAN_POINT('Ctrl Pts',(1.20565282886093,0.363340832817156,-5.71651231673383));
#36197=CARTESIAN_POINT('Ctrl Pts',(1.11110647759861,0.577496730223301,-5.70304565128118));
#36198=CARTESIAN_POINT('Ctrl Pts',(1.06992642102215,0.650107404166377,-5.69832635750262));
#36199=CARTESIAN_POINT('Ctrl Pts',(0.944063252293379,0.828999426635918,
-5.68592634355134));
#36200=CARTESIAN_POINT('Ctrl Pts',(0.84822354797798,0.927636413561337,-5.67824551246648));
#36201=CARTESIAN_POINT('Ctrl Pts',(0.679323690640051,1.05191055815686,-5.66607914245479));
#36202=CARTESIAN_POINT('Ctrl Pts',(0.616172065736563,1.08999231276497,-5.66177019919714));
#36203=CARTESIAN_POINT('Ctrl Pts',(0.474958779197421,1.15866792269239,-5.65272926901884));
#36204=CARTESIAN_POINT('Ctrl Pts',(0.396590390856506,1.18748335031581,-5.64800681550211));
#36205=CARTESIAN_POINT('Ctrl Pts',(0.184681379976035,1.24274328140347,-5.63559226990401));
#36206=CARTESIAN_POINT('Ctrl Pts',(0.0475448526567326,1.25607405418918,
-5.62790341017278));
#36207=CARTESIAN_POINT('Ctrl Pts',(-0.158747611208275,1.2419016812461,-5.6159160019639));
#36208=CARTESIAN_POINT('Ctrl Pts',(-0.228471459127974,1.23091869803186,
-5.61178760980794));
#36209=CARTESIAN_POINT('Ctrl Pts',(-0.37786010424686,1.19392417930954,-5.60291288201398));
#36210=CARTESIAN_POINT('Ctrl Pts',(-0.456479036779733,1.16581410705845,
-5.5981855228565));
#36211=CARTESIAN_POINT('Ctrl Pts',(-0.656372372773785,1.07153597232633,
-5.58565226936609));
#36212=CARTESIAN_POINT('Ctrl Pts',(-0.771729822950002,0.992397318754269,
-5.57785612991876));
#36213=CARTESIAN_POINT('Ctrl Pts',(-0.918751299420806,0.850173600540487,
-5.56601005253366));
#36214=CARTESIAN_POINT('Ctrl Pts',(-0.962497177798991,0.800278747680704,
-5.56212531860281));
#36215=CARTESIAN_POINT('Ctrl Pts',(-1.09809180565154,0.61740790137033,-5.54896687865545));
#36216=CARTESIAN_POINT('Ctrl Pts',(-1.16861654247585,0.469121166842377,
-5.5399082273327));
#36217=CARTESIAN_POINT('Ctrl Pts',(-1.24801622685103,0.165592839605571,
-5.52205386008585));
#36218=CARTESIAN_POINT('Ctrl Pts',(-1.25875502195331,0.0181262164159631,
-5.51350071541098));
#36219=CARTESIAN_POINT('Ctrl Pts',(-1.23412796614598,-0.212041691723438,
-5.50018362657264));
#36220=CARTESIAN_POINT('Ctrl Pts',(-1.21699110135391,-0.293754636185665,
-5.49546390692046));
#36221=CARTESIAN_POINT('Ctrl Pts',(-1.15170546985013,-0.501892996514001,
-5.48309930106408));
#36222=CARTESIAN_POINT('Ctrl Pts',(-1.09079317412563,-0.624488677481668,
-5.47545453135052));
#36223=CARTESIAN_POINT('Ctrl Pts',(-0.968198663043609,-0.794116403411135,
-5.46331411522335));
#36224=CARTESIAN_POINT('Ctrl Pts',(-0.919561652350412,-0.849819592194169,
-5.4589932792317));
#36225=CARTESIAN_POINT('Ctrl Pts',(-0.80589568154704,-0.958454179706746,
-5.44994066352474));
#36226=CARTESIAN_POINT('Ctrl Pts',(-0.740060554789238,-1.00980945165427,
-5.44521815995594));
#36227=CARTESIAN_POINT('Ctrl Pts',(-0.555034233455757,-1.12715793426829,
-5.43279722929553));
#36228=CARTESIAN_POINT('Ctrl Pts',(-0.428397427015014,-1.1817312067325,
-5.42510206701911));
#36229=CARTESIAN_POINT('Ctrl Pts',(-0.22749238542697,-1.23116591024906,
-5.41310748150614));
#36230=CARTESIAN_POINT('Ctrl Pts',(-0.15772833475297,-1.24196725387437,
-5.40897845163875));
#36231=CARTESIAN_POINT('Ctrl Pts',(-0.00416229030680703,-1.25228372556958,
-5.40010325075728));
#36232=CARTESIAN_POINT('Ctrl Pts',(0.0792836668379041,-1.24948344807876,
-5.3953759861892));
#36233=CARTESIAN_POINT('Ctrl Pts',(0.298384557946442,-1.22064573563774,
-5.38284396242009));
#36234=CARTESIAN_POINT('Ctrl Pts',(0.432359677060051,-1.18045766426295,
-5.37504886840061));
#36235=CARTESIAN_POINT('Ctrl Pts',(0.61574593083661,-1.08984333067015,-5.36320281722287));
#36236=CARTESIAN_POINT('Ctrl Pts',(0.672636691788199,-1.05565545308738,
-5.35931712106376));
#36237=CARTESIAN_POINT('Ctrl Pts',(0.857545353227488,-0.922828082187633,
-5.34615798430428));
#36238=CARTESIAN_POINT('Ctrl Pts',(0.969925654675212,-0.803108263823864,
-5.33709947109674));
#36239=CARTESIAN_POINT('Ctrl Pts',(1.1379918851384,-0.538406840277865,-5.31925596605873));
#36240=CARTESIAN_POINT('Ctrl Pts',(1.19315942434402,-0.401401621351654,
-5.31071209962985));
#36241=CARTESIAN_POINT('Ctrl Pts',(1.25564597191947,-0.0988166122171712,
-5.29293654959551));
#36242=CARTESIAN_POINT('Ctrl Pts',(1.25758497619127,0.0650321485579314,
-5.2839084079254));
#36243=CARTESIAN_POINT('Ctrl Pts',(1.20050647840116,0.384378933204612,-5.26539551259472));
#36244=CARTESIAN_POINT('Ctrl Pts',(1.14101560074235,0.535904535944659,-5.25596917053691));
#36245=CARTESIAN_POINT('Ctrl Pts',(0.965647218495031,0.808142751845912,
-5.23747522437915));
#36246=CARTESIAN_POINT('Ctrl Pts',(0.853232698893263,0.926317530602951,
-5.22848854524482));
#36247=CARTESIAN_POINT('Ctrl Pts',(0.665665056433136,1.06018710828656,-5.21524692817884));
#36248=CARTESIAN_POINT('Ctrl Pts',(0.605133327280159,1.096025339646,-5.21115359580372));
#36249=CARTESIAN_POINT('Ctrl Pts',(0.408216854292134,1.19043053073033,-5.19844162651996));
#36250=CARTESIAN_POINT('Ctrl Pts',(0.263350841531732,1.22982241083698,-5.19008170770061));
#36251=CARTESIAN_POINT('Ctrl Pts',(0.0335648761284514,1.25151546350363,
-5.17699740304561));
#36252=CARTESIAN_POINT('Ctrl Pts',(-0.0500459869614035,1.25124308234069,
-5.17226878091564));
#36253=CARTESIAN_POINT('Ctrl Pts',(-0.208300430875469,1.23477564161633,
-5.16310870515926));
#36254=CARTESIAN_POINT('Ctrl Pts',(-0.282555681669839,1.22002648641904,
-5.15868427269107));
#36255=CARTESIAN_POINT('Ctrl Pts',(-0.478021396008706,1.16165000945984,
-5.1468570784796));
#36256=CARTESIAN_POINT('Ctrl Pts',(-0.594870942271891,1.10574458873467,
-5.13960585708624));
#36257=CARTESIAN_POINT('Ctrl Pts',(-0.769702136393781,0.987344731511731,
-5.12763966246471));
#36258=CARTESIAN_POINT('Ctrl Pts',(-0.834035584823648,0.933969583596118,
-5.1229190306032));
#36259=CARTESIAN_POINT('Ctrl Pts',(-1.00316562863355,0.762421362002899,
-5.10908186946697));
#36260=CARTESIAN_POINT('Ctrl Pts',(-1.08914063838115,0.632938430723606,
-5.10009921704361));
#36261=CARTESIAN_POINT('Ctrl Pts',(-1.2131050151576,0.337887886550823,-5.08189295875165));
#36262=CARTESIAN_POINT('Ctrl Pts',(-1.24730782029891,0.177086377376111,
-5.07282160821827));
#36263=CARTESIAN_POINT('Ctrl Pts',(-1.25074524640195,-0.0525654262503107,
-5.05953660300103));
#36264=CARTESIAN_POINT('Ctrl Pts',(-1.24602919303149,-0.120557140971158,
-5.05554602046806));
#36265=CARTESIAN_POINT('Ctrl Pts',(-1.21508721635405,-0.320625864321934,
-5.04383769939516));
#36266=CARTESIAN_POINT('Ctrl Pts',(-1.1729085372533,-0.449710654044156,
-5.03626377490034));
#36267=CARTESIAN_POINT('Ctrl Pts',(-1.07460800163896,-0.64232073157027,
-5.02400074382649));
#36268=CARTESIAN_POINT('Ctrl Pts',(-1.03012914619204,-0.711980852772414,
-5.0193208046912));
#36269=CARTESIAN_POINT('Ctrl Pts',(-0.933790186201797,-0.834123228088677,
-5.01035222997315));
#36270=CARTESIAN_POINT('Ctrl Pts',(-0.883594995637419,-0.887213249032559,
-5.00607834253427));
#36271=CARTESIAN_POINT('Ctrl Pts',(-0.731433976648951,-1.02139932002522,
-4.99432409243777));
#36272=CARTESIAN_POINT('Ctrl Pts',(-0.62070490816199,-1.09160845194591,
-4.98699183988445));
#36273=CARTESIAN_POINT('Ctrl Pts',(-0.426016127082591,-1.17722388431758,
-4.97493746758731));
#36274=CARTESIAN_POINT('Ctrl Pts',(-0.34657396684484,-1.20328297600705,
-4.97021303498468));
#36275=CARTESIAN_POINT('Ctrl Pts',(-0.115622456347341,-1.25415584664946,
-4.95661561497873));
#36276=CARTESIAN_POINT('Ctrl Pts',(0.0368662084239702,-1.25895993925486,
-4.94779868968955));
#36277=CARTESIAN_POINT('Ctrl Pts',(0.351529427749479,-1.20922475185803,
-4.92967766044937));
#36278=CARTESIAN_POINT('Ctrl Pts',(0.506265466721744,-1.15363052022541,
-4.92060437148523));
#36279=CARTESIAN_POINT('Ctrl Pts',(0.703078291497398,-1.03574785005439,
-4.90733154021851));
#36280=CARTESIAN_POINT('Ctrl Pts',(0.758179953516722,-0.996113189942167,
-4.90335736874744));
#36281=CARTESIAN_POINT('Ctrl Pts',(0.912123771114747,-0.864496136601418,
-4.89164540875892));
#36282=CARTESIAN_POINT('Ctrl Pts',(0.999929842988508,-0.7603863800361,-4.88405121228351));
#36283=CARTESIAN_POINT('Ctrl Pts',(1.11206374453665,-0.575053273671101,
-4.87176636926986));
#36284=CARTESIAN_POINT('Ctrl Pts',(1.14784383137581,-0.500556456462736,
-4.86708591728025));
#36285=CARTESIAN_POINT('Ctrl Pts',(1.20078259690565,-0.354683630615294,
-4.85813714691876));
#36286=CARTESIAN_POINT('Ctrl Pts',(1.21939666046203,-0.284428275635072,
-4.85388508961195));
#36287=CARTESIAN_POINT('Ctrl Pts',(1.25344291010085,-0.0846396456922892,
-4.84214457874379));
#36288=CARTESIAN_POINT('Ctrl Pts',(1.25488801214753,0.0466453714559938,
-4.83480351565871));
#36289=CARTESIAN_POINT('Ctrl Pts',(1.22518787451642,0.257424044102171,-4.82273908138619));
#36290=CARTESIAN_POINT('Ctrl Pts',(1.20553022119135,0.338691454838772,-4.818014011537));
#36291=CARTESIAN_POINT('Ctrl Pts',(1.12765509076486,0.560590428986372,-4.80449001523444));
#36292=CARTESIAN_POINT('Ctrl Pts',(1.05233406416851,0.691764352615165,-4.79574497940039));
#36293=CARTESIAN_POINT('Ctrl Pts',(0.845984873630827,0.932814566662742,
-4.77769025112686));
#36294=CARTESIAN_POINT('Ctrl Pts',(0.717528423108332,1.03553798967812,-4.76861321402929));
#36295=CARTESIAN_POINT('Ctrl Pts',(0.512820905109634,1.14205854283913,-4.75526850807405));
#36296=CARTESIAN_POINT('Ctrl Pts',(0.448974984218303,1.168624308156,-4.75122133408201));
#36297=CARTESIAN_POINT('Ctrl Pts',(0.255819218906257,1.23026373995105,-4.73950657944032));
#36298=CARTESIAN_POINT('Ctrl Pts',(0.122213546647829,1.25010859997572,-4.73197931948863));
#36299=CARTESIAN_POINT('Ctrl Pts',(-0.138351662392057,1.24808378903057,
-4.7172051080251));
#36300=CARTESIAN_POINT('Ctrl Pts',(-0.265779189758412,1.2280555759047,-4.70990241740329));
#36301=CARTESIAN_POINT('Ctrl Pts',(-0.511890143544524,1.147781009971,-4.69478191057141));
#36302=CARTESIAN_POINT('Ctrl Pts',(-0.628863836674227,1.08723957239584,
-4.68733470794919));
#36303=CARTESIAN_POINT('Ctrl Pts',(-0.733904641412792,1.01085195669132,
-4.6799679321611));
#36304=CARTESIAN_POINT('',(-0.569874894399988,0.784947385849281,-4.51836716849296));
#36305=CARTESIAN_POINT('',(-0.5698749570781,0.784947471679,-4.518367177796));
#36306=CARTESIAN_POINT('Ctrl Pts',(-0.569529321306653,0.784474167360507,
-4.51835139123805));
#36307=CARTESIAN_POINT('Ctrl Pts',(-0.484636911634744,0.846338237939427,
-4.52610754601023));
#36308=CARTESIAN_POINT('Ctrl Pts',(-0.37498449428145,0.906078691512917,
-4.53516183966203));
#36309=CARTESIAN_POINT('Ctrl Pts',(-0.11318517611704,0.971160390418818,
-4.5551013019754));
#36310=CARTESIAN_POINT('Ctrl Pts',(0.0168632307072555,0.977315047570584,
-4.56452200100877));
#36311=CARTESIAN_POINT('Ctrl Pts',(0.269797863995055,0.940369046501477,
-4.58339652560156));
#36312=CARTESIAN_POINT('Ctrl Pts',(0.389640305530924,0.897489900285439,
-4.59263102988726));
#36313=CARTESIAN_POINT('Ctrl Pts',(0.606900163119466,0.766016505526524,
-4.61138512010795));
#36314=CARTESIAN_POINT('Ctrl Pts',(0.702014304273948,0.680148659476006,
-4.6206625687854));
#36315=CARTESIAN_POINT('Ctrl Pts',(0.865323843694871,0.462565672761053,
-4.64076409343374));
#36316=CARTESIAN_POINT('Ctrl Pts',(0.913111224941757,0.343586895448389,
-4.65004679378182));
#36317=CARTESIAN_POINT('Ctrl Pts',(0.969666070452139,0.119032334142445,
-4.6671393777151));
#36318=CARTESIAN_POINT('Ctrl Pts',(0.977445580061419,-0.00647510823700896,
-4.67625300982894));
#36319=CARTESIAN_POINT('Ctrl Pts',(0.941692548896792,-0.277924360370873,
-4.69649415275001));
#36320=CARTESIAN_POINT('Ctrl Pts',(0.889895690185106,-0.398128861572077,
-4.7059533614874));
#36321=CARTESIAN_POINT('Ctrl Pts',(0.776609403954005,-0.592378633632003,
-4.72254754475627));
#36322=CARTESIAN_POINT('Ctrl Pts',(0.696444599699847,-0.685910391350884,
-4.73148682756529));
#36323=CARTESIAN_POINT('Ctrl Pts',(0.500258893832878,-0.841037207495618,
-4.74998070656194));
#36324=CARTESIAN_POINT('Ctrl Pts',(0.382468956290842,-0.89979700188057,
-4.75950982131112));
#36325=CARTESIAN_POINT('Ctrl Pts',(0.1595943127922,-0.961644353830413,-4.77657890872045));
#36326=CARTESIAN_POINT('Ctrl Pts',(0.0346117104224662,-0.980352509949183,
-4.78572750551008));
#36327=CARTESIAN_POINT('Ctrl Pts',(-0.236343379195985,-0.949058136150452,
-4.80589095990238));
#36328=CARTESIAN_POINT('Ctrl Pts',(-0.360775378580037,-0.908544798855134,
-4.81536040775067));
#36329=CARTESIAN_POINT('Ctrl Pts',(-0.584818511226714,-0.784081692722731,
-4.8342806041015));
#36330=CARTESIAN_POINT('Ctrl Pts',(-0.680375181353441,-0.703150803980066,
-4.8433639480822));
#36331=CARTESIAN_POINT('Ctrl Pts',(-0.837749469773749,-0.503691778064571,
-4.862133732898));
#36332=CARTESIAN_POINT('Ctrl Pts',(-0.896825536918335,-0.388763017720261,
-4.87148647057693));
#36333=CARTESIAN_POINT('Ctrl Pts',(-0.975938218374797,-0.116044677743486,
-4.89246152203582));
#36334=CARTESIAN_POINT('Ctrl Pts',(-0.974268306023393,0.0140308472029995,
-4.9018631625549));
#36335=CARTESIAN_POINT('Ctrl Pts',(-0.949101604663953,0.232235392643118,
-4.91808010593055));
#36336=CARTESIAN_POINT('Ctrl Pts',(-0.911294498982234,0.353494057958645,
-4.92728027117415));
#36337=CARTESIAN_POINT('Ctrl Pts',(-0.781891247636173,0.593234259224568,
-4.9474159245693));
#36338=CARTESIAN_POINT('Ctrl Pts',(-0.692498942409303,0.686771888047523,
-4.95677625159203));
#36339=CARTESIAN_POINT('Ctrl Pts',(-0.514446522986004,0.830392602557005,
-4.97365876339911));
#36340=CARTESIAN_POINT('Ctrl Pts',(-0.404935910777075,0.889665186064197,
-4.98268887214038));
#36341=CARTESIAN_POINT('Ctrl Pts',(-0.134905330150612,0.974113150346353,
-5.00360829629978));
#36342=CARTESIAN_POINT('Ctrl Pts',(0.00160707428446136,0.973750359822927,
-5.01344692669361));
#36343=CARTESIAN_POINT('Ctrl Pts',(0.17456279736015,0.956837613378721,-5.02627079832319));
#36344=CARTESIAN_POINT('Ctrl Pts',(0.302975074330211,0.935375752863385,
-5.03565670525779));
#36345=CARTESIAN_POINT('Ctrl Pts',(0.558866320705606,0.80294190751462,-5.05696065861763));
#36346=CARTESIAN_POINT('Ctrl Pts',(0.660953880687902,0.720339425358643,
-5.06646449149907));
#36347=CARTESIAN_POINT('Ctrl Pts',(0.812076348801616,0.540264139141331,
-5.08381570987471));
#36348=CARTESIAN_POINT('Ctrl Pts',(0.880061774681646,0.433274456521516,
-5.09299651323606));
#36349=CARTESIAN_POINT('Ctrl Pts',(0.962132946141087,0.174042975000017,
-5.11309102803108));
#36350=CARTESIAN_POINT('Ctrl Pts',(0.976467507927318,0.0447635547179919,
-5.12250356332691));
#36351=CARTESIAN_POINT('Ctrl Pts',(0.955533483765514,-0.210117273055868,
-5.14138848855896));
#36352=CARTESIAN_POINT('Ctrl Pts',(0.920176570954098,-0.332501531122724,
-5.15063049292185));
#36353=CARTESIAN_POINT('Ctrl Pts',(0.802602751105272,-0.557551995693596,
-5.1693816063406));
#36354=CARTESIAN_POINT('Ctrl Pts',(0.72299050396223,-0.657793652245647,
-5.17865010803458));
#36355=CARTESIAN_POINT('Ctrl Pts',(0.516180264657057,-0.834477351286836,
-5.19874926601507));
#36356=CARTESIAN_POINT('Ctrl Pts',(0.400332533119837,-0.889665217872399,
-5.20803902810765));
#36357=CARTESIAN_POINT('Ctrl Pts',(0.180035963144122,-0.960200187879757,
-5.22511252501343));
#36358=CARTESIAN_POINT('Ctrl Pts',(0.0554083971430044,-0.975898242544961,
-5.23421679733565));
#36359=CARTESIAN_POINT('Ctrl Pts',(-0.217938297569029,-0.957398080705504,
-5.25447138247956));
#36360=CARTESIAN_POINT('Ctrl Pts',(-0.341312967821625,-0.913148629947773,
-5.2639425011692));
#36361=CARTESIAN_POINT('Ctrl Pts',(-0.541952151862903,-0.81259304074293,
-5.28050388996625));
#36362=CARTESIAN_POINT('Ctrl Pts',(-0.640272812359039,-0.738621444203258,
-5.2894333283859));
#36363=CARTESIAN_POINT('Ctrl Pts',(-0.801962028794448,-0.558898753313217,
-5.30730944492977));
#36364=CARTESIAN_POINT('Ctrl Pts',(-0.865164262002853,-0.453332531951947,
-5.31623888334945));
#36365=CARTESIAN_POINT('Ctrl Pts',(-0.94402364854212,-0.24321659764972,
-5.33280027214652));
#36366=CARTESIAN_POINT('Ctrl Pts',(-0.975029766934588,-0.115866906741197,
-5.34227139083619));
#36367=CARTESIAN_POINT('Ctrl Pts',(-0.964630825541228,0.157907696748253,
-5.36252597598007));
#36368=CARTESIAN_POINT('Ctrl Pts',(-0.935891024457683,0.280188042516797,
-5.37163024830224));
#36369=CARTESIAN_POINT('Ctrl Pts',(-0.842541035141802,0.491828162134418,
-5.38870374520798));
#36370=CARTESIAN_POINT('Ctrl Pts',(-0.775456087044577,0.601217408678344,
-5.39799350730056));
#36371=CARTESIAN_POINT('Ctrl Pts',(-0.577968766812459,0.788263827879977,
-5.41809266528101));
#36372=CARTESIAN_POINT('Ctrl Pts',(-0.469898014985202,0.856872954117074,
-5.42736116697496));
#36373=CARTESIAN_POINT('Ctrl Pts',(-0.233713821582721,0.950084227599802,
-5.44611228039366));
#36374=CARTESIAN_POINT('Ctrl Pts',(-0.108285830905306,0.972351626655509,
-5.45535428475652));
#36375=CARTESIAN_POINT('Ctrl Pts',(0.147382057119426,0.966318321832296,
-5.47423920998856));
#36376=CARTESIAN_POINT('Ctrl Pts',(0.274432011617768,0.938444369260617,
-5.48365174528442));
#36377=CARTESIAN_POINT('Ctrl Pts',(0.523575091539715,0.829520708270321,
-5.50374626007947));
#36378=CARTESIAN_POINT('Ctrl Pts',(0.622807399176721,0.750642577966373,
-5.51292706344084));
#36379=CARTESIAN_POINT('Ctrl Pts',(0.785960420543068,0.581390692617458,
-5.5302782818165));
#36380=CARTESIAN_POINT('Ctrl Pts',(0.857348683054851,0.471169297520886,
-5.53978211469793));
#36381=CARTESIAN_POINT('Ctrl Pts',(0.962088321082959,0.202750480014222,
-5.56108606805791));
#36382=CARTESIAN_POINT('Ctrl Pts',(0.969902954400321,0.0727918102781827,
-5.57047197499261));
#36383=CARTESIAN_POINT('Ctrl Pts',(0.968501283832613,-0.100983212255705,
-5.58329584662227));
#36384=CARTESIAN_POINT('Ctrl Pts',(0.954480930335872,-0.236774220313617,
-5.59313447701619));
#36385=CARTESIAN_POINT('Ctrl Pts',(0.842056053068111,-0.496405921220234,
-5.6140539011755));
#36386=CARTESIAN_POINT('Ctrl Pts',(0.771576711542555,-0.599062999690933,
-5.62308400991669));
#36387=CARTESIAN_POINT('Ctrl Pts',(0.609997938988816,-0.760994695040378,
-5.63996652172369));
#36388=CARTESIAN_POINT('Ctrl Pts',(0.507563614314365,-0.840035705712443,
-5.64932684874635));
#36389=CARTESIAN_POINT('Ctrl Pts',(0.255525233332945,-0.943463071888587,
-5.66946250214136));
#36390=CARTESIAN_POINT('Ctrl Pts',(0.130958452487746,-0.968285607294544,
-5.67866266738487));
#36391=CARTESIAN_POINT('Ctrl Pts',(-0.0886831345802765,-0.970325150882858,
-5.69487961076042));
#36392=CARTESIAN_POINT('Ctrl Pts',(-0.218210781695994,-0.95828274954155,
-5.70428125127945));
#36393=CARTESIAN_POINT('Ctrl Pts',(-0.481077340281045,-0.850880320776053,
-5.72525630273845));
#36394=CARTESIAN_POINT('Ctrl Pts',(-0.589143120265961,-0.780025618322459,
-5.73460904041748));
#36395=CARTESIAN_POINT('Ctrl Pts',(-0.770913413302387,-0.602514688393457,
-5.75337882523339));
#36396=CARTESIAN_POINT('Ctrl Pts',(-0.841327391289039,-0.498963939181004,
-5.76246216921414));
#36397=CARTESIAN_POINT('Ctrl Pts',(-0.941495735081668,-0.263055709192838,
-5.78138236556507));
#36398=CARTESIAN_POINT('Ctrl Pts',(-0.968675143304467,-0.135048159656995,
-5.79085181341341));
#36399=CARTESIAN_POINT('Ctrl Pts',(-0.971251168838686,0.137695974128068,
-5.81101526780577));
#36400=CARTESIAN_POINT('Ctrl Pts',(-0.939480613937675,0.260012276564834,
-5.82016386459539));
#36401=CARTESIAN_POINT('Ctrl Pts',(-0.854498309521635,0.475131335678766,
-5.83723295200468));
#36402=CARTESIAN_POINT('Ctrl Pts',(-0.783656704497048,0.586075690288896,
-5.84676206675381));
#36403=CARTESIAN_POINT('Ctrl Pts',(-0.608725574238593,0.76482764115973,
-5.86525594575038));
#36404=CARTESIAN_POINT('Ctrl Pts',(-0.5072691743685,0.834693115239862,-5.87419522855934));
#36405=CARTESIAN_POINT('Ctrl Pts',(-0.302165962186486,0.926885462785104,
-5.89078941182814));
#36406=CARTESIAN_POINT('Ctrl Pts',(-0.177173705923729,0.965730958737603,
-5.90024862056551));
#36407=CARTESIAN_POINT('Ctrl Pts',(0.0965315452820945,0.97268877333576,
-5.9204897634866));
#36408=CARTESIAN_POINT('Ctrl Pts',(0.220521063650604,0.951730763001616,
-5.9296033956005));
#36409=CARTESIAN_POINT('Ctrl Pts',(0.437868240623847,0.871834541464922,
-5.94669597953381));
#36410=CARTESIAN_POINT('Ctrl Pts',(0.551150726807566,0.811779053944625,
-5.95597867988191));
#36411=CARTESIAN_POINT('Ctrl Pts',(0.750318872098352,0.626456600703946,
-5.97608020453024));
#36412=CARTESIAN_POINT('Ctrl Pts',(0.825688954935265,0.52282582609488,-5.98535765320768));
#36413=CARTESIAN_POINT('Ctrl Pts',(0.93354317436394,0.292924615571315,-6.00411174342834));
#36414=CARTESIAN_POINT('Ctrl Pts',(0.963558721675803,0.169231855504197,
-6.01334624771403));
#36415=CARTESIAN_POINT('Ctrl Pts',(0.973653321148666,-0.0861874757391061,
-6.03222077230681));
#36416=CARTESIAN_POINT('Ctrl Pts',(0.953832746458542,-0.214863863398643,
-6.04164147134018));
#36417=CARTESIAN_POINT('Ctrl Pts',(0.861533526071293,-0.46835022618067,
-6.06158092977344));
#36418=CARTESIAN_POINT('Ctrl Pts',(0.79057401337535,-0.571099005449627,
-6.07063522055322));
#36419=CARTESIAN_POINT('Ctrl Pts',(0.720111076156533,-0.649001853220507,
-6.07839137349091));
#36420=CARTESIAN_POINT('Ctrl Pts',(-1.105278461367,0.6141815276661,-4.190476523559));
#36421=CARTESIAN_POINT('Ctrl Pts',(-0.9603501763984,0.8749938520419,-4.207376614751));
#36422=CARTESIAN_POINT('Ctrl Pts',(-0.4787735230248,1.288332360285,-4.241176797135));
#36423=CARTESIAN_POINT('Ctrl Pts',(0.4742177865421,1.290216115133,-4.291877070711));
#36424=CARTESIAN_POINT('Ctrl Pts',(1.199174499476,0.6718161671883,-4.342577344287));
#36425=CARTESIAN_POINT('Ctrl Pts',(1.347902496231,-0.2693567424601,-4.393277617863));
#36426=CARTESIAN_POINT('Ctrl Pts',(0.8488798849356,-1.081108206051,-4.443977891439));
#36427=CARTESIAN_POINT('Ctrl Pts',(-0.05807257686962,-1.373323620236,-4.494678165015));
#36428=CARTESIAN_POINT('Ctrl Pts',(-0.9371187847959,-1.005584144552,-4.545378438591));
#36429=CARTESIAN_POINT('Ctrl Pts',(-1.365828542296,-0.154606748404,-4.596078712167));
#36430=CARTESIAN_POINT('Ctrl Pts',(-1.138183888149,0.7706674519685,-4.646778985743));
#36431=CARTESIAN_POINT('Ctrl Pts',(-0.3635803184984,1.325594297268,-4.697479259319));
#36432=CARTESIAN_POINT('Ctrl Pts',(0.585743249395,1.243501399596,-4.748179532895));
#36433=CARTESIAN_POINT('Ctrl Pts',(1.253585515332,0.563838844052,-4.798879806471));
#36434=CARTESIAN_POINT('Ctrl Pts',(1.319012158361,-0.386778763844,-4.849580080047));
#36435=CARTESIAN_POINT('Ctrl Pts',(0.7505821391841,-1.151528262098,-4.900280353623));
#36436=CARTESIAN_POINT('Ctrl Pts',(-0.1785431825506,-1.362906166268,-4.950980627199));
#36437=CARTESIAN_POINT('Ctrl Pts',(-1.021868851071,-0.9193339639592,-5.001680900775));
#36438=CARTESIAN_POINT('Ctrl Pts',(-1.374131283277,-0.03397208274731,-5.052381174351));
#36439=CARTESIAN_POINT('Ctrl Pts',(-1.066049333328,0.8677152211312,-5.103081447927));
#36440=CARTESIAN_POINT('Ctrl Pts',(-0.245673036495,1.352418443088,-5.153781721503));
#36441=CARTESIAN_POINT('Ctrl Pts',(0.6927624382813,1.187211476704,-5.204481995079));
#36442=CARTESIAN_POINT('Ctrl Pts',(1.298288102635,0.4514852019331,-5.255182268655));
#36443=CARTESIAN_POINT('Ctrl Pts',(1.27991613604,-0.501204123739,-5.305882542231));
#36444=CARTESIAN_POINT('Ctrl Pts',(0.64647525243,-1.213037770542,-5.356582815807));
#36445=CARTESIAN_POINT('Ctrl Pts',(-0.2976319177969,-1.341941166785,-5.407283089383));
#36446=CARTESIAN_POINT('Ctrl Pts',(-1.098710961602,-0.8259693162864,-5.457983362959));
#36447=CARTESIAN_POINT('Ctrl Pts',(-1.371799594503,0.08692561536059,-5.508683636535));
#36448=CARTESIAN_POINT('Ctrl Pts',(-0.9856657866942,0.9580474775185,-5.559383910111));
#36449=CARTESIAN_POINT('Ctrl Pts',(-0.1258609024748,1.368778005114,-5.610084183687));
#36450=CARTESIAN_POINT('Ctrl Pts',(0.7944069094692,1.121728177802,-5.660784457263));
#36451=CARTESIAN_POINT('Ctrl Pts',(1.332994042363,0.3356590768148,-5.711484730839));
#36452=CARTESIAN_POINT('Ctrl Pts',(1.23072632201,-0.6118309220856,-5.762185004415));
#36453=CARTESIAN_POINT('Ctrl Pts',(0.7689553212985,-1.047184041258,-5.795985186799));
#36454=CARTESIAN_POINT('Ctrl Pts',(0.4943265614066,-1.16383017523,-5.812885277991));
#36455=CARTESIAN_POINT('Ctrl Pts',(-1.015268264933,0.5641646297676,-4.249928256187));
#36456=CARTESIAN_POINT('Ctrl Pts',(-0.882142456765,0.8037372671594,-4.266828347379));
#36457=CARTESIAN_POINT('Ctrl Pts',(-0.4397838020076,1.183414864038,-4.300628529763));
#36458=CARTESIAN_POINT('Ctrl Pts',(0.4355990695298,1.185145212166,-4.351328803339));
#36459=CARTESIAN_POINT('Ctrl Pts',(1.101517722446,0.6171056962164,-4.402029076915));
#36460=CARTESIAN_POINT('Ctrl Pts',(1.238133806529,-0.2474212265271,-4.452729350491));
#36461=CARTESIAN_POINT('Ctrl Pts',(0.7797499345539,-0.9930663547032,-4.503429624067));
#36462=CARTESIAN_POINT('Ctrl Pts',(-0.05334333963738,-1.261484718868,-4.554129897643));
#36463=CARTESIAN_POINT('Ctrl Pts',(-0.8608029523155,-0.9236927212173,-4.604830171219));
#36464=CARTESIAN_POINT('Ctrl Pts',(-1.254600015111,-0.1420160897778,-4.655530444795));
#36465=CARTESIAN_POINT('Ctrl Pts',(-1.045493983358,0.7079068616178,-4.706230718371));
#36466=CARTESIAN_POINT('Ctrl Pts',(-0.3339715483725,1.217642312985,-4.756930991947));
#36467=CARTESIAN_POINT('Ctrl Pts',(0.5380422701567,1.142234787465,-4.807631265523));
#36468=CARTESIAN_POINT('Ctrl Pts',(1.151497686404,0.5179216866258,-4.858331539099));
#36469=CARTESIAN_POINT('Ctrl Pts',(1.211596201547,-0.3552807895985,-4.909031812675));
#36470=CARTESIAN_POINT('Ctrl Pts',(0.6894572298064,-1.05775163594,-4.959732086251));
#36471=CARTESIAN_POINT('Ctrl Pts',(-0.164003220455,-1.251915627652,-5.010432359827));
#36472=CARTESIAN_POINT('Ctrl Pts',(-0.9386512554787,-0.8444664680501,-5.061132633403));
#36473=CARTESIAN_POINT('Ctrl Pts',(-1.262226608521,-0.03120550948252,-5.111832906979));
#36474=CARTESIAN_POINT('Ctrl Pts',(-0.9792338264167,0.7970513837064,-5.162533180555));
#36475=CARTESIAN_POINT('Ctrl Pts',(-0.2256662426901,1.242281989715,-5.213233454131));
#36476=CARTESIAN_POINT('Ctrl Pts',(0.6363461727594,1.090528928403,-5.263933727707));
#36477=CARTESIAN_POINT('Ctrl Pts',(1.192559843892,0.4147177508937,-5.314634001283));
#36478=CARTESIAN_POINT('Ctrl Pts',(1.175684029063,-0.4603877293114,-5.365334274859));
#36479=CARTESIAN_POINT('Ctrl Pts',(0.5938284611506,-1.114252014892,-5.416034548435));
#36480=CARTESIAN_POINT('Ctrl Pts',(-0.2733937657633,-1.232657947897,-5.466734822011));
#36481=CARTESIAN_POINT('Ctrl Pts',(-1.009235600474,-0.758705126305,-5.517435095587));
#36482=CARTESIAN_POINT('Ctrl Pts',(-1.260084804714,0.07984668277729,-5.568135369163));
#36483=CARTESIAN_POINT('Ctrl Pts',(-0.9053964480795,0.8800272820121,-5.618835642739));
#36484=CARTESIAN_POINT('Ctrl Pts',(-0.1156112097945,1.2573092835,-5.669535916315));
#36485=CARTESIAN_POINT('Ctrl Pts',(0.729713056771,1.030378371252,-5.720236189891));
#36486=CARTESIAN_POINT('Ctrl Pts',(1.224439447487,0.3083241196116,-5.770936463467));
#36487=CARTESIAN_POINT('Ctrl Pts',(1.130500069646,-0.5620054496762,-5.821636737043));
#36488=CARTESIAN_POINT('Ctrl Pts',(0.7063341611668,-0.9619048608968,-5.855436919427));
#36489=CARTESIAN_POINT('Ctrl Pts',(0.4540702527476,-1.069051722243,-5.872337010619));
#36490=CARTESIAN_POINT('Ctrl Pts',(-0.9252580684986,0.5141477318691,-4.309379988816));
#36491=CARTESIAN_POINT('Ctrl Pts',(-0.8039347371316,0.7324806822769,-4.326280080008));
#36492=CARTESIAN_POINT('Ctrl Pts',(-0.4007940809904,1.078497367792,-4.360080262392));
#36493=CARTESIAN_POINT('Ctrl Pts',(0.3969803525175,1.080074309199,-4.410780535968));
#36494=CARTESIAN_POINT('Ctrl Pts',(1.003860945417,0.5623952252446,-4.461480809544));
#36495=CARTESIAN_POINT('Ctrl Pts',(1.128365116827,-0.225485710594,-4.51218108312));
#36496=CARTESIAN_POINT('Ctrl Pts',(0.7106199841722,-0.9050245033555,-4.562881356696));
#36497=CARTESIAN_POINT('Ctrl Pts',(-0.04861410240515,-1.1496458175,-4.613581630272));
#36498=CARTESIAN_POINT('Ctrl Pts',(-0.7844871198351,-0.8418012978826,-4.664281903848));
#36499=CARTESIAN_POINT('Ctrl Pts',(-1.143371487925,-0.1294254311517,-4.714982177424));
#36500=CARTESIAN_POINT('Ctrl Pts',(-0.9528040785683,0.6451462712671,-4.765682451));
#36501=CARTESIAN_POINT('Ctrl Pts',(-0.3043627782466,1.109690328703,-4.816382724576));
#36502=CARTESIAN_POINT('Ctrl Pts',(0.4903412909185,1.040968175334,-4.867082998152));
#36503=CARTESIAN_POINT('Ctrl Pts',(1.049409857475,0.4720045291995,-4.917783271728));
#36504=CARTESIAN_POINT('Ctrl Pts',(1.104180244733,-0.323782815353,-4.968483545304));
#36505=CARTESIAN_POINT('Ctrl Pts',(0.6283323204288,-0.9639750097833,-5.01918381888));
#36506=CARTESIAN_POINT('Ctrl Pts',(-0.1494632583593,-1.140925089037,-5.069884092456));
#36507=CARTESIAN_POINT('Ctrl Pts',(-0.8554336598862,-0.7695989721411,-5.120584366032));
#36508=CARTESIAN_POINT('Ctrl Pts',(-1.150321933764,-0.02843893621772,-5.171284639608));
#36509=CARTESIAN_POINT('Ctrl Pts',(-0.8924183195055,0.7263875462816,-5.221984913184));
#36510=CARTESIAN_POINT('Ctrl Pts',(-0.2056594488852,1.132145536343,-5.27268518676));
#36511=CARTESIAN_POINT('Ctrl Pts',(0.5799299072375,0.9938463801022,-5.323385460336));
#36512=CARTESIAN_POINT('Ctrl Pts',(1.086831585149,0.3779502998543,-5.374085733912));
#36513=CARTESIAN_POINT('Ctrl Pts',(1.071451922086,-0.4195713348838,-5.424786007488));
#36514=CARTESIAN_POINT('Ctrl Pts',(0.5411816698712,-1.015466259243,-5.475486281064));
#36515=CARTESIAN_POINT('Ctrl Pts',(-0.2491556137298,-1.123374729009,-5.52618655464));
#36516=CARTESIAN_POINT('Ctrl Pts',(-0.919760239345,-0.6914409363236,-5.576886828216));
#36517=CARTESIAN_POINT('Ctrl Pts',(-1.148370014925,0.072767750194,-5.627587101792));
#36518=CARTESIAN_POINT('Ctrl Pts',(-0.8251271094647,0.8020070865056,-5.678287375368));
#36519=CARTESIAN_POINT('Ctrl Pts',(-0.1053615171142,1.145840561887,-5.728987648944));
#36520=CARTESIAN_POINT('Ctrl Pts',(0.6650192040728,0.9390285647018,-5.77968792252));
#36521=CARTESIAN_POINT('Ctrl Pts',(1.115884852611,0.2809891624084,-5.830388196096));
#36522=CARTESIAN_POINT('Ctrl Pts',(1.030273817282,-0.5121799772668,-5.881088469672));
#36523=CARTESIAN_POINT('Ctrl Pts',(0.6437130010352,-0.8766256805353,-5.914888652056));
#36524=CARTESIAN_POINT('Ctrl Pts',(0.4138139440886,-0.9742732692555,-5.931788743248));
#36525=CARTESIAN_POINT('Ctrl Pts',(-0.8352478720641,0.4641308339706,-4.368831721444));
#36526=CARTESIAN_POINT('Ctrl Pts',(-0.7257270174981,0.6612240973944,-4.385731812636));
#36527=CARTESIAN_POINT('Ctrl Pts',(-0.3618043599731,0.973579871545,-4.41953199502));
#36528=CARTESIAN_POINT('Ctrl Pts',(0.3583616355052,0.9750034062319,-4.470232268596));
#36529=CARTESIAN_POINT('Ctrl Pts',(0.9062041683879,0.5076847542727,-4.520932542172));
#36530=CARTESIAN_POINT('Ctrl Pts',(1.018596427125,-0.203550194661,-4.571632815748));
#36531=CARTESIAN_POINT('Ctrl Pts',(0.6414900337905,-0.8169826520078,-4.622333089324));
#36532=CARTESIAN_POINT('Ctrl Pts',(-0.04388486517291,-1.037806916131,-4.6730333629));
#36533=CARTESIAN_POINT('Ctrl Pts',(-0.7081712873547,-0.759909874548,-4.723733636476));
#36534=CARTESIAN_POINT('Ctrl Pts',(-1.032142960739,-0.1168347725255,-4.774433910052));
#36535=CARTESIAN_POINT('Ctrl Pts',(-0.8601141737781,0.5823856809165,-4.825134183628));
#36536=CARTESIAN_POINT('Ctrl Pts',(-0.2747540081207,1.00173834442,-4.875834457204));
#36537=CARTESIAN_POINT('Ctrl Pts',(0.4426403116802,0.9397015632025,-4.92653473078));
#36538=CARTESIAN_POINT('Ctrl Pts',(0.9473220285466,0.4260873717732,-4.977235004356));
#36539=CARTESIAN_POINT('Ctrl Pts',(0.9967642879194,-0.2922848411075,-5.027935277932));
#36540=CARTESIAN_POINT('Ctrl Pts',(0.5672074110512,-0.8701983836261,-5.078635551508));
#36541=CARTESIAN_POINT('Ctrl Pts',(-0.1349232962637,-1.029934550421,-5.129335825084));
#36542=CARTESIAN_POINT('Ctrl Pts',(-0.7722160642937,-0.694731476232,-5.18003609866));
#36543=CARTESIAN_POINT('Ctrl Pts',(-1.038417259008,-0.02567236295293,-5.230736372236));
#36544=CARTESIAN_POINT('Ctrl Pts',(-0.8056028125943,0.6557237088569,-5.281436645812));
#36545=CARTESIAN_POINT('Ctrl Pts',(-0.1856526550803,1.022009082971,-5.332136919388));
#36546=CARTESIAN_POINT('Ctrl Pts',(0.5235136417157,0.897163831801,-5.382837192964));
#36547=CARTESIAN_POINT('Ctrl Pts',(0.9811033264056,0.3411828488149,-5.43353746654));
#36548=CARTESIAN_POINT('Ctrl Pts',(0.9672198151093,-0.3787549404562,-5.484237740116));
#36549=CARTESIAN_POINT('Ctrl Pts',(0.4885348785918,-0.9166805035943,-5.534938013692));
#36550=CARTESIAN_POINT('Ctrl Pts',(-0.2249174616962,-1.014091510121,-5.585638287268));
#36551=CARTESIAN_POINT('Ctrl Pts',(-0.8302848782164,-0.6241767463422,-5.636338560844));
#36552=CARTESIAN_POINT('Ctrl Pts',(-1.036655225136,0.0656888176107,-5.68703883442));
#36553=CARTESIAN_POINT('Ctrl Pts',(-0.74485777085,0.7239868909991,-5.737739107996));
#36554=CARTESIAN_POINT('Ctrl Pts',(-0.09511182443393,1.034371840274,-5.788439381572));
#36555=CARTESIAN_POINT('Ctrl Pts',(0.6003253513746,0.8476787581516,-5.839139655148));
#36556=CARTESIAN_POINT('Ctrl Pts',(1.007330257735,0.2536542052052,-5.889839928724));
#36557=CARTESIAN_POINT('Ctrl Pts',(0.9300475649187,-0.4623545048573,-5.9405402023));
#36558=CARTESIAN_POINT('Ctrl Pts',(0.5810918409035,-0.7913465001737,-5.974340384684));
#36559=CARTESIAN_POINT('Ctrl Pts',(0.3735576354296,-0.8794948162679,-5.991240475876));
#36560=CARTESIAN_POINT('',(-0.733992715443622,1.01100376667461,-4.23040083151671));
#36561=CARTESIAN_POINT('Ctrl Pts',(-0.733858249660088,1.01085165460594,
-4.23006677329136));
#36562=CARTESIAN_POINT('Ctrl Pts',(-0.656624184784989,1.06704092143774,
-4.23558293594093));
#36563=CARTESIAN_POINT('Ctrl Pts',(-0.573048085765063,1.11459061696366,
-4.24108426906003));
#36564=CARTESIAN_POINT('Ctrl Pts',(-0.397055758914472,1.18918176106475,
-4.25195538849777));
#36565=CARTESIAN_POINT('Ctrl Pts',(-0.305762422032486,1.21563445447107,
-4.25725691531341));
#36566=CARTESIAN_POINT('Ctrl Pts',(-0.0531416665414995,1.25829397068379,
-4.27193030467578));
#36567=CARTESIAN_POINT('Ctrl Pts',(0.111123233468843,1.25441685178384,-4.28132801175063));
#36568=CARTESIAN_POINT('Ctrl Pts',(0.460594426391743,1.17866367040215,-4.30187191226297));
#36569=CARTESIAN_POINT('Ctrl Pts',(0.607960344748149,1.09991175854457,-4.31103977577589));
#36570=CARTESIAN_POINT('Ctrl Pts',(0.847486150103628,0.931203796797836,
-4.3279104257407));
#36571=CARTESIAN_POINT('Ctrl Pts',(0.961057414879083,0.814115725342219,
-4.33722749733213));
#36572=CARTESIAN_POINT('Ctrl Pts',(1.08901672234342,0.618045849386044,-4.3505869949951));
#36573=CARTESIAN_POINT('Ctrl Pts',(1.12361536676105,0.552784443534289,-4.35472027078159));
#36574=CARTESIAN_POINT('Ctrl Pts',(1.21477335836627,0.334472710659284,-4.36818280141384));
#36575=CARTESIAN_POINT('Ctrl Pts',(1.24755694627055,0.172180252671676,-4.37763258313196));
#36576=CARTESIAN_POINT('Ctrl Pts',(1.25087080107157,-0.150696375148907,
-4.39624596226418));
#36577=CARTESIAN_POINT('Ctrl Pts',(1.22275531302733,-0.305267334806458,
-4.40490395817152));
#36578=CARTESIAN_POINT('Ctrl Pts',(1.13388572849473,-0.531217437947803,
-4.41880417367254));
#36579=CARTESIAN_POINT('Ctrl Pts',(1.09568502554916,-0.605568589361117,
-4.42360727682551));
#36580=CARTESIAN_POINT('Ctrl Pts',(0.974278367896043,-0.794239096200339,
-4.43657050998369));
#36581=CARTESIAN_POINT('Ctrl Pts',(0.869783750705368,-0.913412171771251,
-4.44557250988085));
#36582=CARTESIAN_POINT('Ctrl Pts',(0.596567590420889,-1.11131409615458,
-4.46464303751621));
#36583=CARTESIAN_POINT('Ctrl Pts',(0.449841362804258,-1.17396421545565,
-4.47370678657374));
#36584=CARTESIAN_POINT('Ctrl Pts',(0.230696328844762,-1.23046801237028,
-4.48678250348742));
#36585=CARTESIAN_POINT('Ctrl Pts',(0.148087128506761,-1.24338760407243,
-4.49158580711337));
#36586=CARTESIAN_POINT('Ctrl Pts',(-0.0149243810933619,-1.25237940005118,
-4.50092857601243));
#36587=CARTESIAN_POINT('Ctrl Pts',(-0.0948562697134099,-1.2490356489232,
-4.50541104605373));
#36588=CARTESIAN_POINT('Ctrl Pts',(-0.319602267413793,-1.21692007737163,
-4.51830918900455));
#36589=CARTESIAN_POINT('Ctrl Pts',(-0.461052665580677,-1.169955946995,-4.52682047729437));
#36590=CARTESIAN_POINT('Ctrl Pts',(-0.662743299830164,-1.06213194850692,
-4.54002721971129));
#36591=CARTESIAN_POINT('Ctrl Pts',(-0.731406571816841,-1.01645316128059,
-4.5447559342723));
#36592=CARTESIAN_POINT('Ctrl Pts',(-0.855854786351091,-0.914449669496606,
-4.5539350964962));
#36593=CARTESIAN_POINT('Ctrl Pts',(-0.911397890189387,-0.859134433280608,
-4.55831634526413));
#36594=CARTESIAN_POINT('Ctrl Pts',(-1.06306225128544,-0.67548686397915,
-4.57188984157829));
#36595=CARTESIAN_POINT('Ctrl Pts',(-1.14070195689524,-0.532848962125197,
-4.58116298367123));
#36596=CARTESIAN_POINT('Ctrl Pts',(-1.2408543648333,-0.222972138419077,
-4.5999283034156));
#36597=CARTESIAN_POINT('Ctrl Pts',(-1.25922712849244,-0.0621179230072517,
-4.60883218350856));
#36598=CARTESIAN_POINT('Ctrl Pts',(-1.23199809975094,0.260794349941966,
-4.62742590355341));
#36599=CARTESIAN_POINT('Ctrl Pts',(-1.18777147826677,0.418227500329566,
-4.63678069006497));
#36600=CARTESIAN_POINT('Ctrl Pts',(-1.07195006124452,0.650201057523823,
-4.65165382848055));
#36601=CARTESIAN_POINT('Ctrl Pts',(-1.0174876518875,0.733036893765051,-4.657189771762));
#36602=CARTESIAN_POINT('Ctrl Pts',(-0.888289399775233,0.88459835520095,
-4.66850449009343));
#36603=CARTESIAN_POINT('Ctrl Pts',(-0.814482997793992,0.952439727927399,
-4.67423593308293));
#36604=CARTESIAN_POINT('Ctrl Pts',(-0.733889624077889,1.01082887649925,
-4.6799837403912));
#36605=CARTESIAN_POINT('',(-0.569874894277251,0.784947385717,-4.39168333211734));
#36606=CARTESIAN_POINT('Ctrl Pts',(-0.569529227319458,0.784474235852257,
-4.39166755057106));
#36607=CARTESIAN_POINT('Ctrl Pts',(-0.484636830506631,0.846338281756473,
-4.39942370350874));
#36608=CARTESIAN_POINT('Ctrl Pts',(-0.374984443336166,0.906078704177597,
-4.4084779942885));
#36609=CARTESIAN_POINT('Ctrl Pts',(-0.113185176117061,0.971160390418816,
-4.42841745272176));
#36610=CARTESIAN_POINT('Ctrl Pts',(0.0168632307072354,0.977315047570584,
-4.43783815175513));
#36611=CARTESIAN_POINT('Ctrl Pts',(0.269797863995035,0.940369046501483,
-4.45671267634792));
#36612=CARTESIAN_POINT('Ctrl Pts',(0.389640305530905,0.897489900285447,
-4.46594718063363));
#36613=CARTESIAN_POINT('Ctrl Pts',(0.606900163119448,0.766016505526538,
-4.4847012708543));
#36614=CARTESIAN_POINT('Ctrl Pts',(0.702014304273932,0.680148659476022,
-4.49397871953176));
#36615=CARTESIAN_POINT('Ctrl Pts',(0.865323843694858,0.462565672761075,
-4.51408024418007));
#36616=CARTESIAN_POINT('Ctrl Pts',(0.913111224941747,0.343586895448416,
-4.52336294452809));
#36617=CARTESIAN_POINT('Ctrl Pts',(0.969666070452136,0.119032334142472,
-4.54045552846132));
#36618=CARTESIAN_POINT('Ctrl Pts',(0.977445580061419,-0.00647510823698313,
-4.54956916057514));
#36619=CARTESIAN_POINT('Ctrl Pts',(0.9416925488968,-0.277924360370847,-4.5698103034962));
#36620=CARTESIAN_POINT('Ctrl Pts',(0.889895690185117,-0.398128861572051,
-4.57926951223364));
#36621=CARTESIAN_POINT('Ctrl Pts',(0.776609403954023,-0.59237863363198,
-4.59586369550252));
#36622=CARTESIAN_POINT('Ctrl Pts',(0.696444599699867,-0.685910391350863,
-4.60480297831157));
#36623=CARTESIAN_POINT('Ctrl Pts',(0.500258893832906,-0.841037207495601,
-4.62329685730815));
#36624=CARTESIAN_POINT('Ctrl Pts',(0.382468956290877,-0.899797001880555,
-4.6328259720572));
#36625=CARTESIAN_POINT('Ctrl Pts',(0.15959431279224,-0.961644353830406,
-4.64989505946642));
#36626=CARTESIAN_POINT('Ctrl Pts',(0.0346117104225062,-0.980352509949182,
-4.65904365625598));
#36627=CARTESIAN_POINT('Ctrl Pts',(-0.236343379195953,-0.949058136150462,
-4.67920711064833));
#36628=CARTESIAN_POINT('Ctrl Pts',(-0.360775378580012,-0.908544798855145,
-4.68867655849675));
#36629=CARTESIAN_POINT('Ctrl Pts',(-0.584818511226693,-0.784081692722746,
-4.70759675484773));
#36630=CARTESIAN_POINT('Ctrl Pts',(-0.680375181353425,-0.703150803980083,
-4.7166800988285));
#36631=CARTESIAN_POINT('Ctrl Pts',(-0.837749469773741,-0.503691778064584,
-4.73544988364439));
#36632=CARTESIAN_POINT('Ctrl Pts',(-0.89682553691833,-0.388763017720274,
-4.74480262132333));
#36633=CARTESIAN_POINT('Ctrl Pts',(-0.975938218374794,-0.116044677743505,
-4.76577767278224));
#36634=CARTESIAN_POINT('Ctrl Pts',(-0.974268306023395,0.0140308472029775,
-4.77517931330129));
#36635=CARTESIAN_POINT('Ctrl Pts',(-0.949101604663957,0.232235392643103,
-4.79139625667692));
#36636=CARTESIAN_POINT('Ctrl Pts',(-0.91129449898224,0.35349405795863,-4.80059642192052));
#36637=CARTESIAN_POINT('Ctrl Pts',(-0.781891247636186,0.59323425922455,
-4.82073207531561));
#36638=CARTESIAN_POINT('Ctrl Pts',(-0.692498942409321,0.686771888047504,
-4.83009240233825));
#36639=CARTESIAN_POINT('Ctrl Pts',(-0.514446522986027,0.83039260255699,
-4.8469749141452));
#36640=CARTESIAN_POINT('Ctrl Pts',(-0.404935910777101,0.889665186064185,
-4.85600502288631));
#36641=CARTESIAN_POINT('Ctrl Pts',(-0.134905330150572,0.974113150346371,
-4.87692444704566));
#36642=CARTESIAN_POINT('Ctrl Pts',(0.00160707428452082,0.97375035982292,
-4.88676307743964));
#36643=CARTESIAN_POINT('Ctrl Pts',(0.174562797360105,0.956837613378726,
-4.89958694906931));
#36644=CARTESIAN_POINT('Ctrl Pts',(0.302975074330177,0.935375752863402,
-4.90897285600405));
#36645=CARTESIAN_POINT('Ctrl Pts',(0.558866320705603,0.802941907514622,
-4.93027680936402));
#36646=CARTESIAN_POINT('Ctrl Pts',(0.660953880687901,0.720339425358645,
-4.93978064224544));
#36647=CARTESIAN_POINT('Ctrl Pts',(0.812076348801619,0.540264139141327,
-4.95713186062111));
#36648=CARTESIAN_POINT('Ctrl Pts',(0.88006177468165,0.433274456521509,-4.96631266398249));
#36649=CARTESIAN_POINT('Ctrl Pts',(0.962132946141089,0.174042975000006,
-4.98640717877759));
#36650=CARTESIAN_POINT('Ctrl Pts',(0.976467507927319,0.044763554717978,
-4.99581971407352));
#36651=CARTESIAN_POINT('Ctrl Pts',(0.955533483765511,-0.21011727305588,
-5.01470463930562));
#36652=CARTESIAN_POINT('Ctrl Pts',(0.920176570954095,-0.332501531122732,
-5.02394664366846));
#36653=CARTESIAN_POINT('Ctrl Pts',(0.802602751105269,-0.5575519956936,-5.04269775708713));
#36654=CARTESIAN_POINT('Ctrl Pts',(0.722990503962228,-0.657793652245648,
-5.05196625878101));
#36655=CARTESIAN_POINT('Ctrl Pts',(0.516180264657058,-0.834477351286836,
-5.07206541676142));
#36656=CARTESIAN_POINT('Ctrl Pts',(0.400332533119837,-0.889665217872399,
-5.08135517885404));
#36657=CARTESIAN_POINT('Ctrl Pts',(0.180035963144124,-0.960200187879756,
-5.09842867575985));
#36658=CARTESIAN_POINT('Ctrl Pts',(0.0554083971430053,-0.975898242544961,
-5.10753294808212));
#36659=CARTESIAN_POINT('Ctrl Pts',(-0.217938297569027,-0.957398080705504,
-5.12778753322606));
#36660=CARTESIAN_POINT('Ctrl Pts',(-0.341312967821623,-0.913148629947774,
-5.13725865191567));
#36661=CARTESIAN_POINT('Ctrl Pts',(-0.541952151862897,-0.812593040742933,
-5.15382004071268));
#36662=CARTESIAN_POINT('Ctrl Pts',(-0.640272812359031,-0.738621444203264,
-5.16274947913229));
#36663=CARTESIAN_POINT('Ctrl Pts',(-0.801962028794439,-0.55889875331323,
-5.18062559567604));
#36664=CARTESIAN_POINT('Ctrl Pts',(-0.865164262002844,-0.453332531951965,
-5.18955503409562));
#36665=CARTESIAN_POINT('Ctrl Pts',(-0.944023648542113,-0.243216597649746,
-5.20611642289259));
#36666=CARTESIAN_POINT('Ctrl Pts',(-0.975029766934585,-0.115866906741222,
-5.21558754158214));
#36667=CARTESIAN_POINT('Ctrl Pts',(-0.964630825541233,0.157907696748229,
-5.23584212672606));
#36668=CARTESIAN_POINT('Ctrl Pts',(-0.935891024457689,0.280188042516773,
-5.24494639904833));
#36669=CARTESIAN_POINT('Ctrl Pts',(-0.842541035141814,0.491828162134398,
-5.26201989595419));
#36670=CARTESIAN_POINT('Ctrl Pts',(-0.77545608704459,0.601217408678329,
-5.27130965804686));
#36671=CARTESIAN_POINT('Ctrl Pts',(-0.577968766812469,0.788263827879969,
-5.29140881602737));
#36672=CARTESIAN_POINT('Ctrl Pts',(-0.469898014985213,0.856872954117068,
-5.30067731772131));
#36673=CARTESIAN_POINT('Ctrl Pts',(-0.23371382158273,0.9500842275998,-5.31942843114003));
#36674=CARTESIAN_POINT('Ctrl Pts',(-0.108285830905315,0.972351626655508,
-5.32867043550288));
#36675=CARTESIAN_POINT('Ctrl Pts',(0.147382057119419,0.966318321832297,
-5.34755536073492));
#36676=CARTESIAN_POINT('Ctrl Pts',(0.274432011617761,0.938444369260619,
-5.35696789603077));
#36677=CARTESIAN_POINT('Ctrl Pts',(0.523575091539709,0.829520708270325,
-5.37706241082583));
#36678=CARTESIAN_POINT('Ctrl Pts',(0.622807399176715,0.750642577966378,
-5.38624321418721));
#36679=CARTESIAN_POINT('Ctrl Pts',(0.785960420543063,0.581390692617465,
-5.40359443256289));
#36680=CARTESIAN_POINT('Ctrl Pts',(0.857348683054847,0.471169297520893,
-5.41309826544433));
#36681=CARTESIAN_POINT('Ctrl Pts',(0.962088321082967,0.202750480014205,
-5.43440221880429));
#36682=CARTESIAN_POINT('Ctrl Pts',(0.96990295440032,0.0727918102781609,
-5.44378812573895));
#36683=CARTESIAN_POINT('Ctrl Pts',(0.968501283832614,-0.100983212255705,
-5.45661199736858));
#36684=CARTESIAN_POINT('Ctrl Pts',(0.954480930335871,-0.236774220313613,
-5.46645062776246));
#36685=CARTESIAN_POINT('Ctrl Pts',(0.842056053068118,-0.496405921220222,
-5.48737005192177));
#36686=CARTESIAN_POINT('Ctrl Pts',(0.771576711542563,-0.599062999690922,
-5.49640016066297));
#36687=CARTESIAN_POINT('Ctrl Pts',(0.609997938988823,-0.760994695040373,
-5.51328267247002));
#36688=CARTESIAN_POINT('Ctrl Pts',(0.507563614314368,-0.840035705712442,
-5.52264299949269));
#36689=CARTESIAN_POINT('Ctrl Pts',(0.25552523333294,-0.943463071888589,
-5.54277865288789));
#36690=CARTESIAN_POINT('Ctrl Pts',(0.130958452487734,-0.968285607294546,
-5.55197881813158));
#36691=CARTESIAN_POINT('Ctrl Pts',(-0.0886831345803024,-0.970325150882856,
-5.56819576150725));
#36692=CARTESIAN_POINT('Ctrl Pts',(-0.218210781696016,-0.958282749541544,
-5.57759740202637));
#36693=CARTESIAN_POINT('Ctrl Pts',(-0.481077340281054,-0.850880320776047,
-5.59857245348522));
#36694=CARTESIAN_POINT('Ctrl Pts',(-0.589143120265966,-0.780025618322455,
-5.60792519116405));
#36695=CARTESIAN_POINT('Ctrl Pts',(-0.770913413302382,-0.602514688393461,
-5.62669497597979));
#36696=CARTESIAN_POINT('Ctrl Pts',(-0.841327391289032,-0.498963939181014,
-5.63577831996048));
#36697=CARTESIAN_POINT('Ctrl Pts',(-0.941495735081663,-0.263055709192854,
-5.65469851631137));
#36698=CARTESIAN_POINT('Ctrl Pts',(-0.968675143304464,-0.135048159657013,
-5.66416796415975));
#36699=CARTESIAN_POINT('Ctrl Pts',(-0.971251168838689,0.13769597412805,
-5.68433141855208));
#36700=CARTESIAN_POINT('Ctrl Pts',(-0.93948061393768,0.260012276564817,
-5.69348001534169));
#36701=CARTESIAN_POINT('Ctrl Pts',(-0.854498309521642,0.475131335678752,
-5.71054910275097));
#36702=CARTESIAN_POINT('Ctrl Pts',(-0.783656704497057,0.586075690288882,
-5.72007821750008));
#36703=CARTESIAN_POINT('Ctrl Pts',(-0.608725574238606,0.76482764115972,
-5.73857209649671));
#36704=CARTESIAN_POINT('Ctrl Pts',(-0.507269174368512,0.834693115239855,
-5.74751137930577));
#36705=CARTESIAN_POINT('Ctrl Pts',(-0.302165962186496,0.926885462785101,
-5.7641055625747));
#36706=CARTESIAN_POINT('Ctrl Pts',(-0.177173705923737,0.965730958737602,
-5.77356477131219));
#36707=CARTESIAN_POINT('Ctrl Pts',(0.0965315452820904,0.972688773335761,
-5.79380591423329));
#36708=CARTESIAN_POINT('Ctrl Pts',(0.2205210636506,0.951730763001617,-5.80291954634709));
#36709=CARTESIAN_POINT('Ctrl Pts',(0.437868240623845,0.871834541464923,
-5.82001213028032));
#36710=CARTESIAN_POINT('Ctrl Pts',(0.551150726807563,0.811779053944627,
-5.82929483062832));
#36711=CARTESIAN_POINT('Ctrl Pts',(0.750318872098348,0.626456600703951,
-5.84939635527662));
#36712=CARTESIAN_POINT('Ctrl Pts',(0.825688954935261,0.522825826094886,
-5.85867380395408));
#36713=CARTESIAN_POINT('Ctrl Pts',(0.933543174363937,0.292924615571325,
-5.87742789417475));
#36714=CARTESIAN_POINT('Ctrl Pts',(0.963558721675801,0.169231855504208,
-5.88666239846044));
#36715=CARTESIAN_POINT('Ctrl Pts',(0.973653321148666,-0.0861874757390947,
-5.9055369230532));
#36716=CARTESIAN_POINT('Ctrl Pts',(0.953832746458545,-0.214863863398631,
-5.91495762208655));
#36717=CARTESIAN_POINT('Ctrl Pts',(0.861533508110168,-0.46835027550829,
-5.93489708439995));
#36718=CARTESIAN_POINT('Ctrl Pts',(0.790573961255546,-0.571099081510327,
-5.94395137805178));
#36719=CARTESIAN_POINT('Ctrl Pts',(0.720110998144666,-0.649001939469338,
-5.95170753282398));
#36720=CARTESIAN_POINT('',(-0.7343749446882,1.011530247009,-4.230025253169));
#36721=CARTESIAN_POINT('Ctrl Pts',(0.7205712401658,-0.6275615720196,-2.918810030463));
#36722=CARTESIAN_POINT('Ctrl Pts',(0.5724856689652,-0.7975946149087,-2.935710121655));
#36723=CARTESIAN_POINT('Ctrl Pts',(0.1516001974293,-1.027510360684,-2.969510304039));
#36724=CARTESIAN_POINT('Ctrl Pts',(-0.5531418425703,-0.879254687769,-3.020210577615));
#36725=CARTESIAN_POINT('Ctrl Pts',(-0.9919188003728,-0.3082967693496,-3.070910851191));
#36726=CARTESIAN_POINT('Ctrl Pts',(-0.9540654718091,0.4107681080609,-3.121611124767));
#36727=CARTESIAN_POINT('Ctrl Pts',(-0.4577212901491,0.9324491072861,-3.172311398343));
#36728=CARTESIAN_POINT('Ctrl Pts',(0.2585798251871,1.006034567282,-3.223011671919));
#36729=CARTESIAN_POINT('Ctrl Pts',(0.8506201287607,0.5961669113734,-3.273711945495));
#36730=CARTESIAN_POINT('Ctrl Pts',(1.033891258762,-0.1001914194485,-3.324412219071));
#36731=CARTESIAN_POINT('Ctrl Pts',(0.7203217911921,-0.7484022918219,-3.375112492647));
#36732=CARTESIAN_POINT('Ctrl Pts',(0.06059873957321,-1.03696541332,-3.425812766223));
#36733=CARTESIAN_POINT('Ctrl Pts',(-0.6282452790402,-0.8272105794617,-3.476513039799));
#36734=CARTESIAN_POINT('Ctrl Pts',(-1.015183472352,-0.2199363353731,-3.527213313375));
#36735=CARTESIAN_POINT('Ctrl Pts',(-0.914271115017,0.4930292103498,-3.577913586951));
#36736=CARTESIAN_POINT('Ctrl Pts',(-0.3740020515216,0.969067561873,-3.628613860527));
#36737=CARTESIAN_POINT('Ctrl Pts',(0.3459952203822,0.9794165515745,-3.679314134103));
#36738=CARTESIAN_POINT('Ctrl Pts',(0.8997230806097,0.5191029302932,-3.730014407679));
#36739=CARTESIAN_POINT('Ctrl Pts',(1.021085351762,-0.1906677173599,-3.780714681255));
#36740=CARTESIAN_POINT('Ctrl Pts',(0.6517609003688,-0.8088122172466,-3.831414954831));
#36741=CARTESIAN_POINT('Ctrl Pts',(-0.03076990492567,-1.038278713527,-3.882115228407));
#36742=CARTESIAN_POINT('Ctrl Pts',(-0.6985141072616,-0.7687961473049,-3.932815501983));
#36743=CARTESIAN_POINT('Ctrl Pts',(-1.030584511335,-0.1298654627114,-3.983515775559));
#36744=CARTESIAN_POINT('Ctrl Pts',(-0.8674033346712,0.5714725983469,-4.034216049135));
#36745=CARTESIAN_POINT('Ctrl Pts',(-0.287387948432,0.9981871770197,-4.084916322711));
#36746=CARTESIAN_POINT('Ctrl Pts',(0.4307328640486,0.9452188399008,-4.135616596287));
#36747=CARTESIAN_POINT('Ctrl Pts',(0.9418633284912,0.4380217575791,-4.186316869863));
#36748=CARTESIAN_POINT('Ctrl Pts',(1.000377225472,-0.2796685240019,-4.237017143439));
#36749=CARTESIAN_POINT('Ctrl Pts',(0.5781569339062,-0.8629627320519,-4.287717417015));
#36750=CARTESIAN_POINT('Ctrl Pts',(-0.1219033535594,-1.031557528929,-4.338417690591));
#36751=CARTESIAN_POINT('Ctrl Pts',(-0.7633663370709,-0.7044300106834,-4.389117964167));
#36752=CARTESIAN_POINT('Ctrl Pts',(-1.038050796595,-0.03879752124175,-4.439818237743));
#36753=CARTESIAN_POINT('Ctrl Pts',(-0.813670763595,0.6455230821929,-4.490518511319));
#36754=CARTESIAN_POINT('Ctrl Pts',(-0.4039685755409,0.8948219939615,-4.524318693703));
#36755=CARTESIAN_POINT('Ctrl Pts',(-0.1826474890299,0.9379212832541,-4.541218784895));
#36756=CARTESIAN_POINT('Ctrl Pts',(0.7982233492482,-0.6951905265629,-2.978261763091));
#36757=CARTESIAN_POINT('Ctrl Pts',(0.6341793879712,-0.8835471211815,-2.995161854283));
#36758=CARTESIAN_POINT('Ctrl Pts',(0.1679373399789,-1.138239657336,-3.028962036667));
#36759=CARTESIAN_POINT('Ctrl Pts',(-0.6127509808526,-0.9740072633923,-3.079662310243));
#36760=CARTESIAN_POINT('Ctrl Pts',(-1.098812584906,-0.3415202634732,-3.130362583819));
#36761=CARTESIAN_POINT('Ctrl Pts',(-1.056880005555,0.4550343903613,-3.181062857395));
#36762=CARTESIAN_POINT('Ctrl Pts',(-0.5070474657869,1.032934161028,-3.231763130971));
#36763=CARTESIAN_POINT('Ctrl Pts',(0.2864455901145,1.114449532528,-3.282463404547));
#36764=CARTESIAN_POINT('Ctrl Pts',(0.9422869110915,0.6604126312312,-3.333163678123));
#36765=CARTESIAN_POINT('Ctrl Pts',(1.145308190676,-0.1109885129189,-3.383863951699));
#36766=CARTESIAN_POINT('Ctrl Pts',(0.7979470184926,-0.8290536045064,-3.434564225275));
#36767=CARTESIAN_POINT('Ctrl Pts',(0.06712914166712,-1.148713630431,-3.485264498851));
#36768=CARTESIAN_POINT('Ctrl Pts',(-0.6959479130327,-0.9163546398542,-3.535964772427));
#36769=CARTESIAN_POINT('Ctrl Pts',(-1.12458436617,-0.2436376980609,-3.586665046003));
#36770=CARTESIAN_POINT('Ctrl Pts',(-1.012797223744,0.546160331728,-3.637365319579));
#36771=CARTESIAN_POINT('Ctrl Pts',(-0.4143062525262,1.073498790637,-3.688065593155));
#36772=CARTESIAN_POINT('Ctrl Pts',(0.3832812749699,1.084963035615,-3.738765866731));
#36773=CARTESIAN_POINT('Ctrl Pts',(0.9966814254686,0.5750438770327,-3.789466140307));
#36774=CARTESIAN_POINT('Ctrl Pts',(1.131122259562,-0.2112149576071,-3.840166413883));
#36775=CARTESIAN_POINT('Ctrl Pts',(0.7219976871151,-0.8959735845339,-3.890866687459));
#36776=CARTESIAN_POINT('Ctrl Pts',(-0.03408581302824,-1.150168457978,-3.941566961035));
#36777=CARTESIAN_POINT('Ctrl Pts',(-0.773789237088,-0.8516451967325,-3.992267234611));
#36778=CARTESIAN_POINT('Ctrl Pts',(-1.141645092763,-0.1438603691333,-4.042967508187));
#36779=CARTESIAN_POINT('Ctrl Pts',(-0.9608787533499,0.63305714415,-4.093667781763));
#36780=CARTESIAN_POINT('Ctrl Pts',(-0.3183582107415,1.105756470983,-4.144368055339));
#36781=CARTESIAN_POINT('Ctrl Pts',(0.4771506413343,1.047080019436,-4.195068328915));
#36782=CARTESIAN_POINT('Ctrl Pts',(1.043362902507,0.485225019941,-4.245768602491));
#36783=CARTESIAN_POINT('Ctrl Pts',(1.108182529245,-0.3098069052225,-4.296468876067));
#36784=CARTESIAN_POINT('Ctrl Pts',(0.6404618148061,-0.9559596107337,-4.347169149643));
#36785=CARTESIAN_POINT('Ctrl Pts',(-0.1350402260578,-1.142722967259,-4.397869423219));
#36786=CARTESIAN_POINT('Ctrl Pts',(-0.8456302448871,-0.7803426657845,-4.448569696795));
#36787=CARTESIAN_POINT('Ctrl Pts',(-1.149915979657,-0.04297852262462,-4.499269970371));
#36788=CARTESIAN_POINT('Ctrl Pts',(-0.9013557104398,0.715087652633,-4.549970243947));
#36789=CARTESIAN_POINT('Ctrl Pts',(-0.4475021085842,0.9912521749224,-4.583770426331));
#36790=CARTESIAN_POINT('Ctrl Pts',(-0.2023304321606,1.038996044136,-4.600670517523));
#36791=CARTESIAN_POINT('Ctrl Pts',(0.8758754583306,-0.7628194811062,-3.037713495719));
#36792=CARTESIAN_POINT('Ctrl Pts',(0.6958731069771,-0.9694996274544,-3.054613586911));
#36793=CARTESIAN_POINT('Ctrl Pts',(0.1842744825284,-1.248968953987,-3.088413769295));
#36794=CARTESIAN_POINT('Ctrl Pts',(-0.6723601191349,-1.068759839016,-3.139114042871));
#36795=CARTESIAN_POINT('Ctrl Pts',(-1.20570636944,-0.3747437575968,-3.189814316447));
#36796=CARTESIAN_POINT('Ctrl Pts',(-1.159694539302,0.4993006726617,-3.240514590023));
#36797=CARTESIAN_POINT('Ctrl Pts',(-0.5563736414247,1.133419214769,-3.291214863599));
#36798=CARTESIAN_POINT('Ctrl Pts',(0.314311355042,1.222864497773,-3.341915137175));
#36799=CARTESIAN_POINT('Ctrl Pts',(1.033953693422,0.7246583510889,-3.392615410751));
#36800=CARTESIAN_POINT('Ctrl Pts',(1.256725122589,-0.1217856063893,-3.443315684327));
#36801=CARTESIAN_POINT('Ctrl Pts',(0.8755722457931,-0.9097049171909,-3.494015957903));
#36802=CARTESIAN_POINT('Ctrl Pts',(0.07365954376103,-1.260461847542,-3.544716231479));
#36803=CARTESIAN_POINT('Ctrl Pts',(-0.7636505470253,-1.005498700247,-3.595416505055));
#36804=CARTESIAN_POINT('Ctrl Pts',(-1.233985259988,-0.2673390607487,-3.646116778631));
#36805=CARTESIAN_POINT('Ctrl Pts',(-1.111323332471,0.5992914531062,-3.696817052207));
#36806=CARTESIAN_POINT('Ctrl Pts',(-0.4546104535308,1.177930019402,-3.747517325783));
#36807=CARTESIAN_POINT('Ctrl Pts',(0.4205673295575,1.190509519655,-3.798217599359));
#36808=CARTESIAN_POINT('Ctrl Pts',(1.093639770328,0.6309848237721,-3.848917872935));
#36809=CARTESIAN_POINT('Ctrl Pts',(1.241159167361,-0.2317621978543,-3.899618146511));
#36810=CARTESIAN_POINT('Ctrl Pts',(0.7922344738614,-0.9831349518212,-3.950318420088));
#36811=CARTESIAN_POINT('Ctrl Pts',(-0.03740172113081,-1.262058202429,-4.001018693664));
#36812=CARTESIAN_POINT('Ctrl Pts',(-0.8490643669144,-0.9344942461601,-4.05171896724));
#36813=CARTESIAN_POINT('Ctrl Pts',(-1.252705674191,-0.1578552755553,-4.102419240816));
#36814=CARTESIAN_POINT('Ctrl Pts',(-1.054354172029,0.6946416899531,-4.153119514392));
#36815=CARTESIAN_POINT('Ctrl Pts',(-0.3493284730509,1.213325764945,-4.203819787968));
#36816=CARTESIAN_POINT('Ctrl Pts',(0.5235684186199,1.148941198972,-4.254520061544));
#36817=CARTESIAN_POINT('Ctrl Pts',(1.144862476522,0.5324282823029,-4.30522033512));
#36818=CARTESIAN_POINT('Ctrl Pts',(1.215987833017,-0.3399452864431,-4.355920608696));
#36819=CARTESIAN_POINT('Ctrl Pts',(0.702766695706,-1.048956489416,-4.406620882272));
#36820=CARTESIAN_POINT('Ctrl Pts',(-0.1481770985562,-1.253888405589,-4.457321155848));
#36821=CARTESIAN_POINT('Ctrl Pts',(-0.9278941527034,-0.8562553208856,-4.508021429424));
#36822=CARTESIAN_POINT('Ctrl Pts',(-1.261781162719,-0.04715952400749,-4.558721703));
#36823=CARTESIAN_POINT('Ctrl Pts',(-0.9890406572845,0.7846522230731,-4.609421976576));
#36824=CARTESIAN_POINT('Ctrl Pts',(-0.4910356416274,1.087682355883,-4.64322215896));
#36825=CARTESIAN_POINT('Ctrl Pts',(-0.2220133752913,1.140070805017,-4.660122250152));
#36826=CARTESIAN_POINT('Ctrl Pts',(0.9535275674129,-0.8304484356495,-3.097165228348));
#36827=CARTESIAN_POINT('Ctrl Pts',(0.7575668259831,-1.055452133727,-3.11406531954));
#36828=CARTESIAN_POINT('Ctrl Pts',(0.200611625078,-1.359698250639,-3.147865501924));
#36829=CARTESIAN_POINT('Ctrl Pts',(-0.7319692574172,-1.163512414639,-3.1985657755));
#36830=CARTESIAN_POINT('Ctrl Pts',(-1.312600153974,-0.4079672517203,-3.249266049076));
#36831=CARTESIAN_POINT('Ctrl Pts',(-1.262509073048,0.543566954962,-3.299966322652));
#36832=CARTESIAN_POINT('Ctrl Pts',(-0.6056998170625,1.233904268511,-3.350666596228));
#36833=CARTESIAN_POINT('Ctrl Pts',(0.3421771199694,1.331279463018,-3.401366869804));
#36834=CARTESIAN_POINT('Ctrl Pts',(1.125620475753,0.7889040709467,-3.45206714338));
#36835=CARTESIAN_POINT('Ctrl Pts',(1.368142054503,-0.1325826998597,-3.502767416956));
#36836=CARTESIAN_POINT('Ctrl Pts',(0.9531974730936,-0.9903562298753,-3.553467690532));
#36837=CARTESIAN_POINT('Ctrl Pts',(0.08018994585494,-1.372210064652,-3.604167964108));
#36838=CARTESIAN_POINT('Ctrl Pts',(-0.8313531810178,-1.094642760639,-3.654868237684));
#36839=CARTESIAN_POINT('Ctrl Pts',(-1.343386153806,-0.2910404234365,-3.70556851126));
#36840=CARTESIAN_POINT('Ctrl Pts',(-1.209849441198,0.6524225744844,-3.756268784836));
#36841=CARTESIAN_POINT('Ctrl Pts',(-0.4949146545354,1.282361248166,-3.806969058412));
#36842=CARTESIAN_POINT('Ctrl Pts',(0.4578533841451,1.296056003695,-3.857669331988));
#36843=CARTESIAN_POINT('Ctrl Pts',(1.190598115186,0.6869257705116,-3.908369605564));
#36844=CARTESIAN_POINT('Ctrl Pts',(1.351196075161,-0.2523094381015,-3.95906987914));
#36845=CARTESIAN_POINT('Ctrl Pts',(0.8624712606077,-1.070296319109,-4.009770152716));
#36846=CARTESIAN_POINT('Ctrl Pts',(-0.04071762923338,-1.373947946879,-4.060470426292));
#36847=CARTESIAN_POINT('Ctrl Pts',(-0.9243394967408,-1.017343295588,-4.111170699868));
#36848=CARTESIAN_POINT('Ctrl Pts',(-1.363766255618,-0.1718501819773,-4.161870973444));
#36849=CARTESIAN_POINT('Ctrl Pts',(-1.147829590707,0.7562262357563,-4.21257124702));
#36850=CARTESIAN_POINT('Ctrl Pts',(-0.3802987353604,1.320895058908,-4.263271520596));
#36851=CARTESIAN_POINT('Ctrl Pts',(0.5699861959056,1.250802378507,-4.313971794172));
#36852=CARTESIAN_POINT('Ctrl Pts',(1.246362050538,0.5796315446648,-4.364672067748));
#36853=CARTESIAN_POINT('Ctrl Pts',(1.32379313679,-0.3700836676636,-4.415372341324));
#36854=CARTESIAN_POINT('Ctrl Pts',(0.7650715766059,-1.141953368097,-4.4660726149));
#36855=CARTESIAN_POINT('Ctrl Pts',(-0.1613139710547,-1.365053843919,-4.516772888476));
#36856=CARTESIAN_POINT('Ctrl Pts',(-1.01015806052,-0.9321679759867,-4.567473162052));
#36857=CARTESIAN_POINT('Ctrl Pts',(-1.37364634578,-0.05134052539036,-4.618173435628));
#36858=CARTESIAN_POINT('Ctrl Pts',(-1.076725604129,0.8542167935132,-4.668873709204));
#36859=CARTESIAN_POINT('Ctrl Pts',(-0.5345691746706,1.184112536844,-4.702673891588));
#36860=CARTESIAN_POINT('Ctrl Pts',(-0.2416963184219,1.241145565899,-4.71957398278));
#36861=CARTESIAN_POINT('',(0.507887877650121,-1.14145688760839,-3.11964125711469));
#36862=CARTESIAN_POINT('Ctrl Pts',(-0.733875647329055,1.01087300651023,
-4.23008257417792));
#36863=CARTESIAN_POINT('Ctrl Pts',(-0.825987121271145,0.94411145872215,
-4.22363001656661));
#36864=CARTESIAN_POINT('Ctrl Pts',(-0.928569855441707,0.851140106664914,
-4.21583740331039));
#36865=CARTESIAN_POINT('Ctrl Pts',(-1.09492055138801,0.617000415853516,
-4.19906379556599));
#36866=CARTESIAN_POINT('Ctrl Pts',(-1.15319261062486,0.49772291024227,-4.1915815901967));
#36867=CARTESIAN_POINT('Ctrl Pts',(-1.23189231323316,0.245489451432284,
-4.17660903244399));
#36868=CARTESIAN_POINT('Ctrl Pts',(-1.25171978917578,0.111810504704931,
-4.16906604902943));
#36869=CARTESIAN_POINT('Ctrl Pts',(-1.24852928233844,-0.096715149384668,
-4.15698096414954));
#36870=CARTESIAN_POINT('Ctrl Pts',(-1.24042793192133,-0.171145972738229,
-4.15260661067975));
#36871=CARTESIAN_POINT('Ctrl Pts',(-1.20903242612985,-0.326144503860473,
-4.14350186866899));
#36872=CARTESIAN_POINT('Ctrl Pts',(-1.18434831837205,-0.405891266492904,
-4.13877985127521));
#36873=CARTESIAN_POINT('Ctrl Pts',(-1.09931321063353,-0.608469106103288,
-4.12632324246702));
#36874=CARTESIAN_POINT('Ctrl Pts',(-1.02613933958735,-0.726105546047824,
-4.11859175537242));
#36875=CARTESIAN_POINT('Ctrl Pts',(-0.889031840281174,-0.881536851166071,
-4.10657357976713));
#36876=CARTESIAN_POINT('Ctrl Pts',(-0.838070882863559,-0.93003158188435,
-4.10245889965596));
#36877=CARTESIAN_POINT('Ctrl Pts',(-0.71804471629122,-1.02598281535047,
-4.09359767136651));
#36878=CARTESIAN_POINT('Ctrl Pts',(-0.647920116788861,-1.07130370486005,
-4.08887034149716));
#36879=CARTESIAN_POINT('Ctrl Pts',(-0.451607190563765,-1.17261984972335,
-4.07634288194066));
#36880=CARTESIAN_POINT('Ctrl Pts',(-0.318735404546458,-1.21605862648864,
-4.06855248872333));
#36881=CARTESIAN_POINT('Ctrl Pts',(-0.116566973731751,-1.24631682178166,
-4.05671455059356));
#36882=CARTESIAN_POINT('Ctrl Pts',(-0.0503947385544985,-1.25072100020528,
-4.0528319962753));
#36883=CARTESIAN_POINT('Ctrl Pts',(0.177200110844515,-1.24723779942647,
-4.03967510971017));
#36884=CARTESIAN_POINT('Ctrl Pts',(0.337818864680723,-1.21310245611501,
-4.03061613897922));
#36885=CARTESIAN_POINT('Ctrl Pts',(0.627325461026085,-1.09155867140617,
-4.01274824690792));
#36886=CARTESIAN_POINT('Ctrl Pts',(0.751113999919971,-1.01028915862942,
-4.0041824455675));
#36887=CARTESIAN_POINT('Ctrl Pts',(0.918980844614885,-0.850590818913521,
-3.99085360498138));
#36888=CARTESIAN_POINT('Ctrl Pts',(0.973415257658214,-0.787286509795003,
-3.98613405120972));
#36889=CARTESIAN_POINT('Ctrl Pts',(1.09889105453754,-0.608894755549359,
-3.97377157854704));
#36890=CARTESIAN_POINT('Ctrl Pts',(1.15913819005378,-0.486012614431139,
-3.96612861225493));
#36891=CARTESIAN_POINT('Ctrl Pts',(1.21926945032107,-0.285379499728559,
-3.95397856946806));
#36892=CARTESIAN_POINT('Ctrl Pts',(1.23392516157266,-0.212698818790114,
-3.94964661234106));
#36893=CARTESIAN_POINT('Ctrl Pts',(1.25097407343862,-0.0562022111640335,
-3.94058370371999));
#36894=CARTESIAN_POINT('Ctrl Pts',(1.25166086109128,0.0272909789852731,
-3.93586148317175));
#36895=CARTESIAN_POINT('Ctrl Pts',(1.23219006522341,0.245418179734663,-3.92344681075619));
#36896=CARTESIAN_POINT('Ctrl Pts',(1.19847382539114,0.379013246675096,-3.9157572839109));
#36897=CARTESIAN_POINT('Ctrl Pts',(1.11540449196199,0.568718283946679,-3.90375051671024));
#36898=CARTESIAN_POINT('Ctrl Pts',(1.08136457923424,0.630911587796264,-3.89960405334492));
#36899=CARTESIAN_POINT('Ctrl Pts',(0.995866667981166,0.759255627291935,
-3.89071275004434));
#36900=CARTESIAN_POINT('Ctrl Pts',(0.94283254918456,0.823743151752923,-3.88598591056034));
#36901=CARTESIAN_POINT('Ctrl Pts',(0.786673071735048,0.979851467190434,
-3.87346473923337));
#36902=CARTESIAN_POINT('Ctrl Pts',(0.673389570842327,1.06156566729279,-3.86567943453108));
#36903=CARTESIAN_POINT('Ctrl Pts',(0.489746229335454,1.15199765544022,-3.85382352758708));
#36904=CARTESIAN_POINT('Ctrl Pts',(0.427675323548356,1.17642765668122,-3.84991855320174));
#36905=CARTESIAN_POINT('Ctrl Pts',(0.209385353179634,1.24222689073648,-3.83674361154985));
#36906=CARTESIAN_POINT('Ctrl Pts',(0.0459967194180074,1.2584201992733,-3.82768643928908));
#36907=CARTESIAN_POINT('Ctrl Pts',(-0.264125856239754,1.23064739634467,
-3.80996546352936));
#36908=CARTESIAN_POINT('Ctrl Pts',(-0.404568568651727,1.19185916584351,
-3.80153535902006));
#36909=CARTESIAN_POINT('Ctrl Pts',(-0.6115300780727,1.09275004242686,-3.78832831044393));
#36910=CARTESIAN_POINT('Ctrl Pts',(-0.682848754794305,1.04933401051589,
-3.78360702519108));
#36911=CARTESIAN_POINT('Ctrl Pts',(-0.857708853406781,0.918031373235897,
-3.77121134160043));
#36912=CARTESIAN_POINT('Ctrl Pts',(-0.953282912340471,0.819253189261027,
-3.76353878693458));
#36913=CARTESIAN_POINT('Ctrl Pts',(-1.07125640891817,0.648176685622839,
-3.75148822550272));
#36914=CARTESIAN_POINT('Ctrl Pts',(-1.10664532108669,0.585546807113655,
-3.74728237147825));
#36915=CARTESIAN_POINT('Ctrl Pts',(-1.17083993611844,0.44419810319016,-3.73833619083301));
#36916=CARTESIAN_POINT('Ctrl Pts',(-1.19756547092642,0.365094147117043,
-3.73361081846715));
#36917=CARTESIAN_POINT('Ctrl Pts',(-1.24744717470402,0.150623842050563,
-3.72112571182027));
#36918=CARTESIAN_POINT('Ctrl Pts',(-1.25702073797125,0.0119166161975678,
-3.71337291257023));
#36919=CARTESIAN_POINT('Ctrl Pts',(-1.23983357350552,-0.163266891536038,
-3.70317452631609));
#36920=CARTESIAN_POINT('Ctrl Pts',(-1.23420088928342,-0.201636096563702,
-3.70091049128662));
#36921=CARTESIAN_POINT('Ctrl Pts',(-1.19602087654215,-0.396264459324683,
-3.68935075162125));
#36922=CARTESIAN_POINT('Ctrl Pts',(-1.13438572831812,-0.546182761234717,
-3.68035352269049));
#36923=CARTESIAN_POINT('Ctrl Pts',(-1.00347591375521,-0.748602659195634,
-3.66668241530662));
#36924=CARTESIAN_POINT('Ctrl Pts',(-0.952126672075524,-0.813359570715913,
-3.66200205495338));
#36925=CARTESIAN_POINT('Ctrl Pts',(-0.844070250943292,-0.924785227570656,
-3.65305173108173));
#36926=CARTESIAN_POINT('Ctrl Pts',(-0.789002477788614,-0.972269596887259,
-3.64879779712052));
#36927=CARTESIAN_POINT('Ctrl Pts',(-0.624132091077882,-1.09030372751535,
-3.63705110011354));
#36928=CARTESIAN_POINT('Ctrl Pts',(-0.506629078599337,-1.14902801670687,
-3.62970604262753));
#36929=CARTESIAN_POINT('Ctrl Pts',(-0.304011928651628,-1.21446751650945,
-3.61763778112587));
#36930=CARTESIAN_POINT('Ctrl Pts',(-0.222329568483162,-1.23230954292719,
-3.61291280107117));
#36931=CARTESIAN_POINT('Ctrl Pts',(0.0120443509726828,-1.25935018450633,
-3.59934542048976));
#36932=CARTESIAN_POINT('Ctrl Pts',(0.16353090081991,-1.24872899180732,-3.59056887251069));
#36933=CARTESIAN_POINT('Ctrl Pts',(0.47078982918158,-1.16796950043995,-3.57249718230263));
#36934=CARTESIAN_POINT('Ctrl Pts',(0.61917907071545,-1.09716798788213,-3.56342436605197));
#36935=CARTESIAN_POINT('Ctrl Pts',(0.803253762053073,-0.960147658502963,
-3.55014885951359));
#36936=CARTESIAN_POINT('Ctrl Pts',(0.854156106363377,-0.915153330275588,
-3.54617101977603));
#36937=CARTESIAN_POINT('Ctrl Pts',(0.994107305067958,-0.768798171891316,
-3.53446084760397));
#36938=CARTESIAN_POINT('Ctrl Pts',(1.07098938598973,-0.656508753343506,
-3.5268721498646));
#36939=CARTESIAN_POINT('Ctrl Pts',(1.16398616596849,-0.460982468107929,
-3.5145932231718));
#36940=CARTESIAN_POINT('Ctrl Pts',(1.1921384149349,-0.383279648853243,-3.50991290675987));
#36941=CARTESIAN_POINT('Ctrl Pts',(1.23024443209663,-0.232777514142283,
-3.50096071108599));
#36942=CARTESIAN_POINT('Ctrl Pts',(1.24174709866166,-0.160943484599564,
-3.49670472743925));
#36943=CARTESIAN_POINT('Ctrl Pts',(1.2556222927149,0.0413592225819834,-3.48495724321245));
#36944=CARTESIAN_POINT('Ctrl Pts',(1.24390126337967,0.17216988600908,-3.47761349197787));
#36945=CARTESIAN_POINT('Ctrl Pts',(1.19321167061787,0.378945395780619,-3.46554665252736));
#36946=CARTESIAN_POINT('Ctrl Pts',(1.16550737804734,0.457830075032333,-3.46082173077236));
#36947=CARTESIAN_POINT('Ctrl Pts',(1.06543134020746,0.671552931208405,-3.44725088042344));
#36948=CARTESIAN_POINT('Ctrl Pts',(0.976799012979039,0.794958674899222,
-3.4384698933436));
#36949=CARTESIAN_POINT('Ctrl Pts',(0.746627562182523,1.01407250609846,-3.42039294242618));
#36950=CARTESIAN_POINT('Ctrl Pts',(0.608440156904095,1.10315982006909,-3.41132009370902));
#36951=CARTESIAN_POINT('Ctrl Pts',(0.395171729154963,1.18782900119653,-3.39804520758731));
#36952=CARTESIAN_POINT('Ctrl Pts',(0.330160405457533,1.2075100217443,-3.39406810295473));
#36953=CARTESIAN_POINT('Ctrl Pts',(0.1321133813571,1.24973963688798,-3.38235795609272));
#36954=CARTESIAN_POINT('Ctrl Pts',(-0.00383399948244982,1.25618895580989,
-3.37476855565622));
#36955=CARTESIAN_POINT('Ctrl Pts',(-0.219075835306222,1.23262930230883,
-3.36248892666366));
#36956=CARTESIAN_POINT('Ctrl Pts',(-0.299983891499242,1.21577450743834,
-3.35780862343938));
#36957=CARTESIAN_POINT('Ctrl Pts',(-0.448065444823204,1.16915519181047,
-3.34885667158477));
#36958=CARTESIAN_POINT('Ctrl Pts',(-0.515231046729565,1.14121643349784,
-3.34460095198795));
#36959=CARTESIAN_POINT('Ctrl Pts',(-0.694686251822005,1.0467633452116,-3.33285263762908));
#36960=CARTESIAN_POINT('Ctrl Pts',(-0.799861433024963,0.968069776518021,
-3.3255077792573));
#36961=CARTESIAN_POINT('Ctrl Pts',(-0.949205482109416,0.816310659286032,
-3.31343970118704));
#36962=CARTESIAN_POINT('Ctrl Pts',(-1.00178021403193,0.75130095133304,-3.30871470497829));
#36963=CARTESIAN_POINT('Ctrl Pts',(-1.13109745576878,0.553855845839041,
-3.29514185041406));
#36964=CARTESIAN_POINT('Ctrl Pts',(-1.18954659813618,0.413603650031076,
-3.2863606214834));
#36965=CARTESIAN_POINT('Ctrl Pts',(-1.25508746532298,0.102680880205581,
-3.26828620334525));
#36966=CARTESIAN_POINT('Ctrl Pts',(-1.25831131853314,-0.0616836932186077,
-3.25921473718692));
#36967=CARTESIAN_POINT('Ctrl Pts',(-1.21839565445701,-0.287349150006394,
-3.24595615898599));
#36968=CARTESIAN_POINT('Ctrl Pts',(-1.20108917791892,-0.352751485571006,
-3.24199464006113));
#36969=CARTESIAN_POINT('Ctrl Pts',(-1.13307736316836,-0.543662137018506,
-3.23027245184088));
#36970=CARTESIAN_POINT('Ctrl Pts',(-1.06695580974336,-0.663144382443532,
-3.22265656378173));
#36971=CARTESIAN_POINT('Ctrl Pts',(-0.933540585090504,-0.834199642533942,
-3.21035259237703));
#36972=CARTESIAN_POINT('Ctrl Pts',(-0.876705080832201,-0.894150450270504,
-3.20567407636957));
#36973=CARTESIAN_POINT('Ctrl Pts',(-0.758456158600062,-0.996296398557068,
-3.19666510759818));
#36974=CARTESIAN_POINT('Ctrl Pts',(-0.698494311599007,-1.03928012010615,
-3.19235006994326));
#36975=CARTESIAN_POINT('Ctrl Pts',(-0.523367366197831,-1.14197893838959,
-3.18060044677048));
#36976=CARTESIAN_POINT('Ctrl Pts',(-0.401869693488511,-1.18960829308796,
-3.17330940046633));
#36977=CARTESIAN_POINT('Ctrl Pts',(-0.147861403149484,-1.24735560422784,
-3.15854913541049));
#36978=CARTESIAN_POINT('Ctrl Pts',(-0.0146749456347816,-1.25678959869051,
-3.15102599048014));
#36979=CARTESIAN_POINT('Ctrl Pts',(0.272063010777239,-1.22990832794888,
-3.1342070007271));
#36980=CARTESIAN_POINT('Ctrl Pts',(0.403920008211813,-1.18762497665319,
-3.12641288451799));
#36981=CARTESIAN_POINT('Ctrl Pts',(0.507833268109246,-1.14129009144715,
-3.11995951443803));
#36982=CARTESIAN_POINT('',(0.394326187196951,-0.886231714570047,-2.95835875076991));
#36983=CARTESIAN_POINT('',(0.3943262306718,-0.8862318115506,-2.958358760073));
#36984=CARTESIAN_POINT('Ctrl Pts',(0.394086490514282,-0.885697016523154,
-2.95834297351496));
#36985=CARTESIAN_POINT('Ctrl Pts',(0.298191958553152,-0.928570355423577,
-2.96609912828714));
#36986=CARTESIAN_POINT('Ctrl Pts',(0.178519160258169,-0.964221383078607,
-2.97515342193901));
#36987=CARTESIAN_POINT('Ctrl Pts',(-0.0910893742334601,-0.973481439942689,
-2.99509288425242));
#36988=CARTESIAN_POINT('Ctrl Pts',(-0.219578006005614,-0.952478120502751,
-3.00451358328581));
#36989=CARTESIAN_POINT('Ctrl Pts',(-0.459314331859836,-0.863779587384766,
-3.02338810787862));
#36990=CARTESIAN_POINT('Ctrl Pts',(-0.567630710127548,-0.796933539091375,
-3.03262261216431));
#36991=CARTESIAN_POINT('Ctrl Pts',(-0.752828485440924,-0.623184054868312,
-3.05137670238496));
#36992=CARTESIAN_POINT('Ctrl Pts',(-0.828023420909123,-0.519426122579509,
-3.06065415106238));
#36993=CARTESIAN_POINT('Ctrl Pts',(-0.94255521282042,-0.272657343323878,
-3.08075567571069));
#36994=CARTESIAN_POINT('Ctrl Pts',(-0.964576092397812,-0.146345569842894,
-3.09003837605877));
#36995=CARTESIAN_POINT('Ctrl Pts',(-0.973234758229752,0.085059333000687,
-3.10713095999206));
#36996=CARTESIAN_POINT('Ctrl Pts',(-0.954764421553844,0.20944375937905,
-3.11624459210594));
#36997=CARTESIAN_POINT('Ctrl Pts',(-0.863385541083935,0.46753846278374,
-3.13648573502703));
#36998=CARTESIAN_POINT('Ctrl Pts',(-0.787741201038068,0.574355926245695,
-3.14594494376442));
#36999=CARTESIAN_POINT('Ctrl Pts',(-0.636563258090311,0.740825101047974,
-3.16253912703327));
#37000=CARTESIAN_POINT('Ctrl Pts',(-0.538712695870463,0.815657266700886,
-3.17147840984227));
#37001=CARTESIAN_POINT('Ctrl Pts',(-0.314574481362823,0.926631232436044,
-3.18997228883889));
#37002=CARTESIAN_POINT('Ctrl Pts',(-0.187145566187846,0.959632056663,-3.19950140358805));
#37003=CARTESIAN_POINT('Ctrl Pts',(0.0437158535439797,0.973816785682933,
-3.21657049099738));
#37004=CARTESIAN_POINT('Ctrl Pts',(0.169857833048983,0.966145605389418,
-3.22571908778702));
#37005=CARTESIAN_POINT('Ctrl Pts',(0.428395654897745,0.879230744200447,
-3.24588254217937));
#37006=CARTESIAN_POINT('Ctrl Pts',(0.541693017629161,0.813745168936603,
-3.25535199002771));
#37007=CARTESIAN_POINT('Ctrl Pts',(0.734982717893058,0.645443410637272,
-3.27427218637866));
#37008=CARTESIAN_POINT('Ctrl Pts',(0.811636406380411,0.546422715832138,
-3.28335553035938));
#37009=CARTESIAN_POINT('Ctrl Pts',(0.924128601451263,0.318615613830104,
-3.30212531517517));
#37010=CARTESIAN_POINT('Ctrl Pts',(0.958033338094726,0.193919701721441,
-3.3114780528541));
#37011=CARTESIAN_POINT('Ctrl Pts',(0.978749172687539,-0.0892851067193594,
-3.33245310431301));
#37012=CARTESIAN_POINT('Ctrl Pts',(0.950086443151063,-0.216174344769085,
-3.34185474483205));
#37013=CARTESIAN_POINT('Ctrl Pts',(0.88012689003466,-0.424386369963139,
-3.35807168820761));
#37014=CARTESIAN_POINT('Ctrl Pts',(0.817947883267627,-0.535142012129366,
-3.36727185345121));
#37015=CARTESIAN_POINT('Ctrl Pts',(0.641552013655261,-0.742759599885964,
-3.38740750684635));
#37016=CARTESIAN_POINT('Ctrl Pts',(0.534674148075231,-0.815680064014305,
-3.39676783386907));
#37017=CARTESIAN_POINT('Ctrl Pts',(0.330664337416998,-0.919167120470599,
-3.41365034567614));
#37018=CARTESIAN_POINT('Ctrl Pts',(0.211227470815188,-0.954389957357228,
-3.42268045441736));
#37019=CARTESIAN_POINT('Ctrl Pts',(-0.0704569008974092,-0.980883123973585,
-3.44359987857669));
#37020=CARTESIAN_POINT('Ctrl Pts',(-0.203914130061244,-0.952161421978621,
-3.45343850897055));
#37021=CARTESIAN_POINT('Ctrl Pts',(-0.36958016759548,-0.899678213762177,
-3.46626238060016));
#37022=CARTESIAN_POINT('Ctrl Pts',(-0.490729761001405,-0.85200117158237,
-3.4756482875348));
#37023=CARTESIAN_POINT('Ctrl Pts',(-0.713516101842884,-0.669284725414487,
-3.49695224089473));
#37024=CARTESIAN_POINT('Ctrl Pts',(-0.796210772486554,-0.567271827168219,
-3.50645607377617));
#37025=CARTESIAN_POINT('Ctrl Pts',(-0.906615489405553,-0.359724464965967,
-3.52380729215184));
#37026=CARTESIAN_POINT('Ctrl Pts',(-0.950884825918708,-0.240943001075831,
-3.53298809551321));
#37027=CARTESIAN_POINT('Ctrl Pts',(-0.977297097691617,0.0296841041748267,
-3.55308261030826));
#37028=CARTESIAN_POINT('Ctrl Pts',(-0.964454925062392,0.159120292206585,
-3.56249514560412));
#37029=CARTESIAN_POINT('Ctrl Pts',(-0.891014447070674,0.40408756742219,
-3.58138007083618));
#37030=CARTESIAN_POINT('Ctrl Pts',(-0.830998255952594,0.516453374987395,
-3.59062207519904));
#37031=CARTESIAN_POINT('Ctrl Pts',(-0.669226084533194,0.712159990286071,
-3.60937318861775));
#37032=CARTESIAN_POINT('Ctrl Pts',(-0.570521723227346,0.793670410863386,
-3.61864169031169));
#37033=CARTESIAN_POINT('Ctrl Pts',(-0.331511437622609,0.923522973270035,
-3.63874084829215));
#37034=CARTESIAN_POINT('Ctrl Pts',(-0.206724568934881,0.953433421673881,
-3.64803061038475));
#37035=CARTESIAN_POINT('Ctrl Pts',(0.0234203099571745,0.976651850922853,
-3.66510410729054));
#37036=CARTESIAN_POINT('Ctrl Pts',(0.148589513594781,0.966110048972658,
-3.67420837961276));
#37037=CARTESIAN_POINT('Ctrl Pts',(0.412125331987649,0.891213160371829,
-3.69446296475668));
#37038=CARTESIAN_POINT('Ctrl Pts',(0.523612092796829,0.822292732945887,
-3.70393408344633));
#37039=CARTESIAN_POINT('Ctrl Pts',(0.698976608829793,0.682239902879797,
-3.72049547224334));
#37040=CARTESIAN_POINT('Ctrl Pts',(0.77978007351188,0.589452244916243,-3.72942491066296));
#37041=CARTESIAN_POINT('Ctrl Pts',(0.900594156247188,0.380054045915021,
-3.7473010272067));
#37042=CARTESIAN_POINT('Ctrl Pts',(0.940480498058542,0.263658903783144,
-3.75623046562625));
#37043=CARTESIAN_POINT('Ctrl Pts',(0.973957141473117,0.041742651474511,
-3.77279185442322));
#37044=CARTESIAN_POINT('Ctrl Pts',(0.977823610664811,-0.0892702241076244,
-3.7822629731128));
#37045=CARTESIAN_POINT('Ctrl Pts',(0.910762191275745,-0.354908017969238,
-3.80251755825678));
#37046=CARTESIAN_POINT('Ctrl Pts',(0.857240266408211,-0.468547195571489,
-3.8116218305791));
#37047=CARTESIAN_POINT('Ctrl Pts',(0.721949794241172,-0.656169819148452,
-3.82869532748499));
#37048=CARTESIAN_POINT('Ctrl Pts',(0.633598447246363,-0.74923128810756,
-3.83798508957765));
#37049=CARTESIAN_POINT('Ctrl Pts',(0.401554241019619,-0.891157645578996,
-3.85808424755821));
#37050=CARTESIAN_POINT('Ctrl Pts',(0.281585702576723,-0.935812425696929,
-3.86735274925221));
#37051=CARTESIAN_POINT('Ctrl Pts',(0.0311879332374879,-0.97791078465937,
-3.88610386267095));
#37052=CARTESIAN_POINT('Ctrl Pts',(-0.0961293116754427,-0.973628606025544,
-3.89534586703381));
#37053=CARTESIAN_POINT('Ctrl Pts',(-0.344962787881534,-0.914600046384474,
-3.91423079226578));
#37054=CARTESIAN_POINT('Ctrl Pts',(-0.463447383824371,-0.860933961244311,
-3.92364332756156));
#37055=CARTESIAN_POINT('Ctrl Pts',(-0.684518196277557,-0.702616766733428,
-3.94373784235656));
#37056=CARTESIAN_POINT('Ctrl Pts',(-0.765193847051333,-0.60484023738499,
-3.95291864571793));
#37057=CARTESIAN_POINT('Ctrl Pts',(-0.889615581919422,-0.405380113632132,
-3.97026986409359));
#37058=CARTESIAN_POINT('Ctrl Pts',(-0.936541938784192,-0.282730380681453,
-3.97977369697504));
#37059=CARTESIAN_POINT('Ctrl Pts',(-0.983218772209112,0.00159395276037342,
-4.00107765033499));
#37060=CARTESIAN_POINT('Ctrl Pts',(-0.963857842098935,0.13033974383224,
-4.01046355726967));
#37061=CARTESIAN_POINT('Ctrl Pts',(-0.926376886725788,0.300030347936233,
-4.02328742889928));
#37062=CARTESIAN_POINT('Ctrl Pts',(-0.884445642428363,0.429943930495125,
-4.03312605929319));
#37063=CARTESIAN_POINT('Ctrl Pts',(-0.720524154999485,0.660546877362451,
-4.05404548345253));
#37064=CARTESIAN_POINT('Ctrl Pts',(-0.63025142976455,0.746317783972133,
-4.06307559219369));
#37065=CARTESIAN_POINT('Ctrl Pts',(-0.438550717880826,0.87113929959349,
-4.07995810400068));
#37066=CARTESIAN_POINT('Ctrl Pts',(-0.32192786341835,0.92716948839055,-4.08931843102333));
#37067=CARTESIAN_POINT('Ctrl Pts',(-0.053899100625622,0.975966495244121,
-4.10945408441848));
#37068=CARTESIAN_POINT('Ctrl Pts',(0.0731066818806321,0.974362636104428,
-4.11865424966214));
#37069=CARTESIAN_POINT('Ctrl Pts',(0.288377749580686,0.930716858309793,
-4.13487119303781));
#37070=CARTESIAN_POINT('Ctrl Pts',(0.412575699626238,0.892021897374435,
-4.14427283355689));
#37071=CARTESIAN_POINT('Ctrl Pts',(0.647386542142391,0.732341035767536,
-4.16524788501576));
#37072=CARTESIAN_POINT('Ctrl Pts',(0.738370090523778,0.640577232514665,
-4.17460062269466));
#37073=CARTESIAN_POINT('Ctrl Pts',(0.879286517416562,0.429169734287967,
-4.19337040751045));
#37074=CARTESIAN_POINT('Ctrl Pts',(0.926645994771919,0.313247493699817,
-4.20245375149114));
#37075=CARTESIAN_POINT('Ctrl Pts',(0.975606909619788,0.0616740076335012,
-4.22137394784201));
#37076=CARTESIAN_POINT('Ctrl Pts',(0.975593497086551,-0.0691871890201323,
-4.23084339569034));
#37077=CARTESIAN_POINT('Ctrl Pts',(0.921437955672763,-0.336513161862343,
-4.2510068500827));
#37078=CARTESIAN_POINT('Ctrl Pts',(0.864943960511507,-0.449557730556668,
-4.26015544687236));
#37079=CARTESIAN_POINT('Ctrl Pts',(0.737115611443266,-0.642322132956235,
-4.27722453428169));
#37080=CARTESIAN_POINT('Ctrl Pts',(0.644766461351629,-0.736124144126932,
-4.28675364903085));
#37081=CARTESIAN_POINT('Ctrl Pts',(0.436509652621514,-0.874624187055261,
-4.30524752802741));
#37082=CARTESIAN_POINT('Ctrl Pts',(0.322750023297326,-0.921882332163208,
-4.31418681083635));
#37083=CARTESIAN_POINT('Ctrl Pts',(0.102966529943006,-0.969442532354417,
-4.33078099410514));
#37084=CARTESIAN_POINT('Ctrl Pts',(-0.0273693659811713,-0.981467128609303,
-4.34024020284249));
#37085=CARTESIAN_POINT('Ctrl Pts',(-0.296545998415826,-0.931398013650124,
-4.36048134576363));
#37086=CARTESIAN_POINT('Ctrl Pts',(-0.413474071476687,-0.885132858374172,
-4.36959497787757));
#37087=CARTESIAN_POINT('Ctrl Pts',(-0.609474827808156,-0.761816577731484,
-4.38668756181092));
#37088=CARTESIAN_POINT('Ctrl Pts',(-0.707805253771892,-0.679532250019475,
-4.39597026215903));
#37089=CARTESIAN_POINT('Ctrl Pts',(-0.864116564177007,-0.45686852146669,
-4.41607178680735));
#37090=CARTESIAN_POINT('Ctrl Pts',(-0.91630733566222,-0.339838139921241,
-4.42534923548476));
#37091=CARTESIAN_POINT('Ctrl Pts',(-0.974034598054683,-0.0925434525026679,
-4.44410332570542));
#37092=CARTESIAN_POINT('Ctrl Pts',(-0.977692016570372,0.0346864781869573,
-4.45333782999112));
#37093=CARTESIAN_POINT('Ctrl Pts',(-0.934490971108565,0.286628148782353,
-4.47221235458392));
#37094=CARTESIAN_POINT('Ctrl Pts',(-0.888364507480827,0.40837714169557,
-4.48163305361731));
#37095=CARTESIAN_POINT('Ctrl Pts',(-0.745406355841484,0.637150936261831,
-4.50157251205056));
#37096=CARTESIAN_POINT('Ctrl Pts',(-0.654644885472509,0.722911764031138,
-4.51062680283025));
#37097=CARTESIAN_POINT('Ctrl Pts',(-0.569532054520997,0.784472183292758,
-4.51838295576791));
#37098=CARTESIAN_POINT('Ctrl Pts',(0.9535275674129,-0.8304484356495,-2.630468105836));
#37099=CARTESIAN_POINT('Ctrl Pts',(0.7575668259831,-1.055452133727,-2.647368197028));
#37100=CARTESIAN_POINT('Ctrl Pts',(0.200611625078,-1.359698250639,-2.681168379412));
#37101=CARTESIAN_POINT('Ctrl Pts',(-0.7319692574172,-1.163512414639,-2.731868652988));
#37102=CARTESIAN_POINT('Ctrl Pts',(-1.312600153974,-0.4079672517203,-2.782568926564));
#37103=CARTESIAN_POINT('Ctrl Pts',(-1.262509073048,0.543566954962,-2.83326920014));
#37104=CARTESIAN_POINT('Ctrl Pts',(-0.6056998170625,1.233904268511,-2.883969473716));
#37105=CARTESIAN_POINT('Ctrl Pts',(0.3421771199694,1.331279463018,-2.934669747292));
#37106=CARTESIAN_POINT('Ctrl Pts',(1.125620475753,0.7889040709467,-2.985370020868));
#37107=CARTESIAN_POINT('Ctrl Pts',(1.368142054503,-0.1325826998597,-3.036070294444));
#37108=CARTESIAN_POINT('Ctrl Pts',(0.9531974730936,-0.9903562298753,-3.08677056802));
#37109=CARTESIAN_POINT('Ctrl Pts',(0.08018994585494,-1.372210064652,-3.137470841596));
#37110=CARTESIAN_POINT('Ctrl Pts',(-0.8313531810178,-1.094642760639,-3.188171115172));
#37111=CARTESIAN_POINT('Ctrl Pts',(-1.343386153806,-0.2910404234365,-3.238871388748));
#37112=CARTESIAN_POINT('Ctrl Pts',(-1.209849441198,0.6524225744844,-3.289571662324));
#37113=CARTESIAN_POINT('Ctrl Pts',(-0.4949146545354,1.282361248166,-3.3402719359));
#37114=CARTESIAN_POINT('Ctrl Pts',(0.4578533841451,1.296056003695,-3.390972209476));
#37115=CARTESIAN_POINT('Ctrl Pts',(1.190598115186,0.6869257705116,-3.441672483052));
#37116=CARTESIAN_POINT('Ctrl Pts',(1.351196075161,-0.2523094381015,-3.492372756628));
#37117=CARTESIAN_POINT('Ctrl Pts',(0.8624712606077,-1.070296319109,-3.543073030204));
#37118=CARTESIAN_POINT('Ctrl Pts',(-0.04071762923338,-1.373947946879,-3.59377330378));
#37119=CARTESIAN_POINT('Ctrl Pts',(-0.9243394967408,-1.017343295588,-3.644473577356));
#37120=CARTESIAN_POINT('Ctrl Pts',(-1.363766255618,-0.1718501819773,-3.695173850932));
#37121=CARTESIAN_POINT('Ctrl Pts',(-1.147829590707,0.7562262357563,-3.745874124508));
#37122=CARTESIAN_POINT('Ctrl Pts',(-0.3802987353604,1.320895058908,-3.796574398084));
#37123=CARTESIAN_POINT('Ctrl Pts',(0.5699861959056,1.250802378507,-3.84727467166));
#37124=CARTESIAN_POINT('Ctrl Pts',(1.246362050538,0.5796315446648,-3.897974945236));
#37125=CARTESIAN_POINT('Ctrl Pts',(1.32379313679,-0.3700836676636,-3.948675218812));
#37126=CARTESIAN_POINT('Ctrl Pts',(0.7650715766059,-1.141953368097,-3.999375492388));
#37127=CARTESIAN_POINT('Ctrl Pts',(-0.1613139710547,-1.365053843919,-4.050075765964));
#37128=CARTESIAN_POINT('Ctrl Pts',(-1.01015806052,-0.9321679759867,-4.10077603954));
#37129=CARTESIAN_POINT('Ctrl Pts',(-1.37364634578,-0.05134052539036,-4.151476313116));
#37130=CARTESIAN_POINT('Ctrl Pts',(-1.076725604129,0.8542167935132,-4.202176586692));
#37131=CARTESIAN_POINT('Ctrl Pts',(-0.5345691746706,1.184112536844,-4.235976769076));
#37132=CARTESIAN_POINT('Ctrl Pts',(-0.2416963184219,1.241145565899,-4.252876860268));
#37133=CARTESIAN_POINT('Ctrl Pts',(0.8758754583306,-0.7628194811062,-2.689919838464));
#37134=CARTESIAN_POINT('Ctrl Pts',(0.6958731069771,-0.9694996274544,-2.706819929656));
#37135=CARTESIAN_POINT('Ctrl Pts',(0.1842744825284,-1.248968953987,-2.74062011204));
#37136=CARTESIAN_POINT('Ctrl Pts',(-0.6723601191349,-1.068759839016,-2.791320385616));
#37137=CARTESIAN_POINT('Ctrl Pts',(-1.20570636944,-0.3747437575968,-2.842020659192));
#37138=CARTESIAN_POINT('Ctrl Pts',(-1.159694539302,0.4993006726617,-2.892720932768));
#37139=CARTESIAN_POINT('Ctrl Pts',(-0.5563736414247,1.133419214769,-2.943421206344));
#37140=CARTESIAN_POINT('Ctrl Pts',(0.314311355042,1.222864497773,-2.99412147992));
#37141=CARTESIAN_POINT('Ctrl Pts',(1.033953693422,0.7246583510889,-3.044821753496));
#37142=CARTESIAN_POINT('Ctrl Pts',(1.256725122589,-0.1217856063893,-3.095522027072));
#37143=CARTESIAN_POINT('Ctrl Pts',(0.8755722457931,-0.9097049171909,-3.146222300648));
#37144=CARTESIAN_POINT('Ctrl Pts',(0.07365954376103,-1.260461847542,-3.196922574224));
#37145=CARTESIAN_POINT('Ctrl Pts',(-0.7636505470253,-1.005498700247,-3.2476228478));
#37146=CARTESIAN_POINT('Ctrl Pts',(-1.233985259988,-0.2673390607487,-3.298323121376));
#37147=CARTESIAN_POINT('Ctrl Pts',(-1.111323332471,0.5992914531062,-3.349023394952));
#37148=CARTESIAN_POINT('Ctrl Pts',(-0.4546104535308,1.177930019402,-3.399723668528));
#37149=CARTESIAN_POINT('Ctrl Pts',(0.4205673295575,1.190509519655,-3.450423942104));
#37150=CARTESIAN_POINT('Ctrl Pts',(1.093639770328,0.6309848237721,-3.50112421568));
#37151=CARTESIAN_POINT('Ctrl Pts',(1.241159167361,-0.2317621978543,-3.551824489256));
#37152=CARTESIAN_POINT('Ctrl Pts',(0.7922344738614,-0.9831349518212,-3.602524762832));
#37153=CARTESIAN_POINT('Ctrl Pts',(-0.03740172113081,-1.262058202429,-3.653225036408));
#37154=CARTESIAN_POINT('Ctrl Pts',(-0.8490643669144,-0.9344942461601,-3.703925309984));
#37155=CARTESIAN_POINT('Ctrl Pts',(-1.252705674191,-0.1578552755553,-3.75462558356));
#37156=CARTESIAN_POINT('Ctrl Pts',(-1.054354172029,0.6946416899531,-3.805325857136));
#37157=CARTESIAN_POINT('Ctrl Pts',(-0.3493284730509,1.213325764945,-3.856026130712));
#37158=CARTESIAN_POINT('Ctrl Pts',(0.5235684186199,1.148941198972,-3.906726404288));
#37159=CARTESIAN_POINT('Ctrl Pts',(1.144862476522,0.5324282823029,-3.957426677864));
#37160=CARTESIAN_POINT('Ctrl Pts',(1.215987833017,-0.3399452864431,-4.00812695144));
#37161=CARTESIAN_POINT('Ctrl Pts',(0.702766695706,-1.048956489416,-4.058827225016));
#37162=CARTESIAN_POINT('Ctrl Pts',(-0.1481770985562,-1.253888405589,-4.109527498592));
#37163=CARTESIAN_POINT('Ctrl Pts',(-0.9278941527034,-0.8562553208856,-4.160227772168));
#37164=CARTESIAN_POINT('Ctrl Pts',(-1.261781162719,-0.04715952400749,-4.210928045744));
#37165=CARTESIAN_POINT('Ctrl Pts',(-0.9890406572845,0.7846522230731,-4.26162831932));
#37166=CARTESIAN_POINT('Ctrl Pts',(-0.4910356416274,1.087682355883,-4.295428501704));
#37167=CARTESIAN_POINT('Ctrl Pts',(-0.2220133752913,1.140070805017,-4.312328592896));
#37168=CARTESIAN_POINT('Ctrl Pts',(0.7982233492482,-0.6951905265629,-2.749371571093));
#37169=CARTESIAN_POINT('Ctrl Pts',(0.6341793879712,-0.8835471211815,-2.766271662285));
#37170=CARTESIAN_POINT('Ctrl Pts',(0.1679373399789,-1.138239657336,-2.800071844669));
#37171=CARTESIAN_POINT('Ctrl Pts',(-0.6127509808526,-0.9740072633923,-2.850772118245));
#37172=CARTESIAN_POINT('Ctrl Pts',(-1.098812584906,-0.3415202634732,-2.901472391821));
#37173=CARTESIAN_POINT('Ctrl Pts',(-1.056880005555,0.4550343903613,-2.952172665397));
#37174=CARTESIAN_POINT('Ctrl Pts',(-0.5070474657869,1.032934161028,-3.002872938973));
#37175=CARTESIAN_POINT('Ctrl Pts',(0.2864455901145,1.114449532528,-3.053573212549));
#37176=CARTESIAN_POINT('Ctrl Pts',(0.9422869110915,0.6604126312312,-3.104273486125));
#37177=CARTESIAN_POINT('Ctrl Pts',(1.145308190676,-0.1109885129189,-3.154973759701));
#37178=CARTESIAN_POINT('Ctrl Pts',(0.7979470184926,-0.8290536045064,-3.205674033277));
#37179=CARTESIAN_POINT('Ctrl Pts',(0.06712914166712,-1.148713630431,-3.256374306853));
#37180=CARTESIAN_POINT('Ctrl Pts',(-0.6959479130327,-0.9163546398542,-3.307074580429));
#37181=CARTESIAN_POINT('Ctrl Pts',(-1.12458436617,-0.2436376980609,-3.357774854005));
#37182=CARTESIAN_POINT('Ctrl Pts',(-1.012797223744,0.546160331728,-3.408475127581));
#37183=CARTESIAN_POINT('Ctrl Pts',(-0.4143062525262,1.073498790637,-3.459175401157));
#37184=CARTESIAN_POINT('Ctrl Pts',(0.3832812749699,1.084963035615,-3.509875674733));
#37185=CARTESIAN_POINT('Ctrl Pts',(0.9966814254686,0.5750438770327,-3.560575948309));
#37186=CARTESIAN_POINT('Ctrl Pts',(1.131122259562,-0.2112149576071,-3.611276221885));
#37187=CARTESIAN_POINT('Ctrl Pts',(0.7219976871151,-0.8959735845339,-3.661976495461));
#37188=CARTESIAN_POINT('Ctrl Pts',(-0.03408581302824,-1.150168457978,-3.712676769037));
#37189=CARTESIAN_POINT('Ctrl Pts',(-0.773789237088,-0.8516451967325,-3.763377042613));
#37190=CARTESIAN_POINT('Ctrl Pts',(-1.141645092763,-0.1438603691333,-3.814077316189));
#37191=CARTESIAN_POINT('Ctrl Pts',(-0.9608787533499,0.63305714415,-3.864777589765));
#37192=CARTESIAN_POINT('Ctrl Pts',(-0.3183582107415,1.105756470983,-3.915477863341));
#37193=CARTESIAN_POINT('Ctrl Pts',(0.4771506413343,1.047080019436,-3.966178136917));
#37194=CARTESIAN_POINT('Ctrl Pts',(1.043362902507,0.485225019941,-4.016878410493));
#37195=CARTESIAN_POINT('Ctrl Pts',(1.108182529245,-0.3098069052225,-4.067578684069));
#37196=CARTESIAN_POINT('Ctrl Pts',(0.6404618148061,-0.9559596107337,-4.118278957645));
#37197=CARTESIAN_POINT('Ctrl Pts',(-0.1350402260578,-1.142722967259,-4.168979231221));
#37198=CARTESIAN_POINT('Ctrl Pts',(-0.8456302448871,-0.7803426657845,-4.219679504797));
#37199=CARTESIAN_POINT('Ctrl Pts',(-1.149915979657,-0.04297852262462,-4.270379778373));
#37200=CARTESIAN_POINT('Ctrl Pts',(-0.9013557104398,0.715087652633,-4.321080051949));
#37201=CARTESIAN_POINT('Ctrl Pts',(-0.4475021085842,0.9912521749224,-4.354880234333));
#37202=CARTESIAN_POINT('Ctrl Pts',(-0.2023304321606,1.038996044136,-4.371780325525));
#37203=CARTESIAN_POINT('Ctrl Pts',(0.7205712401658,-0.6275615720196,-2.808823303721));
#37204=CARTESIAN_POINT('Ctrl Pts',(0.5724856689652,-0.7975946149087,-2.825723394913));
#37205=CARTESIAN_POINT('Ctrl Pts',(0.1516001974293,-1.027510360684,-2.859523577297));
#37206=CARTESIAN_POINT('Ctrl Pts',(-0.5531418425703,-0.879254687769,-2.910223850873));
#37207=CARTESIAN_POINT('Ctrl Pts',(-0.9919188003728,-0.3082967693496,-2.960924124449));
#37208=CARTESIAN_POINT('Ctrl Pts',(-0.9540654718091,0.4107681080609,-3.011624398025));
#37209=CARTESIAN_POINT('Ctrl Pts',(-0.4577212901491,0.9324491072861,-3.062324671601));
#37210=CARTESIAN_POINT('Ctrl Pts',(0.2585798251871,1.006034567282,-3.113024945177));
#37211=CARTESIAN_POINT('Ctrl Pts',(0.8506201287607,0.5961669113734,-3.163725218753));
#37212=CARTESIAN_POINT('Ctrl Pts',(1.033891258762,-0.1001914194485,-3.214425492329));
#37213=CARTESIAN_POINT('Ctrl Pts',(0.7203217911921,-0.7484022918219,-3.265125765905));
#37214=CARTESIAN_POINT('Ctrl Pts',(0.06059873957321,-1.03696541332,-3.315826039481));
#37215=CARTESIAN_POINT('Ctrl Pts',(-0.6282452790402,-0.8272105794617,-3.366526313057));
#37216=CARTESIAN_POINT('Ctrl Pts',(-1.015183472352,-0.2199363353731,-3.417226586633));
#37217=CARTESIAN_POINT('Ctrl Pts',(-0.914271115017,0.4930292103498,-3.467926860209));
#37218=CARTESIAN_POINT('Ctrl Pts',(-0.3740020515216,0.969067561873,-3.518627133785));
#37219=CARTESIAN_POINT('Ctrl Pts',(0.3459952203822,0.9794165515745,-3.569327407361));
#37220=CARTESIAN_POINT('Ctrl Pts',(0.8997230806097,0.5191029302932,-3.620027680937));
#37221=CARTESIAN_POINT('Ctrl Pts',(1.021085351762,-0.1906677173599,-3.670727954513));
#37222=CARTESIAN_POINT('Ctrl Pts',(0.6517609003688,-0.8088122172466,-3.721428228089));
#37223=CARTESIAN_POINT('Ctrl Pts',(-0.03076990492567,-1.038278713527,-3.772128501665));
#37224=CARTESIAN_POINT('Ctrl Pts',(-0.6985141072616,-0.7687961473049,-3.822828775241));
#37225=CARTESIAN_POINT('Ctrl Pts',(-1.030584511335,-0.1298654627114,-3.873529048817));
#37226=CARTESIAN_POINT('Ctrl Pts',(-0.8674033346712,0.5714725983469,-3.924229322393));
#37227=CARTESIAN_POINT('Ctrl Pts',(-0.287387948432,0.9981871770197,-3.974929595969));
#37228=CARTESIAN_POINT('Ctrl Pts',(0.4307328640486,0.9452188399008,-4.025629869545));
#37229=CARTESIAN_POINT('Ctrl Pts',(0.9418633284912,0.4380217575791,-4.076330143121));
#37230=CARTESIAN_POINT('Ctrl Pts',(1.000377225472,-0.2796685240019,-4.127030416697));
#37231=CARTESIAN_POINT('Ctrl Pts',(0.5781569339062,-0.8629627320519,-4.177730690273));
#37232=CARTESIAN_POINT('Ctrl Pts',(-0.1219033535594,-1.031557528929,-4.228430963849));
#37233=CARTESIAN_POINT('Ctrl Pts',(-0.7633663370709,-0.7044300106834,-4.279131237425));
#37234=CARTESIAN_POINT('Ctrl Pts',(-1.038050796595,-0.03879752124175,-4.329831511001));
#37235=CARTESIAN_POINT('Ctrl Pts',(-0.813670763595,0.6455230821929,-4.380531784577));
#37236=CARTESIAN_POINT('Ctrl Pts',(-0.4039685755409,0.8948219939615,-4.414331966961));
#37237=CARTESIAN_POINT('Ctrl Pts',(-0.1826474890299,0.9379212832541,-4.431232058153));
#37238=CARTESIAN_POINT('',(0.507887874041584,-1.14145688922471,-2.67039241379527));
#37239=CARTESIAN_POINT('Ctrl Pts',(0.507787909469119,-1.14128017477199,
-2.6700583582432));
#37240=CARTESIAN_POINT('Ctrl Pts',(0.430345474071355,-1.17582998645329,
-2.67495591326481));
#37241=CARTESIAN_POINT('Ctrl Pts',(0.349428371731934,-1.20267898189871,
-2.67984218562302));
#37242=CARTESIAN_POINT('Ctrl Pts',(0.184938905475354,-1.23906261135245,
-2.68944881298632));
#37243=CARTESIAN_POINT('Ctrl Pts',(0.102310644116143,-1.24862692557046,
-2.69408879403421));
#37244=CARTESIAN_POINT('Ctrl Pts',(-0.0377210139794821,-1.25032976147046,
-2.7020683174102));
#37245=CARTESIAN_POINT('Ctrl Pts',(-0.094059933784565,-1.24715139756305,
-2.70529937078892));
#37246=CARTESIAN_POINT('Ctrl Pts',(-0.308267034047177,-1.22069996486095,
-2.71773100546558));
#37247=CARTESIAN_POINT('Ctrl Pts',(-0.46323804104122,-1.17121720337973,
-2.72703107911372));
#37248=CARTESIAN_POINT('Ctrl Pts',(-0.672084377225763,-1.05687339674042,
-2.74061849897817));
#37249=CARTESIAN_POINT('Ctrl Pts',(-0.736631740802832,-1.0129562977045,
-2.74498450329827));
#37250=CARTESIAN_POINT('Ctrl Pts',(-0.860062651533776,-0.910226860245701,
-2.75414203962238));
#37251=CARTESIAN_POINT('Ctrl Pts',(-0.917846632144435,-0.851459146178509,
-2.75886595102978));
#37252=CARTESIAN_POINT('Ctrl Pts',(-1.06655239892433,-0.667895772520611,
-2.77250428977867));
#37253=CARTESIAN_POINT('Ctrl Pts',(-1.14207490333669,-0.530236824079974,
-2.78145769204167));
#37254=CARTESIAN_POINT('Ctrl Pts',(-1.21457005475945,-0.306572310540857,
-2.79479482811465));
#37255=CARTESIAN_POINT('Ctrl Pts',(-1.23157071309401,-0.227763492778128,
-2.79932084856198));
#37256=CARTESIAN_POINT('Ctrl Pts',(-1.25941838893502,0.0125005131581018,
-2.81317763140942));
#37257=CARTESIAN_POINT('Ctrl Pts',(-1.24693178471565,0.176576540746456,
-2.82258473910004));
#37258=CARTESIAN_POINT('Ctrl Pts',(-1.1841615241506,0.406933361119969,-2.8362949159062));
#37259=CARTESIAN_POINT('Ctrl Pts',(-1.15687979077424,0.479766542899355,
-2.84069774142107));
#37260=CARTESIAN_POINT('Ctrl Pts',(-1.04698062949429,0.704023621238008,
-2.85481790222142));
#37261=CARTESIAN_POINT('Ctrl Pts',(-0.942854924895815,0.833437644084537,
-2.86426235362398));
#37262=CARTESIAN_POINT('Ctrl Pts',(-0.766217344968764,0.99004602720095,
-2.87789669534409));
#37263=CARTESIAN_POINT('Ctrl Pts',(-0.699515492219252,1.03860857285202,
-2.8826304404166));
#37264=CARTESIAN_POINT('Ctrl Pts',(-0.560312387087706,1.12016176874203,
-2.89184314967875));
#37265=CARTESIAN_POINT('Ctrl Pts',(-0.488709702220395,1.15327292383292,
-2.89625397165448));
#37266=CARTESIAN_POINT('Ctrl Pts',(-0.267376405963998,1.23032185121952,
-2.90959982294864));
#37267=CARTESIAN_POINT('Ctrl Pts',(-0.111255966138179,1.25355040542599,
-2.91861580960043));
#37268=CARTESIAN_POINT('Ctrl Pts',(0.207811766416421,1.2430813478547,-2.93702646035043));
#37269=CARTESIAN_POINT('Ctrl Pts',(0.365890893482803,1.20689167074436,-2.94595727210507));
#37270=CARTESIAN_POINT('Ctrl Pts',(0.66246547575248,1.07105294148954,-2.96463369266693));
#37271=CARTESIAN_POINT('Ctrl Pts',(0.795390494780788,0.976179148988214,
-2.97397058103383));
#37272=CARTESIAN_POINT('Ctrl Pts',(1.01906706662552,0.742059658066752,-2.99257707154));
#37273=CARTESIAN_POINT('Ctrl Pts',(1.10593290745587,0.604765495264961,-3.00150243713672));
#37274=CARTESIAN_POINT('Ctrl Pts',(1.22268749271409,0.301608920291551,-3.02018667806096));
#37275=CARTESIAN_POINT('Ctrl Pts',(1.25191342090965,0.139437458052851,-3.02960093321319));
#37276=CARTESIAN_POINT('Ctrl Pts',(1.24721623296255,-0.179028670469711,
-3.04780586454829));
#37277=CARTESIAN_POINT('Ctrl Pts',(1.21539049696997,-0.330706345188818,
-3.05637607013176));
#37278=CARTESIAN_POINT('Ctrl Pts',(1.09215941669519,-0.62701970757549,-3.07489627414963));
#37279=CARTESIAN_POINT('Ctrl Pts',(1.00108185129908,-0.765207162330717,
-3.08433677338233));
#37280=CARTESIAN_POINT('Ctrl Pts',(0.833365504294956,-0.934835618383368,
-3.09787786040257));
#37281=CARTESIAN_POINT('Ctrl Pts',(0.775086564049311,-0.983541309444154,
-3.1021282893586));
#37282=CARTESIAN_POINT('Ctrl Pts',(0.648015857718714,-1.07117841812588,
-3.11094391137086));
#37283=CARTESIAN_POINT('Ctrl Pts',(0.579365773160173,-1.10951676907334,
-3.11545488387097));
#37284=CARTESIAN_POINT('Ctrl Pts',(0.507823374560588,-1.14126439449584,
-3.11997532266811));
#37285=CARTESIAN_POINT('',(0.394326187104466,-0.886231714415119,-2.83167491439397));
#37286=CARTESIAN_POINT('Ctrl Pts',(0.394086384346302,-0.885697063989625,
-2.83165913284815));
#37287=CARTESIAN_POINT('Ctrl Pts',(0.298191870090869,-0.928570381426029,
-2.83941528578584));
#37288=CARTESIAN_POINT('Ctrl Pts',(0.178519107793232,-0.964221384880582,
-2.84846957656523));
#37289=CARTESIAN_POINT('Ctrl Pts',(-0.0910893742334462,-0.97348143994269,
-2.86840903499846));
#37290=CARTESIAN_POINT('Ctrl Pts',(-0.219578006005599,-0.952478120502755,
-2.87782973403179));
#37291=CARTESIAN_POINT('Ctrl Pts',(-0.459314331859824,-0.863779587384772,
-2.89670425862456));
#37292=CARTESIAN_POINT('Ctrl Pts',(-0.567630710127538,-0.796933539091381,
-2.90593876291026));
#37293=CARTESIAN_POINT('Ctrl Pts',(-0.752828485440917,-0.623184054868321,
-2.92469285313095));
#37294=CARTESIAN_POINT('Ctrl Pts',(-0.828023420909118,-0.519426122579518,
-2.93397030180843));
#37295=CARTESIAN_POINT('Ctrl Pts',(-0.942555212820417,-0.272657343323888,
-2.95407182645678));
#37296=CARTESIAN_POINT('Ctrl Pts',(-0.964576092397811,-0.146345569842905,
-2.96335452680482));
#37297=CARTESIAN_POINT('Ctrl Pts',(-0.973234758229753,0.085059333000677,
-2.98044711073806));
#37298=CARTESIAN_POINT('Ctrl Pts',(-0.954764421553846,0.209443759379039,
-2.98956074285187));
#37299=CARTESIAN_POINT('Ctrl Pts',(-0.863385541083941,0.467538462783729,
-3.00980188577291));
#37300=CARTESIAN_POINT('Ctrl Pts',(-0.787741201038076,0.574355926245684,
-3.01926109451035));
#37301=CARTESIAN_POINT('Ctrl Pts',(-0.636563258090323,0.740825101047964,
-3.03585527777922));
#37302=CARTESIAN_POINT('Ctrl Pts',(-0.538712695870475,0.815657266700878,
-3.04479456058827));
#37303=CARTESIAN_POINT('Ctrl Pts',(-0.314574481362839,0.926631232436039,
-3.06328843958487));
#37304=CARTESIAN_POINT('Ctrl Pts',(-0.187145566187865,0.959632056662996,
-3.07281755433396));
#37305=CARTESIAN_POINT('Ctrl Pts',(0.0437158535439579,0.973816785682934,
-3.08988664174321));
#37306=CARTESIAN_POINT('Ctrl Pts',(0.169857833048961,0.966145605389422,
-3.09903523853281));
#37307=CARTESIAN_POINT('Ctrl Pts',(0.428395654897726,0.879230744200456,
-3.11919869292516));
#37308=CARTESIAN_POINT('Ctrl Pts',(0.541693017629146,0.813745168936613,
-3.12866814077356));
#37309=CARTESIAN_POINT('Ctrl Pts',(0.734982717893037,0.645443410637293,
-3.14758833712456));
#37310=CARTESIAN_POINT('Ctrl Pts',(0.811636406380394,0.546422715832165,
-3.1566716811053));
#37311=CARTESIAN_POINT('Ctrl Pts',(0.924128601451255,0.318615613830126,
-3.17544146592106));
#37312=CARTESIAN_POINT('Ctrl Pts',(0.958033338094721,0.193919701721466,
-3.18479420359993));
#37313=CARTESIAN_POINT('Ctrl Pts',(0.97874917268754,-0.089285106719314,
-3.20576925505879));
#37314=CARTESIAN_POINT('Ctrl Pts',(0.950086443151077,-0.216174344769035,
-3.21517089557785));
#37315=CARTESIAN_POINT('Ctrl Pts',(0.880126890034671,-0.424386369963116,
-3.23138783895344));
#37316=CARTESIAN_POINT('Ctrl Pts',(0.81794788326764,-0.535142012129345,
-3.24058800419709));
#37317=CARTESIAN_POINT('Ctrl Pts',(0.641552013655281,-0.742759599885946,
-3.26072365759223));
#37318=CARTESIAN_POINT('Ctrl Pts',(0.534674148075254,-0.81568006401429,
-3.27008398461488));
#37319=CARTESIAN_POINT('Ctrl Pts',(0.330664337417023,-0.91916712047059,
-3.28696649642188));
#37320=CARTESIAN_POINT('Ctrl Pts',(0.211227470815213,-0.954389957357222,
-3.29599660516303));
#37321=CARTESIAN_POINT('Ctrl Pts',(-0.070456900897414,-0.98088312397359,
-3.31691602932236));
#37322=CARTESIAN_POINT('Ctrl Pts',(-0.203914130061255,-0.952161421978616,
-3.32675465971631));
#37323=CARTESIAN_POINT('Ctrl Pts',(-0.369580167595495,-0.899678213762173,
-3.33957853134598));
#37324=CARTESIAN_POINT('Ctrl Pts',(-0.490729761001413,-0.852001171582361,
-3.34896443828069));
#37325=CARTESIAN_POINT('Ctrl Pts',(-0.713516101842874,-0.669284725414497,
-3.37026839164066));
#37326=CARTESIAN_POINT('Ctrl Pts',(-0.796210772486546,-0.567271827168231,
-3.37977222452207));
#37327=CARTESIAN_POINT('Ctrl Pts',(-0.906615489405549,-0.359724464965979,
-3.39712344289772));
#37328=CARTESIAN_POINT('Ctrl Pts',(-0.950884825918705,-0.240943001075843,
-3.4063042462591));
#37329=CARTESIAN_POINT('Ctrl Pts',(-0.977297097691617,0.0296841041748129,
-3.42639876105417));
#37330=CARTESIAN_POINT('Ctrl Pts',(-0.964454925062395,0.159120292206572,
-3.43581129635004));
#37331=CARTESIAN_POINT('Ctrl Pts',(-0.891014447070679,0.404087567422178,
-3.45469622158211));
#37332=CARTESIAN_POINT('Ctrl Pts',(-0.830998255952601,0.516453374987384,
-3.46393822594497));
#37333=CARTESIAN_POINT('Ctrl Pts',(-0.669226084533204,0.712159990286062,
-3.48268933936367));
#37334=CARTESIAN_POINT('Ctrl Pts',(-0.570521723227356,0.793670410863379,
-3.49195784105761));
#37335=CARTESIAN_POINT('Ctrl Pts',(-0.331511437622619,0.923522973270032,
-3.51205699903807));
#37336=CARTESIAN_POINT('Ctrl Pts',(-0.20672456893489,0.953433421673878,
-3.52134676113068));
#37337=CARTESIAN_POINT('Ctrl Pts',(0.0234203099571636,0.976651850922853,
-3.5384202580365));
#37338=CARTESIAN_POINT('Ctrl Pts',(0.148589513594771,0.96611004897266,-3.54752453035876));
#37339=CARTESIAN_POINT('Ctrl Pts',(0.412125331987641,0.891213160371833,
-3.56777911550269));
#37340=CARTESIAN_POINT('Ctrl Pts',(0.523612092796821,0.822292732945892,
-3.57725023419229));
#37341=CARTESIAN_POINT('Ctrl Pts',(0.69897660882979,0.682239902879801,-3.5938116229893));
#37342=CARTESIAN_POINT('Ctrl Pts',(0.77978007351188,0.589452244916244,-3.60274106140891));
#37343=CARTESIAN_POINT('Ctrl Pts',(0.90059415624719,0.380054045915018,-3.62061717795275));
#37344=CARTESIAN_POINT('Ctrl Pts',(0.940480498058544,0.263658903783137,
-3.62954661637244));
#37345=CARTESIAN_POINT('Ctrl Pts',(0.973957141473118,0.0417426514745017,
-3.64610800516952));
#37346=CARTESIAN_POINT('Ctrl Pts',(0.97782361066481,-0.0892702241076332,
-3.65557912385921));
#37347=CARTESIAN_POINT('Ctrl Pts',(0.910762191275743,-0.354908017969242,
-3.67583370900311));
#37348=CARTESIAN_POINT('Ctrl Pts',(0.857240266408209,-0.468547195571491,
-3.68493798132528));
#37349=CARTESIAN_POINT('Ctrl Pts',(0.721949794241174,-0.65616981914845,
-3.70201147823101));
#37350=CARTESIAN_POINT('Ctrl Pts',(0.633598447246369,-0.749231288107553,
-3.71130124032356));
#37351=CARTESIAN_POINT('Ctrl Pts',(0.401554241019639,-0.891157645578987,
-3.73140039830393));
#37352=CARTESIAN_POINT('Ctrl Pts',(0.28158570257675,-0.93581242569692,-3.74066889999782));
#37353=CARTESIAN_POINT('Ctrl Pts',(0.031187933237524,-0.977910784659368,
-3.75942001341647));
#37354=CARTESIAN_POINT('Ctrl Pts',(-0.0961293116754024,-0.973628606025547,
-3.7686620177793));
#37355=CARTESIAN_POINT('Ctrl Pts',(-0.344962787881492,-0.914600046384491,
-3.7875469430114));
#37356=CARTESIAN_POINT('Ctrl Pts',(-0.463447383824335,-0.860933961244331,
-3.79695947830734));
#37357=CARTESIAN_POINT('Ctrl Pts',(-0.684518196277534,-0.702616766733451,
-3.81705399310246));
#37358=CARTESIAN_POINT('Ctrl Pts',(-0.765193847051316,-0.604840237385012,
-3.82623479646385));
#37359=CARTESIAN_POINT('Ctrl Pts',(-0.889615581919413,-0.405380113632151,
-3.84358601483951));
#37360=CARTESIAN_POINT('Ctrl Pts',(-0.936541938784186,-0.282730380681472,
-3.85308984772092));
#37361=CARTESIAN_POINT('Ctrl Pts',(-0.983218772209115,0.00159395276037214,
-3.87439380108085));
#37362=CARTESIAN_POINT('Ctrl Pts',(-0.963857842098933,0.13033974383224,
-3.88377970801553));
#37363=CARTESIAN_POINT('Ctrl Pts',(-0.926376886725791,0.30003034793623,
-3.89660357964515));
#37364=CARTESIAN_POINT('Ctrl Pts',(-0.884445642428363,0.429943930495119,
-3.90644221003906));
#37365=CARTESIAN_POINT('Ctrl Pts',(-0.720524154999497,0.660546877362438,
-3.92736163419847));
#37366=CARTESIAN_POINT('Ctrl Pts',(-0.630251429764562,0.746317783972123,
-3.9363917429397));
#37367=CARTESIAN_POINT('Ctrl Pts',(-0.43855071788084,0.871139299593482,
-3.95327425474676));
#37368=CARTESIAN_POINT('Ctrl Pts',(-0.321927863418365,0.927169488390545,
-3.96263458176947));
#37369=CARTESIAN_POINT('Ctrl Pts',(-0.0538991006256375,0.97596649524412,
-3.98277023516459));
#37370=CARTESIAN_POINT('Ctrl Pts',(0.0731066818806159,0.974362636104429,
-3.99197040040816));
#37371=CARTESIAN_POINT('Ctrl Pts',(0.288377749580642,0.930716858309803,
-4.00818734378377));
#37372=CARTESIAN_POINT('Ctrl Pts',(0.412575699626203,0.892021897374454,
-4.01758898430277));
#37373=CARTESIAN_POINT('Ctrl Pts',(0.647386542142373,0.732341035767552,
-4.03856403576163));
#37374=CARTESIAN_POINT('Ctrl Pts',(0.738370090523761,0.640577232514683,
-4.04791677344056));
#37375=CARTESIAN_POINT('Ctrl Pts',(0.879286517416555,0.429169734287984,
-4.0666865582564));
#37376=CARTESIAN_POINT('Ctrl Pts',(0.926645994771913,0.313247493699832,
-4.07576990223715));
#37377=CARTESIAN_POINT('Ctrl Pts',(0.975606909619787,0.0616740076335164,
-4.09469009858811));
#37378=CARTESIAN_POINT('Ctrl Pts',(0.975593497086552,-0.0691871890201205,
-4.10415954643651));
#37379=CARTESIAN_POINT('Ctrl Pts',(0.921437955672765,-0.336513161862337,
-4.12432300082888));
#37380=CARTESIAN_POINT('Ctrl Pts',(0.86494396051151,-0.449557730556663,
-4.13347159761848));
#37381=CARTESIAN_POINT('Ctrl Pts',(0.737115611443269,-0.642322132956231,
-4.15054068502775));
#37382=CARTESIAN_POINT('Ctrl Pts',(0.644766461351634,-0.736124144126927,
-4.16006979977683));
#37383=CARTESIAN_POINT('Ctrl Pts',(0.436509652621522,-0.874624187055258,
-4.17856367877346));
#37384=CARTESIAN_POINT('Ctrl Pts',(0.322750023297333,-0.921882332163206,
-4.18750296158255));
#37385=CARTESIAN_POINT('Ctrl Pts',(0.102966529943014,-0.969442532354416,
-4.20409714485148));
#37386=CARTESIAN_POINT('Ctrl Pts',(-0.0273693659811663,-0.981467128609304,
-4.21355635358899));
#37387=CARTESIAN_POINT('Ctrl Pts',(-0.296545998415822,-0.931398013650125,
-4.23379749651006));
#37388=CARTESIAN_POINT('Ctrl Pts',(-0.413474071476682,-0.885132858374174,
-4.24291112862382));
#37389=CARTESIAN_POINT('Ctrl Pts',(-0.609474827808149,-0.761816577731489,
-4.26000371255701));
#37390=CARTESIAN_POINT('Ctrl Pts',(-0.707805253771882,-0.679532250019484,
-4.26928641290498));
#37391=CARTESIAN_POINT('Ctrl Pts',(-0.864116564176997,-0.45686852146671,
-4.28938793755327));
#37392=CARTESIAN_POINT('Ctrl Pts',(-0.916307335662212,-0.339838139921263,
-4.29866538623074));
#37393=CARTESIAN_POINT('Ctrl Pts',(-0.974034598054681,-0.0925434525026932,
-4.31741947645142));
#37394=CARTESIAN_POINT('Ctrl Pts',(-0.977692016570374,0.0346864781869331,
-4.32665398073712));
#37395=CARTESIAN_POINT('Ctrl Pts',(-0.934490971108571,0.286628148782332,
-4.3455285053299));
#37396=CARTESIAN_POINT('Ctrl Pts',(-0.888364507480836,0.40837714169555,
-4.35494920436324));
#37397=CARTESIAN_POINT('Ctrl Pts',(-0.745406328022297,0.637150980780467,
-4.3748886666766));
#37398=CARTESIAN_POINT('Ctrl Pts',(-0.654644818685211,0.722911827601264,
-4.38394296032879));
#37399=CARTESIAN_POINT('Ctrl Pts',(-0.569531960289745,0.784472251448342,
-4.39169911510096));
#37400=CARTESIAN_POINT('',(0.5081523591131,-1.142051303545,-2.670016835446));
#37401=CARTESIAN_POINT('Ctrl Pts',(-0.5744373942835,0.7635955204679,-1.35880161274));
#37402=CARTESIAN_POINT('Ctrl Pts',(-0.3942519210863,0.8991453907025,-1.375701703932));
#37403=CARTESIAN_POINT('Ctrl Pts',(0.06522221406019,1.036583920368,-1.409501886316));
#37404=CARTESIAN_POINT('Ctrl Pts',(0.7237741231913,0.74512128044,-1.460202159892));
#37405=CARTESIAN_POINT('Ctrl Pts',(1.034330285883,0.09544979952193,-1.510902433468));
#37406=CARTESIAN_POINT('Ctrl Pts',(0.8478838926151,-0.6000535540617,-1.561602707044));
#37407=CARTESIAN_POINT('Ctrl Pts',(0.2539702938632,-1.007208621374,-1.61230298062));
#37408=CARTESIAN_POINT('Ctrl Pts',(-0.46198624017,-0.9303428349025,-1.663003254196));
#37409=CARTESIAN_POINT('Ctrl Pts',(-0.955934349857,-0.4063977219828,-1.713703527772));
#37410=CARTESIAN_POINT('Ctrl Pts',(-0.9905040632336,0.3128436609437,-1.764403801348));
#37411=CARTESIAN_POINT('Ctrl Pts',(-0.5490830845512,0.8817466980546,-1.815104074924));
#37412=CARTESIAN_POINT('Ctrl Pts',(0.1562020238423,1.026922783566,-1.8658043485));
#37413=CARTESIAN_POINT('Ctrl Pts',(0.7864236089275,0.6786069412635,-1.916504622076));
#37414=CARTESIAN_POINT('Ctrl Pts',(1.038726128586,0.004183771769307,-1.967204895652));
#37415=CARTESIAN_POINT('Ctrl Pts',(0.7918645782425,-0.6722499265432,-2.017905169228));
#37416=CARTESIAN_POINT('Ctrl Pts',(0.1644692813081,-1.025631185916,-2.068605442804));
#37417=CARTESIAN_POINT('Ctrl Pts',(-0.541962398324,-0.8861412036624,-2.11930571638));
#37418=CARTESIAN_POINT('Ctrl Pts',(-0.9879518411537,-0.3208124585826,-2.170005989956));
#37419=CARTESIAN_POINT('Ctrl Pts',(-0.9591770048575,0.3986840194666,-2.220706263532));
#37420=CARTESIAN_POINT('Ctrl Pts',(-0.4694657541443,0.9265912689544,-2.271406537108));
#37421=CARTESIAN_POINT('Ctrl Pts',(0.2458491758444,1.009221312076,-2.322106810684));
#37422=CARTESIAN_POINT('Ctrl Pts',(0.8430202836683,0.6068659452285,-2.37280708426));
#37423=CARTESIAN_POINT('Ctrl Pts',(1.035074561878,-0.08712132208854,-2.423507357836));
#37424=CARTESIAN_POINT('Ctrl Pts',(0.7297195473129,-0.7392420834405,-2.474207631412));
#37425=CARTESIAN_POINT('Ctrl Pts',(0.07369482757466,-1.036117052103,-2.524907904988));
#37426=CARTESIAN_POINT('Ctrl Pts',(-0.6177442188356,-0.8350817538242,-2.575608178564));
#37427=CARTESIAN_POINT('Ctrl Pts',(-1.01232385091,-0.2327445177605,-2.62630845214));
#37428=CARTESIAN_POINT('Ctrl Pts',(-0.9204268188452,0.4814390384163,-2.677008725716));
#37429=CARTESIAN_POINT('Ctrl Pts',(-0.3862161132211,0.9642651248607,-2.727708999292));
#37430=CARTESIAN_POINT('Ctrl Pts',(0.3335967262064,0.9837096051999,-2.778409272868));
#37431=CARTESIAN_POINT('Ctrl Pts',(0.8930818486504,0.5304287097581,-2.829109546444));
#37432=CARTESIAN_POINT('Ctrl Pts',(1.023454253376,-0.1777529049358,-2.87980982002));
#37433=CARTESIAN_POINT('Ctrl Pts',(0.6617724011872,-0.8005107433383,-2.930510093596));
#37434=CARTESIAN_POINT('Ctrl Pts',(0.209209682755,-0.9592331935163,-2.96431027598));
#37435=CARTESIAN_POINT('Ctrl Pts',(-0.01623630497839,-0.9554019160702,-2.981210367172));
#37436=CARTESIAN_POINT('Ctrl Pts',(-0.6363414402896,0.8458841261532,-1.418253345368));
#37437=CARTESIAN_POINT('Ctrl Pts',(-0.4367383422416,0.9960414810095,-1.43515343656));
#37438=CARTESIAN_POINT('Ctrl Pts',(0.07225086327415,1.148291026024,-1.468953618944));
#37439=CARTESIAN_POINT('Ctrl Pts',(0.8017713898489,0.825419016074,-1.51965389252));
#37440=CARTESIAN_POINT('Ctrl Pts',(1.145794529402,0.10573591397,-1.570354166096));
#37441=CARTESIAN_POINT('Ctrl Pts',(0.9392558054095,-0.664718116617,-1.621054439672));
#37442=CARTESIAN_POINT('Ctrl Pts',(0.2813393142507,-1.11575010815,-1.671754713248));
#37443=CARTESIAN_POINT('Ctrl Pts',(-0.5117720266635,-1.030600906933,-1.722454986824));
#37444=CARTESIAN_POINT('Ctrl Pts',(-1.058950282596,-0.4501930311474,-1.7731552604));
#37445=CARTESIAN_POINT('Ctrl Pts',(-1.097245389111,0.3465571492585,-1.823855533976));
#37446=CARTESIAN_POINT('Ctrl Pts',(-0.6082548321872,0.9767678242997,-1.874555807552));
#37447=CARTESIAN_POINT('Ctrl Pts',(0.1730350806147,1.137588760174,-1.925256081128));
#37448=CARTESIAN_POINT('Ctrl Pts',(0.8711722756261,0.7517367822698,-1.975956354704));
#37449=CARTESIAN_POINT('Ctrl Pts',(1.150664088565,0.004634634478914,-2.02665662828));
#37450=CARTESIAN_POINT('Ctrl Pts',(0.877199589107,-0.7446947060692,-2.077356901856));
#37451=CARTESIAN_POINT('Ctrl Pts',(0.1821932562059,-1.136157973952,-2.128057175432));
#37452=CARTESIAN_POINT('Ctrl Pts',(-0.6003667876853,-0.9816359022759,-2.178757449008));
#37453=CARTESIAN_POINT('Ctrl Pts',(-1.094418127707,-0.3553847016034,-2.229457722584));
#37454=CARTESIAN_POINT('Ctrl Pts',(-1.062542381185,0.4416480641625,-2.28015799616));
#37455=CARTESIAN_POINT('Ctrl Pts',(-0.5200575678599,1.026445054786,-2.330858269736));
#37456=CARTESIAN_POINT('Ctrl Pts',(0.2723430267731,1.117979695766,-2.381558543312));
#37457=CARTESIAN_POINT('Ctrl Pts',(0.933868071336,0.6722646427485,-2.432258816888));
#37458=CARTESIAN_POINT('Ctrl Pts',(1.146619012041,-0.09650992106268,-2.482959090464));
#37459=CARTESIAN_POINT('Ctrl Pts',(0.8083575205332,-0.8189062494547,-2.53365936404));
#37460=CARTESIAN_POINT('Ctrl Pts',(0.08163652503724,-1.147773845863,-2.584359637616));
#37461=CARTESIAN_POINT('Ctrl Pts',(-0.6843152097275,-0.9250740485843,-2.635059911192));
#37462=CARTESIAN_POINT('Ctrl Pts',(-1.121416578618,-0.2578261497687,-2.685760184768));
#37463=CARTESIAN_POINT('Ctrl Pts',(-1.019616294854,0.5333211489471,-2.736460458344));
#37464=CARTESIAN_POINT('Ctrl Pts',(-0.4278365583367,1.068178820671,-2.78716073192));
#37465=CARTESIAN_POINT('Ctrl Pts',(0.3695466613813,1.089718728671,-2.837861005496));
#37466=CARTESIAN_POINT('Ctrl Pts',(0.9893245034571,0.5875901751825,-2.888561279072));
#37467=CARTESIAN_POINT('Ctrl Pts',(1.133746445034,-0.1969083849139,-2.939261552648));
#37468=CARTESIAN_POINT('Ctrl Pts',(0.7330880738372,-0.8867775051772,-2.989961826224));
#37469=CARTESIAN_POINT('Ctrl Pts',(0.2317550914541,-1.062604624995,-3.023762008608));
#37470=CARTESIAN_POINT('Ctrl Pts',(-0.01798600473741,-1.058360471267,-3.0406620998));
#37471=CARTESIAN_POINT('Ctrl Pts',(-0.6982454862957,0.9281727318386,-1.477705077996));
#37472=CARTESIAN_POINT('Ctrl Pts',(-0.479224763397,1.092937571317,-1.494605169188));
#37473=CARTESIAN_POINT('Ctrl Pts',(0.07927951248811,1.259998131679,-1.528405351572));
#37474=CARTESIAN_POINT('Ctrl Pts',(0.8797686565066,0.905716751708,-1.579105625148));
#37475=CARTESIAN_POINT('Ctrl Pts',(1.257258772921,0.1160220284182,-1.629805898724));
#37476=CARTESIAN_POINT('Ctrl Pts',(1.030627718204,-0.7293826791723,-1.6805061723));
#37477=CARTESIAN_POINT('Ctrl Pts',(0.3087083346382,-1.224291594926,-1.731206445876));
#37478=CARTESIAN_POINT('Ctrl Pts',(-0.561557813157,-1.130858978964,-1.781906719452));
#37479=CARTESIAN_POINT('Ctrl Pts',(-1.161966215335,-0.4939883403121,-1.832606993028));
#37480=CARTESIAN_POINT('Ctrl Pts',(-1.203986714989,0.3802706375734,-1.883307266604));
#37481=CARTESIAN_POINT('Ctrl Pts',(-0.6674265798232,1.071788950545,-1.93400754018));
#37482=CARTESIAN_POINT('Ctrl Pts',(0.1898681373872,1.248254736783,-1.984707813756));
#37483=CARTESIAN_POINT('Ctrl Pts',(0.9559209423246,0.8248666232761,-2.035408087332));
#37484=CARTESIAN_POINT('Ctrl Pts',(1.262602048544,0.005085497188518,-2.086108360908));
#37485=CARTESIAN_POINT('Ctrl Pts',(0.9625345999714,-0.8171394855951,-2.136808634484));
#37486=CARTESIAN_POINT('Ctrl Pts',(0.1999172311038,-1.246684761989,-2.18750890806));
#37487=CARTESIAN_POINT('Ctrl Pts',(-0.6587711770466,-1.077130600889,-2.238209181636));
#37488=CARTESIAN_POINT('Ctrl Pts',(-1.20088441426,-0.3899569446243,-2.288909455212));
#37489=CARTESIAN_POINT('Ctrl Pts',(-1.165907757512,0.4846121088583,-2.339609728788));
#37490=CARTESIAN_POINT('Ctrl Pts',(-0.5706493815754,1.126298840617,-2.390310002364));
#37491=CARTESIAN_POINT('Ctrl Pts',(0.2988368777019,1.226738079456,-2.44101027594));
#37492=CARTESIAN_POINT('Ctrl Pts',(1.024715859004,0.7376633402686,-2.491710549516));
#37493=CARTESIAN_POINT('Ctrl Pts',(1.258163462203,-0.1058985200368,-2.542410823092));
#37494=CARTESIAN_POINT('Ctrl Pts',(0.8869954937535,-0.8985704154689,-2.593111096668));
#37495=CARTESIAN_POINT('Ctrl Pts',(0.08957822249982,-1.259430639622,-2.643811370244));
#37496=CARTESIAN_POINT('Ctrl Pts',(-0.7508862006194,-1.015066343344,-2.69451164382));
#37497=CARTESIAN_POINT('Ctrl Pts',(-1.230509306326,-0.2829077817768,-2.745211917396));
#37498=CARTESIAN_POINT('Ctrl Pts',(-1.118805770864,0.585203259478,-2.795912190972));
#37499=CARTESIAN_POINT('Ctrl Pts',(-0.4694570034523,1.172092516481,-2.846612464548));
#37500=CARTESIAN_POINT('Ctrl Pts',(0.4054965965563,1.195727852142,-2.897312738124));
#37501=CARTESIAN_POINT('Ctrl Pts',(1.085567158264,0.6447516406069,-2.9480130117));
#37502=CARTESIAN_POINT('Ctrl Pts',(1.244038636693,-0.216063864892,-2.998713285276));
#37503=CARTESIAN_POINT('Ctrl Pts',(0.8044037464872,-0.973044267016,-3.049413558852));
#37504=CARTESIAN_POINT('Ctrl Pts',(0.2543005001532,-1.165976056474,-3.083213741236));
#37505=CARTESIAN_POINT('Ctrl Pts',(-0.01973570449643,-1.161319026465,-3.100113832428));
#37506=CARTESIAN_POINT('Ctrl Pts',(-0.7601495323018,1.010461337524,-1.537156810625));
#37507=CARTESIAN_POINT('Ctrl Pts',(-0.5217111845523,1.189833661624,-1.554056901817));
#37508=CARTESIAN_POINT('Ctrl Pts',(0.08630816170208,1.371705237335,-1.587857084201));
#37509=CARTESIAN_POINT('Ctrl Pts',(0.9577659231642,0.986014487342,-1.638557357777));
#37510=CARTESIAN_POINT('Ctrl Pts',(1.36872301644,0.1263081428663,-1.689257631353));
#37511=CARTESIAN_POINT('Ctrl Pts',(1.121999630998,-0.7940472417276,-1.739957904929));
#37512=CARTESIAN_POINT('Ctrl Pts',(0.3360773550257,-1.332833081702,-1.790658178505));
#37513=CARTESIAN_POINT('Ctrl Pts',(-0.6113435996505,-1.231117050995,-1.841358452081));
#37514=CARTESIAN_POINT('Ctrl Pts',(-1.264982148074,-0.5377836494768,-1.892058725657));
#37515=CARTESIAN_POINT('Ctrl Pts',(-1.310728040867,0.4139841258882,-1.942758999233));
#37516=CARTESIAN_POINT('Ctrl Pts',(-0.7265983274592,1.16681007679,-1.993459272809));
#37517=CARTESIAN_POINT('Ctrl Pts',(0.2067011941596,1.358920713391,-2.044159546385));
#37518=CARTESIAN_POINT('Ctrl Pts',(1.040669609023,0.8979964642824,-2.094859819961));
#37519=CARTESIAN_POINT('Ctrl Pts',(1.374540008523,0.005536359898125,-2.145560093537));
#37520=CARTESIAN_POINT('Ctrl Pts',(1.047869610836,-0.8895842651211,-2.196260367113));
#37521=CARTESIAN_POINT('Ctrl Pts',(0.2176412060017,-1.357211550025,-2.246960640689));
#37522=CARTESIAN_POINT('Ctrl Pts',(-0.7171755664079,-1.172625299503,-2.297660914265));
#37523=CARTESIAN_POINT('Ctrl Pts',(-1.307350700813,-0.4245291876451,-2.348361187841));
#37524=CARTESIAN_POINT('Ctrl Pts',(-1.26927313384,0.5275761535541,-2.399061461417));
#37525=CARTESIAN_POINT('Ctrl Pts',(-0.621241195291,1.226152626448,-2.449761734993));
#37526=CARTESIAN_POINT('Ctrl Pts',(0.3253307286306,1.335496463145,-2.500462008569));
#37527=CARTESIAN_POINT('Ctrl Pts',(1.115563646671,0.8030620377886,-2.551162282145));
#37528=CARTESIAN_POINT('Ctrl Pts',(1.369707912366,-0.115287119011,-2.601862555721));
#37529=CARTESIAN_POINT('Ctrl Pts',(0.9656334669738,-0.978234581483,-2.652562829297));
#37530=CARTESIAN_POINT('Ctrl Pts',(0.0975199199624,-1.371087433381,-2.703263102873));
#37531=CARTESIAN_POINT('Ctrl Pts',(-0.8174571915112,-1.105058638105,-2.753963376449));
#37532=CARTESIAN_POINT('Ctrl Pts',(-1.339602034034,-0.3079894137849,-2.804663650025));
#37533=CARTESIAN_POINT('Ctrl Pts',(-1.217995246873,0.6370853700088,-2.855363923601));
#37534=CARTESIAN_POINT('Ctrl Pts',(-0.5110774485679,1.276006212291,-2.906064197177));
#37535=CARTESIAN_POINT('Ctrl Pts',(0.4414465317312,1.301736975613,-2.956764470753));
#37536=CARTESIAN_POINT('Ctrl Pts',(1.18180981307,0.7019131060313,-3.007464744329));
#37537=CARTESIAN_POINT('Ctrl Pts',(1.354330828351,-0.23521934487,-3.058165017905));
#37538=CARTESIAN_POINT('Ctrl Pts',(0.8757194191373,-1.059311028855,-3.108865291481));
#37539=CARTESIAN_POINT('Ctrl Pts',(0.2768459088523,-1.269347487952,-3.142665473865));
#37540=CARTESIAN_POINT('Ctrl Pts',(-0.02148540425545,-1.264277581662,-3.159565565057));
#37541=CARTESIAN_POINT('',(-0.259610714546449,1.22207863880594,-1.55963283939182));
#37542=CARTESIAN_POINT('Ctrl Pts',(0.507800078725617,-1.14130485853319,
-2.67007418463596));
#37543=CARTESIAN_POINT('Ctrl Pts',(0.612233666406878,-1.0949369024171,-2.66359308772046));
#37544=CARTESIAN_POINT('Ctrl Pts',(0.730114711952954,-1.02596491093318,
-2.65590451342733));
#37545=CARTESIAN_POINT('Ctrl Pts',(0.939047723037593,-0.835150961272447,
-2.6393783299617));
#37546=CARTESIAN_POINT('Ctrl Pts',(1.02060011568731,-0.731926231542939,
-2.63195399377308));
#37547=CARTESIAN_POINT('Ctrl Pts',(1.15133052288156,-0.502486024562013,
-2.61698799059436));
#37548=CARTESIAN_POINT('Ctrl Pts',(1.1994984257216,-0.375115822630611,-2.60939271858708));
#37549=CARTESIAN_POINT('Ctrl Pts',(1.24006231487454,-0.172945597679168,
-2.59745051292342));
#37550=CARTESIAN_POINT('Ctrl Pts',(1.24785745820879,-0.101838259601154,
-2.59326743352897));
#37551=CARTESIAN_POINT('Ctrl Pts',(1.25117970484064,0.0529687419467126,
-2.58433960981054));
#37552=CARTESIAN_POINT('Ctrl Pts',(1.24457703692924,0.136181129120054,-2.57961312073553));
#37553=CARTESIAN_POINT('Ctrl Pts',(1.20567920166832,0.354280324729834,-2.56704836928307));
#37554=CARTESIAN_POINT('Ctrl Pts',(1.15913703077502,0.48681205395866,-2.55921950127501));
#37555=CARTESIAN_POINT('Ctrl Pts',(1.05981281816954,0.666090081600009,-2.54734749584298));
#37556=CARTESIAN_POINT('Ctrl Pts',(1.02309201000238,0.721182755833519,-2.54347119827756));
#37557=CARTESIAN_POINT('Ctrl Pts',(0.881914044721003,0.899560322331259,
-2.53032283606007));
#37558=CARTESIAN_POINT('Ctrl Pts',(0.757112161818906,1.006236439173,-2.52126598676422));
#37559=CARTESIAN_POINT('Ctrl Pts',(0.485273028040564,1.161587970364,-2.50344835191949));
#37560=CARTESIAN_POINT('Ctrl Pts',(0.34622708590613,1.21028400666312,-2.49492562637545));
#37561=CARTESIAN_POINT('Ctrl Pts',(0.1180758092039,1.24663611655136,-2.48163302861913));
#37562=CARTESIAN_POINT('Ctrl Pts',(0.0347233483400104,1.25146309140558,
-2.47691284801568));
#37563=CARTESIAN_POINT('Ctrl Pts',(-0.183382111018931,1.242869499445,-2.46454018040272));
#37564=CARTESIAN_POINT('Ctrl Pts',(-0.317775396484216,1.21608479852621,
-2.45688827247895));
#37565=CARTESIAN_POINT('Ctrl Pts',(-0.513164682464846,1.1421950940086,-2.44477199616997));
#37566=CARTESIAN_POINT('Ctrl Pts',(-0.579179773460147,1.11007605609173,
-2.44048168561375));
#37567=CARTESIAN_POINT('Ctrl Pts',(-0.713385303800749,1.02917629167349,
-2.431457345549));
#37568=CARTESIAN_POINT('Ctrl Pts',(-0.78021602350588,0.979122799501168,
-2.42673408745597));
#37569=CARTESIAN_POINT('Ctrl Pts',(-0.942214698504906,0.831173369487071,
-2.4142961651556));
#37570=CARTESIAN_POINT('Ctrl Pts',(-1.02825443966183,0.723026175962959,
-2.40658569983318));
#37571=CARTESIAN_POINT('Ctrl Pts',(-1.12831490924974,0.54250411551147,-2.39462199127633));
#37572=CARTESIAN_POINT('Ctrl Pts',(-1.15674670073225,0.478748838097753,
-2.39053815767876));
#37573=CARTESIAN_POINT('Ctrl Pts',(-1.20692115391492,0.334074387634818,
-2.38170467512774));
#37574=CARTESIAN_POINT('Ctrl Pts',(-1.22620888847941,0.252843748251602,
-2.37697631382472));
#37575=CARTESIAN_POINT('Ctrl Pts',(-1.2561914452077,0.0334025692953118,
-2.36441535390944));
#37576=CARTESIAN_POINT('Ctrl Pts',(-1.25263171750077,-0.106940783976178,
-2.35659413774588));
#37577=CARTESIAN_POINT('Ctrl Pts',(-1.21339160002161,-0.307346916463829,
-2.34477087009704));
#37578=CARTESIAN_POINT('Ctrl Pts',(-1.19562718031006,-0.370440174551519,
-2.34093320722807));
#37579=CARTESIAN_POINT('Ctrl Pts',(-1.11669511647946,-0.583141614803438,
-2.3278132653876));
#37580=CARTESIAN_POINT('Ctrl Pts',(-1.03089836416202,-0.723181862464307,
-2.31875130601161));
#37581=CARTESIAN_POINT('Ctrl Pts',(-0.814183597922892,-0.961623796844712,
-2.30041965778142));
#37582=CARTESIAN_POINT('Ctrl Pts',(-0.688622940074993,-1.05517691514589,
-2.29136876480927));
#37583=CARTESIAN_POINT('Ctrl Pts',(-0.402020857708303,-1.19353931793331,
-2.27309719359508));
#37584=CARTESIAN_POINT('Ctrl Pts',(-0.243808191860089,-1.23545544282677,
-2.26408213986346));
#37585=CARTESIAN_POINT('Ctrl Pts',(0.0812534277319099,-1.25821680962395,
-2.24545715027443));
#37586=CARTESIAN_POINT('Ctrl Pts',(0.244148088549536,-1.2367630646173,-2.23594808814865));
#37587=CARTESIAN_POINT('Ctrl Pts',(0.547496572649703,-1.13330715703507,
-2.21767661682907));
#37588=CARTESIAN_POINT('Ctrl Pts',(0.685768765362047,-1.05573529789564,
-2.20892469455316));
#37589=CARTESIAN_POINT('Ctrl Pts',(0.932890934550272,-0.848759548429491,
-2.19037969795629));
#37590=CARTESIAN_POINT('Ctrl Pts',(1.03356532261343,-0.721010795095412,
-2.18102416631749));
#37591=CARTESIAN_POINT('Ctrl Pts',(1.17487291216457,-0.447522694588082,
-2.16354273775075));
#37592=CARTESIAN_POINT('Ctrl Pts',(1.21933694334434,-0.308252026913084,
-2.15542543471449));
#37593=CARTESIAN_POINT('Ctrl Pts',(1.24684374138559,-0.1063117898711,-2.14365527952404));
#37594=CARTESIAN_POINT('Ctrl Pts',(1.25054027644431,-0.046790781155218,
-2.14016870831578));
#37595=CARTESIAN_POINT('Ctrl Pts',(1.24885165159501,0.0949819512083569,
-2.13193169800581));
#37596=CARTESIAN_POINT('Ctrl Pts',(1.23957690789249,0.17684746522871,-2.12723897694521));
#37597=CARTESIAN_POINT('Ctrl Pts',(1.18899122454946,0.414872034867468,-2.11340296941449));
#37598=CARTESIAN_POINT('Ctrl Pts',(1.1253086931289,0.566545863998217,-2.10432200684995));
#37599=CARTESIAN_POINT('Ctrl Pts',(0.99772842630465,0.755973242928381,-2.09109665472807));
#37600=CARTESIAN_POINT('Ctrl Pts',(0.955975765769682,0.8080929264264,-2.08718705160299));
#37601=CARTESIAN_POINT('Ctrl Pts',(0.816508252869463,0.955501643623805,
-2.07545874339807));
#37602=CARTESIAN_POINT('Ctrl Pts',(0.706723827562254,1.03873387903179,-2.06778322435594));
#37603=CARTESIAN_POINT('Ctrl Pts',(0.514318875156416,1.14144932299447,-2.05541075057229));
#37604=CARTESIAN_POINT('Ctrl Pts',(0.438025563379678,1.17316462797112,-2.05072820289678));
#37605=CARTESIAN_POINT('Ctrl Pts',(0.291082021764648,1.21768121802146,-2.0418654362662));
#37606=CARTESIAN_POINT('Ctrl Pts',(0.221560531534333,1.23226747309818,-2.037707766503));
#37607=CARTESIAN_POINT('Ctrl Pts',(0.0206049999289771,1.25624693474514,
-2.02598976383744));
#37608=CARTESIAN_POINT('Ctrl Pts',(-0.11199415053374,1.25087818655238,-2.01857533351991));
#37609=CARTESIAN_POINT('Ctrl Pts',(-0.322236465734706,1.20977941365008,
-2.00643183442636));
#37610=CARTESIAN_POINT('Ctrl Pts',(-0.402346692969266,1.18583658575053,
-2.00170402448945));
#37611=CARTESIAN_POINT('Ctrl Pts',(-0.617543203539604,1.09717922754569,
-1.98830826792993));
#37612=CARTESIAN_POINT('Ctrl Pts',(-0.742072545436565,1.01688835433628,
-1.97974310797231));
#37613=CARTESIAN_POINT('Ctrl Pts',(-0.970528733933381,0.802411539894461,
-1.961916047245));
#37614=CARTESIAN_POINT('Ctrl Pts',(-1.06721562926637,0.669459708521441,
-1.9528453631822));
#37615=CARTESIAN_POINT('Ctrl Pts',(-1.16387689970394,0.461009366896075,
-1.93955597171686));
#37616=CARTESIAN_POINT('Ctrl Pts',(-1.18727315637734,0.396889281624173,
-1.93555952718361));
#37617=CARTESIAN_POINT('Ctrl Pts',(-1.24039670893314,0.201558749017812,
-1.92385192259047));
#37618=CARTESIAN_POINT('Ctrl Pts',(-1.25438695473961,0.0666101745329706,
-1.91628466662226));
#37619=CARTESIAN_POINT('Ctrl Pts',(-1.24301618552763,-0.14921257142496,
-1.90402880525015));
#37620=CARTESIAN_POINT('Ctrl Pts',(-1.2307474601993,-0.230947903243687,
-1.89934903401867));
#37621=CARTESIAN_POINT('Ctrl Pts',(-1.19244304551431,-0.381867692531711,
-1.89037302683353));
#37622=CARTESIAN_POINT('Ctrl Pts',(-1.16815111772457,-0.450924156209753,
-1.88609102206247));
#37623=CARTESIAN_POINT('Ctrl Pts',(-1.08371526213591,-0.635447518825377,
-1.87433352012401));
#37624=CARTESIAN_POINT('Ctrl Pts',(-1.01118775305882,-0.744554530895352,
-1.86700630443897));
#37625=CARTESIAN_POINT('Ctrl Pts',(-0.868260159324179,-0.901923869417574,
-1.85495740437297));
#37626=CARTESIAN_POINT('Ctrl Pts',(-0.806301169348746,-0.958058661436189,
-1.85023319411109));
#37627=CARTESIAN_POINT('Ctrl Pts',(-0.615864140590997,-1.09866090397637,
-1.83662343191714));
#37628=CARTESIAN_POINT('Ctrl Pts',(-0.478259891318438,-1.16521149345142,
-1.82779005534706));
#37629=CARTESIAN_POINT('Ctrl Pts',(-0.170195428785501,-1.24773053246873,
-1.80964900900546));
#37630=CARTESIAN_POINT('Ctrl Pts',(-0.00621787061589819,-1.25981453753794,
-1.80057552254435));
#37631=CARTESIAN_POINT('Ctrl Pts',(0.22148838945788,-1.23208442147924,-1.78730395750846));
#37632=CARTESIAN_POINT('Ctrl Pts',(0.287913517277362,-1.21826906905728,
-1.78333149002799));
#37633=CARTESIAN_POINT('Ctrl Pts',(0.48206990334696,-1.16057766045874,-1.77161922627142));
#37634=CARTESIAN_POINT('Ctrl Pts',(0.604642908876124,-1.10111918041112,
-1.76402300138723));
#37635=CARTESIAN_POINT('Ctrl Pts',(0.782442334550935,-0.977321574209538,
-1.75173597566535));
#37636=CARTESIAN_POINT('Ctrl Pts',(0.845406612756201,-0.923792114009704,
-1.74705547216814));
#37637=CARTESIAN_POINT('Ctrl Pts',(0.953023639005534,-0.812046846764356,
-1.73810889089031));
#37638=CARTESIAN_POINT('Ctrl Pts',(0.998555941030456,-0.755451629151792,
-1.73385923094735));
#37639=CARTESIAN_POINT('Ctrl Pts',(1.11085797729936,-0.586757033603323,
-1.72211958756504));
#37640=CARTESIAN_POINT('Ctrl Pts',(1.16554656062255,-0.467362481813021,
-1.71477694616158));
#37641=CARTESIAN_POINT('Ctrl Pts',(1.22407329621253,-0.262674922530386,
-1.70271079771865));
#37642=CARTESIAN_POINT('Ctrl Pts',(1.23913722339119,-0.180431870011504,
-1.6979856595597));
#37643=CARTESIAN_POINT('Ctrl Pts',(1.25815025227789,0.0538952546014994,
-1.68446543178557));
#37644=CARTESIAN_POINT('Ctrl Pts',(1.2426521532669,0.204271826373771,-1.67572541607777));
#37645=CARTESIAN_POINT('Ctrl Pts',(1.15216029633937,0.50829118316365,-1.65767678627267));
#37646=CARTESIAN_POINT('Ctrl Pts',(1.07656356464772,0.654366821513739,-1.64859980495065));
#37647=CARTESIAN_POINT('Ctrl Pts',(0.932841222330786,0.834919960138557,
-1.63525471667252));
#37648=CARTESIAN_POINT('Ctrl Pts',(0.885304617597667,0.885154473762003,
-1.63120703593855));
#37649=CARTESIAN_POINT('Ctrl Pts',(0.733892730794094,1.0199957546792,-1.61949235591571));
#37650=CARTESIAN_POINT('Ctrl Pts',(0.619904967924308,1.09243893007311,-1.61196568392511));
#37651=CARTESIAN_POINT('Ctrl Pts',(0.38102479404947,1.19652686604501,-1.59719153192072));
#37652=CARTESIAN_POINT('Ctrl Pts',(0.256450708106922,1.23003839998894,-1.58988830890701));
#37653=CARTESIAN_POINT('Ctrl Pts',(-0.0010614922244034,1.25675580911652,
-1.57476647375581));
#37654=CARTESIAN_POINT('Ctrl Pts',(-0.132557389488584,1.24899611401415,
-1.5673185533228));
#37655=CARTESIAN_POINT('Ctrl Pts',(-0.259591956716904,1.22190413578271,
-1.55995109671497));
#37656=CARTESIAN_POINT('',(-0.201562741974311,0.948826487356528,-1.3983503624951));
#37657=CARTESIAN_POINT('',(-0.2015628224599,0.948826869667,-1.39835034235));
#37658=CARTESIAN_POINT('Ctrl Pts',(-0.201438444627362,0.948254145075348,
-1.39833463125939));
#37659=CARTESIAN_POINT('Ctrl Pts',(-0.0987242220368489,0.970265808362698,
-1.40609108145075));
#37660=CARTESIAN_POINT('Ctrl Pts',(0.0257428725608549,0.980269505514474,
-1.4151452502064));
#37661=CARTESIAN_POINT('Ctrl Pts',(0.291387332434439,0.933304243270978,
-1.43508446652971));
#37662=CARTESIAN_POINT('Ctrl Pts',(0.412706897305461,0.88605986686801,-1.44450516556305));
#37663=CARTESIAN_POINT('Ctrl Pts',(0.628779001349331,0.749481019437183,
-1.46337969015587));
#37664=CARTESIAN_POINT('Ctrl Pts',(0.720840663164952,0.66158629606172,-1.47261419444165));
#37665=CARTESIAN_POINT('Ctrl Pts',(0.865891373452379,0.453145919229779,
-1.49136828466245));
#37666=CARTESIAN_POINT('Ctrl Pts',(0.917884397731051,0.336027550648196,
-1.50064573334002));
#37667=CARTESIAN_POINT('Ctrl Pts',(0.978638449230794,0.0708459015851718,
-1.52074725798837));
#37668=CARTESIAN_POINT('Ctrl Pts',(0.973931484966905,-0.0572846090069996,
-1.53002995833632));
#37669=CARTESIAN_POINT('Ctrl Pts',(0.934315968934625,-0.285437655104305,
-1.54712254226946));
#37670=CARTESIAN_POINT('Ctrl Pts',(0.890402125861598,-0.403268946572186,
-1.5562361743832));
#37671=CARTESIAN_POINT('Ctrl Pts',(0.747386626902548,-0.636741734663479,
-1.57647731730412));
#37672=CARTESIAN_POINT('Ctrl Pts',(0.651197130204397,-0.725508943735299,
-1.58593652604146));
#37673=CARTESIAN_POINT('Ctrl Pts',(0.46872734556964,-0.856930153167852,
-1.60253070931023));
#37674=CARTESIAN_POINT('Ctrl Pts',(0.357462783542698,-0.90979585830865,
-1.61146999211917));
#37675=CARTESIAN_POINT('Ctrl Pts',(0.1151570245764,-0.971772300974352,-1.62996387111578));
#37676=CARTESIAN_POINT('Ctrl Pts',(-0.016347839305272,-0.977573473079552,
-1.639492985865));
#37677=CARTESIAN_POINT('Ctrl Pts',(-0.245117563251694,-0.943476331507241,
-1.65656207327439));
#37678=CARTESIAN_POINT('Ctrl Pts',(-0.366912073350302,-0.90976070737921,
-1.66571067006408));
#37679=CARTESIAN_POINT('Ctrl Pts',(-0.601745916092765,-0.771019708663967,
-1.68587412445648));
#37680=CARTESIAN_POINT('Ctrl Pts',(-0.698962539434392,-0.683420729699717,
-1.69534357230481));
#37681=CARTESIAN_POINT('Ctrl Pts',(-0.853060563983244,-0.478627690499663,
-1.71426376865579));
#37682=CARTESIAN_POINT('Ctrl Pts',(-0.907464882095698,-0.365840031027879,
-1.72334711263655));
#37683=CARTESIAN_POINT('Ctrl Pts',(-0.970164031430926,-0.119629985848659,
-1.74211689745239));
#37684=CARTESIAN_POINT('Ctrl Pts',(-0.977417294464398,0.00938936091317684,
-1.75146963513136));
#37685=CARTESIAN_POINT('Ctrl Pts',(-0.938831912985727,0.290717066024187,
-1.77244468659029));
#37686=CARTESIAN_POINT('Ctrl Pts',(-0.884427664631833,0.408880548362764,
-1.78184632710929));
#37687=CARTESIAN_POINT('Ctrl Pts',(-0.772729409729827,0.598010361875881,
-1.79806327048482));
#37688=CARTESIAN_POINT('Ctrl Pts',(-0.688892984793707,0.693427839352924,
-1.80726343572838));
#37689=CARTESIAN_POINT('Ctrl Pts',(-0.473205224209429,0.859859072888414,
-1.82739908912347));
#37690=CARTESIAN_POINT('Ctrl Pts',(-0.353507651838664,0.908978961000493,
-1.83675941614616));
#37691=CARTESIAN_POINT('Ctrl Pts',(-0.132446689760668,0.967814534797147,
-1.85364192795321));
#37692=CARTESIAN_POINT('Ctrl Pts',(-0.00829769730837255,0.977449939050658,
-1.86267203669443));
#37693=CARTESIAN_POINT('Ctrl Pts',(0.272743269789277,0.944831723940324,
-1.88359146085372));
#37694=CARTESIAN_POINT('Ctrl Pts',(0.397319123049016,0.889004983339366,
-1.8934300912476));
#37695=CARTESIAN_POINT('Ctrl Pts',(0.54846316864109,0.803242517078114,-1.90625396287727));
#37696=CARTESIAN_POINT('Ctrl Pts',(0.657061179243564,0.731431679270899,
-1.91563986981193));
#37697=CARTESIAN_POINT('Ctrl Pts',(0.837016667682568,0.506409290281685,
-1.93694382317187));
#37698=CARTESIAN_POINT('Ctrl Pts',(0.896708335504397,0.389439444790955,
-1.94644765605331));
#37699=CARTESIAN_POINT('Ctrl Pts',(0.961575479660275,0.163480681552635,
-1.96379887442898));
#37700=CARTESIAN_POINT('Ctrl Pts',(0.980196107359686,0.038092952714017,
-1.97297967779038));
#37701=CARTESIAN_POINT('Ctrl Pts',(0.949796426925323,-0.232115295912927,
-1.99307419258545));
#37702=CARTESIAN_POINT('Ctrl Pts',(0.910338156983532,-0.356057593387196,
-2.00248672788133));
#37703=CARTESIAN_POINT('Ctrl Pts',(0.787597338177096,-0.580417039662108,
-2.02137165311335));
#37704=CARTESIAN_POINT('Ctrl Pts',(0.705541931920849,-0.677858961903907,
-2.03061365747613));
#37705=CARTESIAN_POINT('Ctrl Pts',(0.506633724951066,-0.835677971904185,
-2.04936477089474));
#37706=CARTESIAN_POINT('Ctrl Pts',(0.393146281041908,-0.894898742571984,
-2.05863327258857));
#37707=CARTESIAN_POINT('Ctrl Pts',(0.132370167545827,-0.972251332822705,
-2.07873243056899));
#37708=CARTESIAN_POINT('Ctrl Pts',(0.00409184961383252,-0.975578594338933,
-2.08802219266169));
#37709=CARTESIAN_POINT('Ctrl Pts',(-0.225854147439267,-0.950466860502564,
-2.10509568956757));
#37710=CARTESIAN_POINT('Ctrl Pts',(-0.346100609615678,-0.914145414198234,
-2.1141999618899));
#37711=CARTESIAN_POINT('Ctrl Pts',(-0.588320648121434,-0.786121492823866,
-2.13445454703384));
#37712=CARTESIAN_POINT('Ctrl Pts',(-0.683052440276746,-0.695538874693907,
-2.14392566572338));
#37713=CARTESIAN_POINT('Ctrl Pts',(-0.825486585716714,-0.522102941548968,
-2.16048705452036));
#37714=CARTESIAN_POINT('Ctrl Pts',(-0.88524530347349,-0.414549954481618,
-2.16941649293993));
#37715=CARTESIAN_POINT('Ctrl Pts',(-0.959910000303239,-0.184617722335589,
-2.18729260948374));
#37716=CARTESIAN_POINT('Ctrl Pts',(-0.974739175019372,-0.0624749986378993,
-2.19622204790341));
#37717=CARTESIAN_POINT('Ctrl Pts',(-0.961371621012054,0.161553609341058,
-2.21278343670051));
#37718=CARTESIAN_POINT('Ctrl Pts',(-0.937929646660382,0.290510179513995,
-2.22225455539021));
#37719=CARTESIAN_POINT('Ctrl Pts',(-0.817133378498529,0.536414496466949,
-2.24250914053417));
#37720=CARTESIAN_POINT('Ctrl Pts',(-0.741165879725255,0.636451480916389,
-2.25161341285639));
#37721=CARTESIAN_POINT('Ctrl Pts',(-0.569841157284644,0.791865766674308,
-2.26868690976221));
#37722=CARTESIAN_POINT('Ctrl Pts',(-0.464080472392293,0.864536772252294,
-2.27797667185481));
#37723=CARTESIAN_POINT('Ctrl Pts',(-0.207609487844049,0.955147139613417,
-2.29807582983535));
#37724=CARTESIAN_POINT('Ctrl Pts',(-0.0809805019614242,0.973898127262912,
-2.30734433152936));
#37725=CARTESIAN_POINT('Ctrl Pts',(0.172699493612978,0.963045728321461,
-2.32609544494811));
#37726=CARTESIAN_POINT('Ctrl Pts',(0.296347838905494,0.932400914526657,
-2.33533744931096));
#37727=CARTESIAN_POINT('Ctrl Pts',(0.527483844276784,0.822954047256741,
-2.35422237454296));
#37728=CARTESIAN_POINT('Ctrl Pts',(0.63223052539128,0.745838672878272,-2.36363490983875));
#37729=CARTESIAN_POINT('Ctrl Pts',(0.815578016510061,0.54503943060626,-2.38372942463377));
#37730=CARTESIAN_POINT('Ctrl Pts',(0.874175039145352,0.432633028397659,
-2.39291022799515));
#37731=CARTESIAN_POINT('Ctrl Pts',(0.954433739868647,0.211672285202659,
-2.41026144637082));
#37732=CARTESIAN_POINT('Ctrl Pts',(0.974849576921623,0.0819486036372085,
-2.41976527925227));
#37733=CARTESIAN_POINT('Ctrl Pts',(0.961425884758652,-0.205868800031195,
-2.44106923261221));
#37734=CARTESIAN_POINT('Ctrl Pts',(0.915734610801321,-0.327781194058935,
-2.45045513954686));
#37735=CARTESIAN_POINT('Ctrl Pts',(0.843810636917665,-0.485979377100993,
-2.4632790111765));
#37736=CARTESIAN_POINT('Ctrl Pts',(0.775799049655213,-0.604344034746782,
-2.47311764157039));
#37737=CARTESIAN_POINT('Ctrl Pts',(0.567537098494519,-0.795851039430973,
-2.49403706572968));
#37738=CARTESIAN_POINT('Ctrl Pts',(0.461411930121146,-0.860991364727363,
-2.50306717447086));
#37739=CARTESIAN_POINT('Ctrl Pts',(0.247958153459295,-0.943253500169966,
-2.51994968627787));
#37740=CARTESIAN_POINT('Ctrl Pts',(0.122238049409578,-0.973826816597205,
-2.52931001330053));
#37741=CARTESIAN_POINT('Ctrl Pts',(-0.150080047920812,-0.965863184981856,
-2.54944566669569));
#37742=CARTESIAN_POINT('Ctrl Pts',(-0.273980275415711,-0.937902949273016,
-2.55864583193933));
#37743=CARTESIAN_POINT('Ctrl Pts',(-0.475482963183443,-0.85047724750135,
-2.57486277531498));
#37744=CARTESIAN_POINT('Ctrl Pts',(-0.588929238049097,-0.786818991819914,
-2.58426441583404));
#37745=CARTESIAN_POINT('Ctrl Pts',(-0.785433476719409,-0.581830715298288,
-2.60523946729291));
#37746=CARTESIAN_POINT('Ctrl Pts',(-0.855362821274645,-0.473163846227886,
-2.61459220497182));
#37747=CARTESIAN_POINT('Ctrl Pts',(-0.949273543111333,-0.237088972514631,
-2.63336198978761));
#37748=CARTESIAN_POINT('Ctrl Pts',(-0.971510997389175,-0.113855934794878,
-2.64244533376835));
#37749=CARTESIAN_POINT('Ctrl Pts',(-0.967127048588767,0.142400130630832,
-2.6613655301193));
#37750=CARTESIAN_POINT('Ctrl Pts',(-0.939921400836311,0.270402106005835,
-2.67083497796768));
#37751=CARTESIAN_POINT('Ctrl Pts',(-0.831398503477933,0.520639551586384,
-2.69099843236003));
#37752=CARTESIAN_POINT('Ctrl Pts',(-0.752647366453703,0.619477319761821,
-2.70014702914963));
#37753=CARTESIAN_POINT('Ctrl Pts',(-0.587553439321292,0.78147175448688,
-2.7172161165589));
#37754=CARTESIAN_POINT('Ctrl Pts',(-0.477728333010138,0.854036407356267,
-2.726745231308));
#37755=CARTESIAN_POINT('Ctrl Pts',(-0.245237492311451,0.946238192940212,
-2.7452391103046));
#37756=CARTESIAN_POINT('Ctrl Pts',(-0.124140916952226,0.968825910384071,
-2.75417839311363));
#37757=CARTESIAN_POINT('Ctrl Pts',(0.100728002832586,0.969677678031108,
-2.77077257638251));
#37758=CARTESIAN_POINT('Ctrl Pts',(0.230717602518166,0.954356429549928,
-2.78023178511994));
#37759=CARTESIAN_POINT('Ctrl Pts',(0.483614457581182,0.849446199253669,
-2.80047292804102));
#37760=CARTESIAN_POINT('Ctrl Pts',(0.58837648052914,0.779893647824787,-2.80958656015487));
#37761=CARTESIAN_POINT('Ctrl Pts',(0.754474219189733,0.618540796080957,
-2.82667914408813));
#37762=CARTESIAN_POINT('Ctrl Pts',(0.833559877872636,0.517619827754594,
-2.83596184443618));
#37763=CARTESIAN_POINT('Ctrl Pts',(0.940190436386863,0.267335418003295,
-2.85606336908445));
#37764=CARTESIAN_POINT('Ctrl Pts',(0.966923459393059,0.142014500699582,
-2.86534081776185));
#37765=CARTESIAN_POINT('Ctrl Pts',(0.972003626913642,-0.111877781866752,
-2.88409490798249));
#37766=CARTESIAN_POINT('Ctrl Pts',(0.949143248594239,-0.237090541107098,
-2.89332941226818));
#37767=CARTESIAN_POINT('Ctrl Pts',(0.854532540396046,-0.474555800893968,
-2.912203936861));
#37768=CARTESIAN_POINT('Ctrl Pts',(0.784113881905413,-0.584062332473451,
-2.92162463589442));
#37769=CARTESIAN_POINT('Ctrl Pts',(0.596737771337372,-0.778136224042799,
-2.94156409432769));
#37770=CARTESIAN_POINT('Ctrl Pts',(0.490136620493726,-0.843165130861668,
-2.95061838510722));
#37771=CARTESIAN_POINT('Ctrl Pts',(0.394089576350919,-0.885695643716614,
-2.95837453804489));
#37772=CARTESIAN_POINT('Ctrl Pts',(-0.7601495323018,1.010461337524,-1.070459688113));
#37773=CARTESIAN_POINT('Ctrl Pts',(-0.5217111845523,1.189833661624,-1.087359779305));
#37774=CARTESIAN_POINT('Ctrl Pts',(0.08630816170208,1.371705237335,-1.121159961689));
#37775=CARTESIAN_POINT('Ctrl Pts',(0.9577659231642,0.986014487342,-1.171860235265));
#37776=CARTESIAN_POINT('Ctrl Pts',(1.36872301644,0.1263081428663,-1.222560508841));
#37777=CARTESIAN_POINT('Ctrl Pts',(1.121999630998,-0.7940472417276,-1.273260782417));
#37778=CARTESIAN_POINT('Ctrl Pts',(0.3360773550257,-1.332833081702,-1.323961055993));
#37779=CARTESIAN_POINT('Ctrl Pts',(-0.6113435996505,-1.231117050995,-1.374661329569));
#37780=CARTESIAN_POINT('Ctrl Pts',(-1.264982148074,-0.5377836494768,-1.425361603145));
#37781=CARTESIAN_POINT('Ctrl Pts',(-1.310728040867,0.4139841258882,-1.476061876721));
#37782=CARTESIAN_POINT('Ctrl Pts',(-0.7265983274592,1.16681007679,-1.526762150297));
#37783=CARTESIAN_POINT('Ctrl Pts',(0.2067011941596,1.358920713391,-1.577462423873));
#37784=CARTESIAN_POINT('Ctrl Pts',(1.040669609023,0.8979964642824,-1.628162697449));
#37785=CARTESIAN_POINT('Ctrl Pts',(1.374540008523,0.005536359898125,-1.678862971025));
#37786=CARTESIAN_POINT('Ctrl Pts',(1.047869610836,-0.8895842651211,-1.729563244601));
#37787=CARTESIAN_POINT('Ctrl Pts',(0.2176412060017,-1.357211550025,-1.780263518177));
#37788=CARTESIAN_POINT('Ctrl Pts',(-0.7171755664079,-1.172625299503,-1.830963791753));
#37789=CARTESIAN_POINT('Ctrl Pts',(-1.307350700813,-0.4245291876451,-1.881664065329));
#37790=CARTESIAN_POINT('Ctrl Pts',(-1.26927313384,0.5275761535541,-1.932364338905));
#37791=CARTESIAN_POINT('Ctrl Pts',(-0.621241195291,1.226152626448,-1.983064612481));
#37792=CARTESIAN_POINT('Ctrl Pts',(0.3253307286306,1.335496463145,-2.033764886057));
#37793=CARTESIAN_POINT('Ctrl Pts',(1.115563646671,0.8030620377886,-2.084465159633));
#37794=CARTESIAN_POINT('Ctrl Pts',(1.369707912366,-0.115287119011,-2.135165433209));
#37795=CARTESIAN_POINT('Ctrl Pts',(0.9656334669738,-0.978234581483,-2.185865706785));
#37796=CARTESIAN_POINT('Ctrl Pts',(0.0975199199624,-1.371087433381,-2.236565980361));
#37797=CARTESIAN_POINT('Ctrl Pts',(-0.8174571915112,-1.105058638105,-2.287266253937));
#37798=CARTESIAN_POINT('Ctrl Pts',(-1.339602034034,-0.3079894137849,-2.337966527513));
#37799=CARTESIAN_POINT('Ctrl Pts',(-1.217995246873,0.6370853700088,-2.388666801089));
#37800=CARTESIAN_POINT('Ctrl Pts',(-0.5110774485679,1.276006212291,-2.439367074665));
#37801=CARTESIAN_POINT('Ctrl Pts',(0.4414465317312,1.301736975613,-2.490067348241));
#37802=CARTESIAN_POINT('Ctrl Pts',(1.18180981307,0.7019131060313,-2.540767621817));
#37803=CARTESIAN_POINT('Ctrl Pts',(1.354330828351,-0.23521934487,-2.591467895393));
#37804=CARTESIAN_POINT('Ctrl Pts',(0.8757194191373,-1.059311028855,-2.642168168969));
#37805=CARTESIAN_POINT('Ctrl Pts',(0.2768459088523,-1.269347487952,-2.675968351353));
#37806=CARTESIAN_POINT('Ctrl Pts',(-0.02148540425545,-1.264277581662,-2.692868442545));
#37807=CARTESIAN_POINT('Ctrl Pts',(-0.6982454862957,0.9281727318386,-1.129911420741));
#37808=CARTESIAN_POINT('Ctrl Pts',(-0.479224763397,1.092937571317,-1.146811511933));
#37809=CARTESIAN_POINT('Ctrl Pts',(0.07927951248811,1.259998131679,-1.180611694317));
#37810=CARTESIAN_POINT('Ctrl Pts',(0.8797686565066,0.905716751708,-1.231311967893));
#37811=CARTESIAN_POINT('Ctrl Pts',(1.257258772921,0.1160220284182,-1.282012241469));
#37812=CARTESIAN_POINT('Ctrl Pts',(1.030627718204,-0.7293826791723,-1.332712515045));
#37813=CARTESIAN_POINT('Ctrl Pts',(0.3087083346382,-1.224291594926,-1.383412788621));
#37814=CARTESIAN_POINT('Ctrl Pts',(-0.561557813157,-1.130858978964,-1.434113062197));
#37815=CARTESIAN_POINT('Ctrl Pts',(-1.161966215335,-0.4939883403121,-1.484813335773));
#37816=CARTESIAN_POINT('Ctrl Pts',(-1.203986714989,0.3802706375734,-1.535513609349));
#37817=CARTESIAN_POINT('Ctrl Pts',(-0.6674265798232,1.071788950545,-1.586213882925));
#37818=CARTESIAN_POINT('Ctrl Pts',(0.1898681373872,1.248254736783,-1.636914156501));
#37819=CARTESIAN_POINT('Ctrl Pts',(0.9559209423246,0.8248666232761,-1.687614430077));
#37820=CARTESIAN_POINT('Ctrl Pts',(1.262602048544,0.005085497188518,-1.738314703653));
#37821=CARTESIAN_POINT('Ctrl Pts',(0.9625345999714,-0.8171394855951,-1.789014977229));
#37822=CARTESIAN_POINT('Ctrl Pts',(0.1999172311038,-1.246684761989,-1.839715250805));
#37823=CARTESIAN_POINT('Ctrl Pts',(-0.6587711770466,-1.077130600889,-1.890415524381));
#37824=CARTESIAN_POINT('Ctrl Pts',(-1.20088441426,-0.3899569446243,-1.941115797957));
#37825=CARTESIAN_POINT('Ctrl Pts',(-1.165907757512,0.4846121088583,-1.991816071533));
#37826=CARTESIAN_POINT('Ctrl Pts',(-0.5706493815754,1.126298840617,-2.042516345109));
#37827=CARTESIAN_POINT('Ctrl Pts',(0.2988368777019,1.226738079456,-2.093216618685));
#37828=CARTESIAN_POINT('Ctrl Pts',(1.024715859004,0.7376633402686,-2.143916892261));
#37829=CARTESIAN_POINT('Ctrl Pts',(1.258163462203,-0.1058985200368,-2.194617165837));
#37830=CARTESIAN_POINT('Ctrl Pts',(0.8869954937535,-0.8985704154689,-2.245317439413));
#37831=CARTESIAN_POINT('Ctrl Pts',(0.08957822249982,-1.259430639622,-2.296017712989));
#37832=CARTESIAN_POINT('Ctrl Pts',(-0.7508862006194,-1.015066343344,-2.346717986565));
#37833=CARTESIAN_POINT('Ctrl Pts',(-1.230509306326,-0.2829077817768,-2.397418260141));
#37834=CARTESIAN_POINT('Ctrl Pts',(-1.118805770864,0.585203259478,-2.448118533717));
#37835=CARTESIAN_POINT('Ctrl Pts',(-0.4694570034523,1.172092516481,-2.498818807293));
#37836=CARTESIAN_POINT('Ctrl Pts',(0.4054965965563,1.195727852142,-2.549519080869));
#37837=CARTESIAN_POINT('Ctrl Pts',(1.085567158264,0.6447516406069,-2.600219354445));
#37838=CARTESIAN_POINT('Ctrl Pts',(1.244038636693,-0.216063864892,-2.650919628021));
#37839=CARTESIAN_POINT('Ctrl Pts',(0.8044037464872,-0.973044267016,-2.701619901597));
#37840=CARTESIAN_POINT('Ctrl Pts',(0.2543005001532,-1.165976056474,-2.735420083981));
#37841=CARTESIAN_POINT('Ctrl Pts',(-0.01973570449643,-1.161319026465,-2.752320175173));
#37842=CARTESIAN_POINT('Ctrl Pts',(-0.6363414402896,0.8458841261532,-1.189363153369));
#37843=CARTESIAN_POINT('Ctrl Pts',(-0.4367383422416,0.9960414810095,-1.206263244561));
#37844=CARTESIAN_POINT('Ctrl Pts',(0.07225086327415,1.148291026024,-1.240063426945));
#37845=CARTESIAN_POINT('Ctrl Pts',(0.8017713898489,0.825419016074,-1.290763700521));
#37846=CARTESIAN_POINT('Ctrl Pts',(1.145794529402,0.10573591397,-1.341463974097));
#37847=CARTESIAN_POINT('Ctrl Pts',(0.9392558054095,-0.664718116617,-1.392164247673));
#37848=CARTESIAN_POINT('Ctrl Pts',(0.2813393142507,-1.11575010815,-1.442864521249));
#37849=CARTESIAN_POINT('Ctrl Pts',(-0.5117720266635,-1.030600906933,-1.493564794825));
#37850=CARTESIAN_POINT('Ctrl Pts',(-1.058950282596,-0.4501930311474,-1.544265068401));
#37851=CARTESIAN_POINT('Ctrl Pts',(-1.097245389111,0.3465571492585,-1.594965341977));
#37852=CARTESIAN_POINT('Ctrl Pts',(-0.6082548321872,0.9767678242997,-1.645665615553));
#37853=CARTESIAN_POINT('Ctrl Pts',(0.1730350806147,1.137588760174,-1.696365889129));
#37854=CARTESIAN_POINT('Ctrl Pts',(0.8711722756261,0.7517367822698,-1.747066162705));
#37855=CARTESIAN_POINT('Ctrl Pts',(1.150664088565,0.004634634478915,-1.797766436281));
#37856=CARTESIAN_POINT('Ctrl Pts',(0.877199589107,-0.7446947060692,-1.848466709857));
#37857=CARTESIAN_POINT('Ctrl Pts',(0.1821932562059,-1.136157973952,-1.899166983433));
#37858=CARTESIAN_POINT('Ctrl Pts',(-0.6003667876853,-0.9816359022759,-1.949867257009));
#37859=CARTESIAN_POINT('Ctrl Pts',(-1.094418127707,-0.3553847016034,-2.000567530585));
#37860=CARTESIAN_POINT('Ctrl Pts',(-1.062542381185,0.4416480641625,-2.051267804161));
#37861=CARTESIAN_POINT('Ctrl Pts',(-0.5200575678599,1.026445054786,-2.101968077737));
#37862=CARTESIAN_POINT('Ctrl Pts',(0.2723430267731,1.117979695766,-2.152668351313));
#37863=CARTESIAN_POINT('Ctrl Pts',(0.933868071336,0.6722646427485,-2.203368624889));
#37864=CARTESIAN_POINT('Ctrl Pts',(1.146619012041,-0.09650992106268,-2.254068898465));
#37865=CARTESIAN_POINT('Ctrl Pts',(0.8083575205332,-0.8189062494547,-2.304769172041));
#37866=CARTESIAN_POINT('Ctrl Pts',(0.08163652503724,-1.147773845863,-2.355469445617));
#37867=CARTESIAN_POINT('Ctrl Pts',(-0.6843152097275,-0.9250740485843,-2.406169719193));
#37868=CARTESIAN_POINT('Ctrl Pts',(-1.121416578618,-0.2578261497687,-2.456869992769));
#37869=CARTESIAN_POINT('Ctrl Pts',(-1.019616294854,0.5333211489471,-2.507570266345));
#37870=CARTESIAN_POINT('Ctrl Pts',(-0.4278365583367,1.068178820671,-2.558270539921));
#37871=CARTESIAN_POINT('Ctrl Pts',(0.3695466613813,1.089718728671,-2.608970813497));
#37872=CARTESIAN_POINT('Ctrl Pts',(0.9893245034571,0.5875901751825,-2.659671087073));
#37873=CARTESIAN_POINT('Ctrl Pts',(1.133746445034,-0.1969083849139,-2.710371360649));
#37874=CARTESIAN_POINT('Ctrl Pts',(0.7330880738372,-0.8867775051772,-2.761071634225));
#37875=CARTESIAN_POINT('Ctrl Pts',(0.2317550914541,-1.062604624995,-2.794871816609));
#37876=CARTESIAN_POINT('Ctrl Pts',(-0.01798600473741,-1.058360471267,-2.811771907801));
#37877=CARTESIAN_POINT('Ctrl Pts',(-0.5744373942835,0.7635955204679,-1.248814885998));
#37878=CARTESIAN_POINT('Ctrl Pts',(-0.3942519210863,0.8991453907025,-1.26571497719));
#37879=CARTESIAN_POINT('Ctrl Pts',(0.06522221406019,1.036583920368,-1.299515159574));
#37880=CARTESIAN_POINT('Ctrl Pts',(0.7237741231913,0.74512128044,-1.35021543315));
#37881=CARTESIAN_POINT('Ctrl Pts',(1.034330285883,0.09544979952193,-1.400915706726));
#37882=CARTESIAN_POINT('Ctrl Pts',(0.8478838926151,-0.6000535540617,-1.451615980302));
#37883=CARTESIAN_POINT('Ctrl Pts',(0.2539702938632,-1.007208621374,-1.502316253878));
#37884=CARTESIAN_POINT('Ctrl Pts',(-0.46198624017,-0.9303428349025,-1.553016527454));
#37885=CARTESIAN_POINT('Ctrl Pts',(-0.955934349857,-0.4063977219828,-1.60371680103));
#37886=CARTESIAN_POINT('Ctrl Pts',(-0.9905040632336,0.3128436609437,-1.654417074606));
#37887=CARTESIAN_POINT('Ctrl Pts',(-0.5490830845512,0.8817466980546,-1.705117348182));
#37888=CARTESIAN_POINT('Ctrl Pts',(0.1562020238423,1.026922783566,-1.755817621758));
#37889=CARTESIAN_POINT('Ctrl Pts',(0.7864236089275,0.6786069412635,-1.806517895334));
#37890=CARTESIAN_POINT('Ctrl Pts',(1.038726128586,0.004183771769308,-1.85721816891));
#37891=CARTESIAN_POINT('Ctrl Pts',(0.7918645782425,-0.6722499265432,-1.907918442486));
#37892=CARTESIAN_POINT('Ctrl Pts',(0.1644692813081,-1.025631185916,-1.958618716062));
#37893=CARTESIAN_POINT('Ctrl Pts',(-0.541962398324,-0.8861412036624,-2.009318989638));
#37894=CARTESIAN_POINT('Ctrl Pts',(-0.9879518411537,-0.3208124585826,-2.060019263214));
#37895=CARTESIAN_POINT('Ctrl Pts',(-0.9591770048575,0.3986840194666,-2.11071953679));
#37896=CARTESIAN_POINT('Ctrl Pts',(-0.4694657541443,0.9265912689544,-2.161419810366));
#37897=CARTESIAN_POINT('Ctrl Pts',(0.2458491758444,1.009221312076,-2.212120083942));
#37898=CARTESIAN_POINT('Ctrl Pts',(0.8430202836683,0.6068659452285,-2.262820357518));
#37899=CARTESIAN_POINT('Ctrl Pts',(1.035074561878,-0.08712132208854,-2.313520631094));
#37900=CARTESIAN_POINT('Ctrl Pts',(0.7297195473129,-0.7392420834405,-2.36422090467));
#37901=CARTESIAN_POINT('Ctrl Pts',(0.07369482757466,-1.036117052103,-2.414921178246));
#37902=CARTESIAN_POINT('Ctrl Pts',(-0.6177442188356,-0.8350817538242,-2.465621451822));
#37903=CARTESIAN_POINT('Ctrl Pts',(-1.01232385091,-0.2327445177605,-2.516321725398));
#37904=CARTESIAN_POINT('Ctrl Pts',(-0.9204268188452,0.4814390384163,-2.567021998974));
#37905=CARTESIAN_POINT('Ctrl Pts',(-0.3862161132211,0.9642651248607,-2.61772227255));
#37906=CARTESIAN_POINT('Ctrl Pts',(0.3335967262064,0.9837096051999,-2.668422546126));
#37907=CARTESIAN_POINT('Ctrl Pts',(0.8930818486504,0.5304287097581,-2.719122819702));
#37908=CARTESIAN_POINT('Ctrl Pts',(1.023454253376,-0.1777529049358,-2.769823093278));
#37909=CARTESIAN_POINT('Ctrl Pts',(0.6617724011872,-0.8005107433383,-2.820523366854));
#37910=CARTESIAN_POINT('Ctrl Pts',(0.209209682755,-0.9592331935163,-2.854323549238));
#37911=CARTESIAN_POINT('Ctrl Pts',(-0.01623630497839,-0.9554019160702,-2.87122364043));
#37912=CARTESIAN_POINT('',(-0.259620813216912,1.22212682904672,-1.11035239491773));
#37913=CARTESIAN_POINT('Ctrl Pts',(-0.259550427067826,1.2218848440576,-1.11004989456032));
#37914=CARTESIAN_POINT('Ctrl Pts',(-0.176089993779685,1.23970121447083,
-1.11497869489726));
#37915=CARTESIAN_POINT('Ctrl Pts',(-0.0908079081753038,1.24915717847783,
-1.11989604862454));
#37916=CARTESIAN_POINT('Ctrl Pts',(0.078907392811349,1.2503536393333,-1.12957295158789));
#37917=CARTESIAN_POINT('Ctrl Pts',(0.162375297690802,1.24228645451723,-1.13424992803467));
#37918=CARTESIAN_POINT('Ctrl Pts',(0.403734930196471,1.19332043365468,-1.14828701945804));
#37919=CARTESIAN_POINT('Ctrl Pts',(0.556180896601559,1.12984504867094,-1.15772076971209));
#37920=CARTESIAN_POINT('Ctrl Pts',(0.79311118448388,0.973386735470281,-1.17408123400961));
#37921=CARTESIAN_POINT('Ctrl Pts',(0.919885403903609,0.869811354026893,
-1.18306885097986));
#37922=CARTESIAN_POINT('Ctrl Pts',(1.12233993543671,0.571332489916865,-1.20376271043536));
#37923=CARTESIAN_POINT('Ctrl Pts',(1.18717976490115,0.420371499103929,-1.21315322596248));
#37924=CARTESIAN_POINT('Ctrl Pts',(1.26532256770491,0.0628365754308183,
-1.23413706582087));
#37925=CARTESIAN_POINT('Ctrl Pts',(1.25085721746949,-0.105155817320906,
-1.24338943208094));
#37926=CARTESIAN_POINT('Ctrl Pts',(1.20048510106074,-0.379552281401981,
-1.25946420042759));
#37927=CARTESIAN_POINT('Ctrl Pts',(1.1419432982034,-0.531453654769294,-1.26876281109958));
#37928=CARTESIAN_POINT('Ctrl Pts',(1.01524185767701,-0.73350518608508,-1.28235787310138));
#37929=CARTESIAN_POINT('Ctrl Pts',(0.967392529020281,-0.795523411523133,
-1.28673633950651));
#37930=CARTESIAN_POINT('Ctrl Pts',(0.857289770780207,-0.912799058533321,
-1.29591217872114));
#37931=CARTESIAN_POINT('Ctrl Pts',(0.795144597656944,-0.967011082703482,
-1.30064043572717));
#37932=CARTESIAN_POINT('Ctrl Pts',(0.599484790288714,-1.10705926876841,
-1.31453434606277));
#37933=CARTESIAN_POINT('Ctrl Pts',(0.453032617993671,-1.17555061064353,
-1.32374476309936));
#37934=CARTESIAN_POINT('Ctrl Pts',(0.261514424480917,-1.22293451905085,
-1.33491640565985));
#37935=CARTESIAN_POINT('Ctrl Pts',(0.223775349447442,-1.23038193593054,
-1.337082972641));
#37936=CARTESIAN_POINT('Ctrl Pts',(0.0402342673113264,-1.25757860289646,
-1.34762444380788));
#37937=CARTESIAN_POINT('Ctrl Pts',(-0.10904320782717,-1.25282127697789,
-1.35615292953458));
#37938=CARTESIAN_POINT('Ctrl Pts',(-0.333345813583322,-1.20674934849765,
-1.36937522906284));
#37939=CARTESIAN_POINT('Ctrl Pts',(-0.412152165025727,-1.18248733842875,
-1.37410284257688));
#37940=CARTESIAN_POINT('Ctrl Pts',(-0.560423900027475,-1.12010380073129,
-1.38327871661146));
#37941=CARTESIAN_POINT('Ctrl Pts',(-0.629363619347819,-1.082889305217,-1.38765781242608));
#37942=CARTESIAN_POINT('Ctrl Pts',(-0.826731718365693,-0.950152059149684,
-1.40121639690562));
#37943=CARTESIAN_POINT('Ctrl Pts',(-0.94156875397672,-0.835743004688424,
-1.41047617204213));
#37944=CARTESIAN_POINT('Ctrl Pts',(-1.09839950351904,-0.607361502190615,
-1.4264405463437));
#37945=CARTESIAN_POINT('Ctrl Pts',(-1.1806943421766,-0.459743797365995,
-1.43571505413252));
#37946=CARTESIAN_POINT('Ctrl Pts',(-1.25530379565404,-0.100950817236402,
-1.45672466500082));
#37947=CARTESIAN_POINT('Ctrl Pts',(-1.25775645832347,0.0628411125803556,
-1.46608791139449));
#37948=CARTESIAN_POINT('Ctrl Pts',(-1.1958299869675,0.413688700430408,-1.48653374157504));
#37949=CARTESIAN_POINT('Ctrl Pts',(-1.1241484394092,0.560291562992558,-1.49549654622063));
#37950=CARTESIAN_POINT('Ctrl Pts',(-0.969749982883845,0.803367902875652,
-1.51208747191069));
#37951=CARTESIAN_POINT('Ctrl Pts',(-0.856799218163433,0.923462389601029,
-1.52150714900259));
#37952=CARTESIAN_POINT('Ctrl Pts',(-0.656371658525956,1.06719626571009,
-1.53556970304047));
#37953=CARTESIAN_POINT('Ctrl Pts',(-0.582976315656834,1.10899652214491,
-1.54027990124189));
#37954=CARTESIAN_POINT('Ctrl Pts',(-0.426276585958984,1.17773985476701,
-1.55003464226733));
#37955=CARTESIAN_POINT('Ctrl Pts',(-0.343814511766357,1.20407158687264,
-1.55499493675363));
#37956=CARTESIAN_POINT('Ctrl Pts',(-0.259587618866585,1.2218769438964,-1.5599669049452));
#37957=CARTESIAN_POINT('',(-0.20156254994044,0.948825615807999,-1.27169584474002));
#37958=CARTESIAN_POINT('Ctrl Pts',(-0.201438348341829,0.948254165709337,
-1.27165078927618));
#37959=CARTESIAN_POINT('Ctrl Pts',(-0.0987243392846107,0.970265772525782,
-1.27940722318184));
#37960=CARTESIAN_POINT('Ctrl Pts',(0.025742728243312,0.980269531029446,
-1.28846139011945));
#37961=CARTESIAN_POINT('Ctrl Pts',(0.291387332434426,0.933304243270982,
-1.30840061727523));
#37962=CARTESIAN_POINT('Ctrl Pts',(0.412706897305448,0.886059866868016,
-1.31782131630864));
#37963=CARTESIAN_POINT('Ctrl Pts',(0.628779001349306,0.749481019437201,
-1.33669584090143));
#37964=CARTESIAN_POINT('Ctrl Pts',(0.720840663164924,0.661586296061749,
-1.34593034518707));
#37965=CARTESIAN_POINT('Ctrl Pts',(0.865891373452356,0.453145919229823,
-1.36468443540759));
#37966=CARTESIAN_POINT('Ctrl Pts',(0.917884397731031,0.336027550648247,
-1.37396188408488));
#37967=CARTESIAN_POINT('Ctrl Pts',(0.978638449230792,0.0708459015852234,
-1.39406340873307));
#37968=CARTESIAN_POINT('Ctrl Pts',(0.973931484966908,-0.0572846090069489,
-1.40334610908117));
#37969=CARTESIAN_POINT('Ctrl Pts',(0.934315968934639,-0.285437655104263,
-1.42043869301452));
#37970=CARTESIAN_POINT('Ctrl Pts',(0.890402125861612,-0.403268946572158,
-1.42955232512848));
#37971=CARTESIAN_POINT('Ctrl Pts',(0.747386626902557,-0.636741734663472,
-1.44979346804974));
#37972=CARTESIAN_POINT('Ctrl Pts',(0.651197130204398,-0.7255089437353,-1.45925267678724));
#37973=CARTESIAN_POINT('Ctrl Pts',(0.468727345569633,-0.856930153167856,
-1.47584686005623));
#37974=CARTESIAN_POINT('Ctrl Pts',(0.35746278354269,-0.909795858308654,
-1.48478614286536));
#37975=CARTESIAN_POINT('Ctrl Pts',(0.1151570245764,-0.97177230097435,-1.50328002186201));
#37976=CARTESIAN_POINT('Ctrl Pts',(-0.0163478393052635,-0.977573473079552,
-1.51280913661105));
#37977=CARTESIAN_POINT('Ctrl Pts',(-0.24511756325168,-0.943476331507244,
-1.52987822402024));
#37978=CARTESIAN_POINT('Ctrl Pts',(-0.366912073350283,-0.909760707379217,
-1.53902682080977));
#37979=CARTESIAN_POINT('Ctrl Pts',(-0.601745916092746,-0.771019708663982,
-1.55919027520204));
#37980=CARTESIAN_POINT('Ctrl Pts',(-0.698962539434374,-0.683420729699734,
-1.56865972305043));
#37981=CARTESIAN_POINT('Ctrl Pts',(-0.853060563983216,-0.478627690499707,
-1.58757991940138));
#37982=CARTESIAN_POINT('Ctrl Pts',(-0.907464882095679,-0.365840031027934,
-1.59666326338209));
#37983=CARTESIAN_POINT('Ctrl Pts',(-0.970164031430921,-0.119629985848702,
-1.61543304819782));
#37984=CARTESIAN_POINT('Ctrl Pts',(-0.977417294464398,0.00938936091313193,
-1.62478578587667));
#37985=CARTESIAN_POINT('Ctrl Pts',(-0.938831912985746,0.290717066024108,
-1.64576083733552));
#37986=CARTESIAN_POINT('Ctrl Pts',(-0.884427664631876,0.408880548362682,
-1.65516247785461));
#37987=CARTESIAN_POINT('Ctrl Pts',(-0.772729409729853,0.598010361875847,
-1.67137942123023));
#37988=CARTESIAN_POINT('Ctrl Pts',(-0.688892984793735,0.693427839352897,
-1.68057958647389));
#37989=CARTESIAN_POINT('Ctrl Pts',(-0.47320522420946,0.859859072888397,
-1.70071523986905));
#37990=CARTESIAN_POINT('Ctrl Pts',(-0.353507651838696,0.908978961000481,
-1.71007556689172));
#37991=CARTESIAN_POINT('Ctrl Pts',(-0.132446689760698,0.967814534797143,
-1.72695807869875));
#37992=CARTESIAN_POINT('Ctrl Pts',(-0.00829769730840238,0.977449939050657,
-1.73598818743995));
#37993=CARTESIAN_POINT('Ctrl Pts',(0.272743269789283,0.944831723940328,
-1.75690761159923));
#37994=CARTESIAN_POINT('Ctrl Pts',(0.397319123049025,0.889004983339358,
-1.76674624199313));
#37995=CARTESIAN_POINT('Ctrl Pts',(0.548463168641115,0.803242517078102,
-1.77957011362282));
#37996=CARTESIAN_POINT('Ctrl Pts',(0.657061179243573,0.731431679270879,
-1.7889560205575));
#37997=CARTESIAN_POINT('Ctrl Pts',(0.837016667682552,0.506409290281711,
-1.81025997391745));
#37998=CARTESIAN_POINT('Ctrl Pts',(0.896708335504385,0.389439444790983,
-1.81976380679888));
#37999=CARTESIAN_POINT('Ctrl Pts',(0.961575479660269,0.163480681552666,
-1.83711502517455));
#38000=CARTESIAN_POINT('Ctrl Pts',(0.980196107359684,0.0380929527140501,
-1.84629582853592));
#38001=CARTESIAN_POINT('Ctrl Pts',(0.949796426925332,-0.232115295912896,
-1.86639034333097));
#38002=CARTESIAN_POINT('Ctrl Pts',(0.910338156983544,-0.356057593387167,
-1.8758028786268));
#38003=CARTESIAN_POINT('Ctrl Pts',(0.787597338177108,-0.580417039662094,
-1.89468780385886));
#38004=CARTESIAN_POINT('Ctrl Pts',(0.705541931920857,-0.6778589619039,-1.90392980822176));
#38005=CARTESIAN_POINT('Ctrl Pts',(0.506633724951068,-0.835677971904184,
-1.92268092164057));
#38006=CARTESIAN_POINT('Ctrl Pts',(0.393146281041906,-0.894898742571985,
-1.93194942333464));
#38007=CARTESIAN_POINT('Ctrl Pts',(0.132370167545825,-0.972251332822704,
-1.95204858131521));
#38008=CARTESIAN_POINT('Ctrl Pts',(0.00409184961383161,-0.975578594338933,
-1.96133834340777));
#38009=CARTESIAN_POINT('Ctrl Pts',(-0.225854147439271,-0.950466860502563,
-1.9784118403135));
#38010=CARTESIAN_POINT('Ctrl Pts',(-0.346100609615679,-0.914145414198233,
-1.98751611263562));
#38011=CARTESIAN_POINT('Ctrl Pts',(-0.588320648121432,-0.786121492823868,
-2.00777069777945));
#38012=CARTESIAN_POINT('Ctrl Pts',(-0.683052440276743,-0.69553887469391,
-2.01724181646912));
#38013=CARTESIAN_POINT('Ctrl Pts',(-0.825486585716711,-0.522102941548972,
-2.0338032052662));
#38014=CARTESIAN_POINT('Ctrl Pts',(-0.885245303473489,-0.414549954481621,
-2.04273264368591));
#38015=CARTESIAN_POINT('Ctrl Pts',(-0.959910000303239,-0.184617722335591,
-2.06060876022976));
#38016=CARTESIAN_POINT('Ctrl Pts',(-0.974739175019373,-0.0624749986379006,
-2.06953819864937));
#38017=CARTESIAN_POINT('Ctrl Pts',(-0.961371621012054,0.161553609341053,
-2.08609958744636));
#38018=CARTESIAN_POINT('Ctrl Pts',(-0.937929646660384,0.290510179513987,
-2.0955707061359));
#38019=CARTESIAN_POINT('Ctrl Pts',(-0.817133378498537,0.536414496466936,
-2.11582529127975));
#38020=CARTESIAN_POINT('Ctrl Pts',(-0.741165879725267,0.636451480916373,
-2.12492956360197));
#38021=CARTESIAN_POINT('Ctrl Pts',(-0.569841157284668,0.791865766674289,
-2.14200306050775));
#38022=CARTESIAN_POINT('Ctrl Pts',(-0.464080472392323,0.864536772252278,
-2.15129282260037));
#38023=CARTESIAN_POINT('Ctrl Pts',(-0.207609487844088,0.955147139613408,
-2.17139198058076));
#38024=CARTESIAN_POINT('Ctrl Pts',(-0.0809805019614702,0.973898127262907,
-2.18066048227463));
#38025=CARTESIAN_POINT('Ctrl Pts',(0.172699493612926,0.96304572832147,-2.19941159569329));
#38026=CARTESIAN_POINT('Ctrl Pts',(0.296347838905441,0.932400914526673,
-2.20865360005613));
#38027=CARTESIAN_POINT('Ctrl Pts',(0.527483844276734,0.822954047256773,
-2.22753852528824));
#38028=CARTESIAN_POINT('Ctrl Pts',(0.632230525391237,0.745838672878308,
-2.23695106058418));
#38029=CARTESIAN_POINT('Ctrl Pts',(0.815578016510035,0.545039430606301,
-2.25704557537929));
#38030=CARTESIAN_POINT('Ctrl Pts',(0.874175039145334,0.432633028397699,
-2.26622637874067));
#38031=CARTESIAN_POINT('Ctrl Pts',(0.954433739868639,0.211672285202696,
-2.28357759711632));
#38032=CARTESIAN_POINT('Ctrl Pts',(0.97484957692162,0.0819486036372458,
-2.29308142999772));
#38033=CARTESIAN_POINT('Ctrl Pts',(0.961425884758658,-0.205868800031201,
-2.31438538335767));
#38034=CARTESIAN_POINT('Ctrl Pts',(0.915734610801314,-0.327781194058943,
-2.32377129029236));
#38035=CARTESIAN_POINT('Ctrl Pts',(0.843810636917658,-0.485979377101017,
-2.33659516192202));
#38036=CARTESIAN_POINT('Ctrl Pts',(0.775799049655197,-0.604344034746789,
-2.34643379231593));
#38037=CARTESIAN_POINT('Ctrl Pts',(0.567537098494545,-0.795851039430955,
-2.36735321647528));
#38038=CARTESIAN_POINT('Ctrl Pts',(0.461411930121172,-0.860991364727349,
-2.37638332521648));
#38039=CARTESIAN_POINT('Ctrl Pts',(0.247958153459323,-0.943253500169958,
-2.39326583702354));
#38040=CARTESIAN_POINT('Ctrl Pts',(0.122238049409607,-0.973826816597201,
-2.40262616404625));
#38041=CARTESIAN_POINT('Ctrl Pts',(-0.150080047920781,-0.965863184981861,
-2.42276181744138));
#38042=CARTESIAN_POINT('Ctrl Pts',(-0.273980275415678,-0.937902949273026,
-2.43196198268497));
#38043=CARTESIAN_POINT('Ctrl Pts',(-0.475482963183398,-0.850477247501373,
-2.44817892606057));
#38044=CARTESIAN_POINT('Ctrl Pts',(-0.588929238049058,-0.786818991819945,
-2.45758056657959));
#38045=CARTESIAN_POINT('Ctrl Pts',(-0.785433476719383,-0.581830715298323,
-2.47855561803846));
#38046=CARTESIAN_POINT('Ctrl Pts',(-0.855362821274623,-0.473163846227926,
-2.48790835571739));
#38047=CARTESIAN_POINT('Ctrl Pts',(-0.949273543111316,-0.237088972514691,
-2.50667814053319));
#38048=CARTESIAN_POINT('Ctrl Pts',(-0.97151099738917,-0.113855934794938,
-2.51576148451392));
#38049=CARTESIAN_POINT('Ctrl Pts',(-0.967127048588774,0.142400130630789,
-2.53468168086486));
#38050=CARTESIAN_POINT('Ctrl Pts',(-0.939921400836323,0.270402106005793,
-2.54415112871322));
#38051=CARTESIAN_POINT('Ctrl Pts',(-0.831398503477957,0.520639551586347,
-2.56431458310557));
#38052=CARTESIAN_POINT('Ctrl Pts',(-0.752647366453729,0.619477319761789,
-2.57346317989518));
#38053=CARTESIAN_POINT('Ctrl Pts',(-0.587553439321323,0.781471754486857,
-2.59053226730448));
#38054=CARTESIAN_POINT('Ctrl Pts',(-0.477728333010171,0.854036407356249,
-2.60006138205362));
#38055=CARTESIAN_POINT('Ctrl Pts',(-0.245237492311489,0.946238192940202,
-2.61855526105023));
#38056=CARTESIAN_POINT('Ctrl Pts',(-0.124140916952267,0.968825910384066,
-2.62749454385925));
#38057=CARTESIAN_POINT('Ctrl Pts',(0.100728002832542,0.969677678031112,
-2.64408872712811));
#38058=CARTESIAN_POINT('Ctrl Pts',(0.230717602518123,0.954356429549939,
-2.65354793586552));
#38059=CARTESIAN_POINT('Ctrl Pts',(0.483614457581144,0.849446199253691,
-2.6737890787866));
#38060=CARTESIAN_POINT('Ctrl Pts',(0.588376480529104,0.779893647824814,
-2.68290271090044));
#38061=CARTESIAN_POINT('Ctrl Pts',(0.754474219189705,0.618540796080992,
-2.69999529483371));
#38062=CARTESIAN_POINT('Ctrl Pts',(0.833559877872614,0.51761982775463,-2.70927799518176));
#38063=CARTESIAN_POINT('Ctrl Pts',(0.940190436386853,0.267335418003333,
-2.7293795198301));
#38064=CARTESIAN_POINT('Ctrl Pts',(0.966923459393054,0.142014500699619,
-2.73865696850759));
#38065=CARTESIAN_POINT('Ctrl Pts',(0.972003626913646,-0.111877781866718,
-2.75741105872829));
#38066=CARTESIAN_POINT('Ctrl Pts',(0.949143248594248,-0.237090541107069,
-2.766645563014));
#38067=CARTESIAN_POINT('Ctrl Pts',(0.854532540396059,-0.474555800893944,
-2.78552008760676));
#38068=CARTESIAN_POINT('Ctrl Pts',(0.784113881905431,-0.584062332473427,
-2.79494078664008));
#38069=CARTESIAN_POINT('Ctrl Pts',(0.596737734874605,-0.77813626180894,
-2.81488024895344));
#38070=CARTESIAN_POINT('Ctrl Pts',(0.490136541954605,-0.843165179166,-2.82393454260568));
#38071=CARTESIAN_POINT('Ctrl Pts',(0.394089470014046,-0.88569569080355,
-2.83169069737786));
#38072=CARTESIAN_POINT('',(-0.2597459052318,1.222715038231,-1.110008417723));
#38073=CARTESIAN_POINT('Ctrl Pts',(0.4032259446541,-0.8662939895831,0.2012068049836));
#38074=CARTESIAN_POINT('Ctrl Pts',(0.1988067354564,-0.9614431303197,0.1843067137916));
#38075=CARTESIAN_POINT('Ctrl Pts',(-0.2791972885623,-1.000404435832,0.1505065314076));
#38076=CARTESIAN_POINT('Ctrl Pts',(-0.8628093649628,-0.5784589040704,0.09980625783161));
#38077=CARTESIAN_POINT('Ctrl Pts',(-1.031587111702,0.1215641209151,0.04910598425561));
#38078=CARTESIAN_POINT('Ctrl Pts',(-0.7046871460694,0.7631430988109,-0.001594289320396));
#38079=CARTESIAN_POINT('Ctrl Pts',(-0.03913198596358,1.037997497496,-0.0522945628964));
#38080=CARTESIAN_POINT('Ctrl Pts',(0.6452242121113,0.8140361126302,-0.1029948364724));
#38081=CARTESIAN_POINT('Ctrl Pts',(1.01951635945,0.1988868585002,-0.1536951100484));
#38082=CARTESIAN_POINT('Ctrl Pts',(0.9038754829091,-0.5118384187131,-0.2043953836244));
#38083=CARTESIAN_POINT('Ctrl Pts',(0.353873640358,-0.9765976243727,-0.2550956572004));
#38084=CARTESIAN_POINT('Ctrl Pts',(-0.3661836412597,-0.972048875589,-0.3057959307764));
#38085=CARTESIAN_POINT('Ctrl Pts',(-0.9102698778482,-0.5003780799473,-0.3564962043524));
#38086=CARTESIAN_POINT('Ctrl Pts',(-1.016922220489,0.211751438319,-0.4071964779284));
#38087=CARTESIAN_POINT('Ctrl Pts',(-0.6348884498779,0.8221229410644,-0.4578967515044));
#38088=CARTESIAN_POINT('Ctrl Pts',(0.0522435497898,1.037419917643,-0.5085970250804));
#38089=CARTESIAN_POINT('Ctrl Pts',(0.7142696989558,0.7541805295677,-0.5592972986564));
#38090=CARTESIAN_POINT('Ctrl Pts',(1.033050636552,0.1085166178039,-0.6099975722324));
#38091=CARTESIAN_POINT('Ctrl Pts',(0.8553948853012,-0.5892953964066,-0.6606978458084));
#38092=CARTESIAN_POINT('Ctrl Pts',(0.2666756396737,-1.003919108903,-0.7113981193844));
#38093=CARTESIAN_POINT('Ctrl Pts',(-0.4501956701808,-0.9361054067588,-0.7620983929604));
#38094=CARTESIAN_POINT('Ctrl Pts',(-0.9507236181379,-0.4184424405686,-0.8127986665364));
#38095=CARTESIAN_POINT('Ctrl Pts',(-0.9943774606619,0.3003047437805,-0.8634989401124));
#38096=CARTESIAN_POINT('Ctrl Pts',(-0.5601791680333,0.8747392613582,-0.9141992136884));
#38097=CARTESIAN_POINT('Ctrl Pts',(0.1432155101674,1.028814264539,-0.9648994872644));
#38098=CARTESIAN_POINT('Ctrl Pts',(0.777787369792,0.6884883897838,-1.01559976084));
#38099=CARTESIAN_POINT('Ctrl Pts',(1.038590425217,0.01730659751134,-1.066300034416));
#38100=CARTESIAN_POINT('Ctrl Pts',(0.8002943153164,-0.6621918796188,-1.117000307992));
#38101=CARTESIAN_POINT('Ctrl Pts',(0.1774146655216,-1.023471618362,-1.167700581568));
#38102=CARTESIAN_POINT('Ctrl Pts',(-0.5307266205799,-0.8929169151192,-1.218400855144));
#38103=CARTESIAN_POINT('Ctrl Pts',(-0.9838090336742,-0.3332710455254,-1.26910112872));
#38104=CARTESIAN_POINT('Ctrl Pts',(-0.9641778538747,0.3865433611684,-1.319801402296));
#38105=CARTESIAN_POINT('Ctrl Pts',(-0.4809837433131,0.920551356439,-1.370501675872));
#38106=CARTESIAN_POINT('Ctrl Pts',(-0.00531754485576,0.9817681674502,-1.404301858256));
#38107=CARTESIAN_POINT('Ctrl Pts',(0.2144112878497,0.9311735812793,-1.421201949448));
#38108=CARTESIAN_POINT('Ctrl Pts',(0.446679448338,-0.9596498600741,0.1417550723552));
#38109=CARTESIAN_POINT('Ctrl Pts',(0.220231074158,-1.065052714869,0.1248549811632));
#38110=CARTESIAN_POINT('Ctrl Pts',(-0.3092848872596,-1.10821267192,0.09105479877921));
#38111=CARTESIAN_POINT('Ctrl Pts',(-0.9557897160936,-0.6407963266799,0.04035452520321));
#38112=CARTESIAN_POINT('Ctrl Pts',(-1.14275573801,0.1346644361256,-0.0103457483728));
#38113=CARTESIAN_POINT('Ctrl Pts',(-0.780627511276,0.8453829494337,-0.0610460219488));
#38114=CARTESIAN_POINT('Ctrl Pts',(-0.04334903082087,1.149856936799,-0.1117462955248));
#38115=CARTESIAN_POINT('Ctrl Pts',(0.714756574921,0.9017604311867,-0.1624465691008));
#38116=CARTESIAN_POINT('Ctrl Pts',(1.129384185339,0.2203198316338,-0.2131468426768));
#38117=CARTESIAN_POINT('Ctrl Pts',(1.001281309958,-0.5669965078887,-0.2638471162528));
#38118=CARTESIAN_POINT('Ctrl Pts',(0.3920087101342,-1.081840327703,-0.3145473898288));
#38119=CARTESIAN_POINT('Ctrl Pts',(-0.4056452940017,-1.076801384589,-0.3652476634048));
#38120=CARTESIAN_POINT('Ctrl Pts',(-1.008364794643,-0.5543011497017,-0.4159479369808));
#38121=CARTESIAN_POINT('Ctrl Pts',(-1.126510489895,0.2345707584224,-0.4666482105568));
#38122=CARTESIAN_POINT('Ctrl Pts',(-0.7033069828653,0.9107187338744,-0.5173484841328));
#38123=CARTESIAN_POINT('Ctrl Pts',(0.05787355776263,1.149217114254,-0.5680487577088));
#38124=CARTESIAN_POINT('Ctrl Pts',(0.7912427246413,0.8354545320332,-0.6187490312848));
#38125=CARTESIAN_POINT('Ctrl Pts',(1.144376979106,0.1202108733795,-0.6694493048608));
#38126=CARTESIAN_POINT('Ctrl Pts',(0.94757621761,-0.6528006098439,-0.7201495784368));
#38127=CARTESIAN_POINT('Ctrl Pts',(0.2954138472336,-1.112106102512,-0.7708498520128));
#38128=CARTESIAN_POINT('Ctrl Pts',(-0.4987108500002,-1.036984480341,-0.8215501255888));
#38129=CARTESIAN_POINT('Ctrl Pts',(-1.053178018186,-0.4635357446425,-0.8722503991648));
#38130=CARTESIAN_POINT('Ctrl Pts',(-1.101536201866,0.3326669800482,-0.9229506727408));
#38131=CARTESIAN_POINT('Ctrl Pts',(-0.6205466812466,0.9690052336249,-0.9736509463168));
#38132=CARTESIAN_POINT('Ctrl Pts',(0.1586490798104,1.139684075936,-1.024351219893));
#38133=CARTESIAN_POINT('Ctrl Pts',(0.8616053551838,0.7626831016531,-1.075051493469));
#38134=CARTESIAN_POINT('Ctrl Pts',(1.150513761169,0.01917163697293,-1.125751767045));
#38135=CARTESIAN_POINT('Ctrl Pts',(0.8865377538647,-0.7335527572161,-1.176452040621));
#38136=CARTESIAN_POINT('Ctrl Pts',(0.1965336952469,-1.133765681352,-1.227152314197));
#38137=CARTESIAN_POINT('Ctrl Pts',(-0.5879201902604,-0.9891417959213,-1.277852587773));
#38138=CARTESIAN_POINT('Ctrl Pts',(-1.08982887202,-0.369185883835,-1.328552861349));
#38139=CARTESIAN_POINT('Ctrl Pts',(-1.068082144957,0.4281990720453,-1.379253134925));
#38140=CARTESIAN_POINT('Ctrl Pts',(-0.5328167891255,1.019754253199,-1.429953408501));
#38141=CARTESIAN_POINT('Ctrl Pts',(-0.005890588227703,1.087568072557,-1.463753590885));
#38142=CARTESIAN_POINT('Ctrl Pts',(0.2375172457128,1.031521178404,-1.480653682077));
#38143=CARTESIAN_POINT('Ctrl Pts',(0.490132952022,-1.053005730565,0.08230333972681));
#38144=CARTESIAN_POINT('Ctrl Pts',(0.2416554128596,-1.168662299419,0.06540324853481));
#38145=CARTESIAN_POINT('Ctrl Pts',(-0.3393724859569,-1.216020908007,0.03160306615081));
#38146=CARTESIAN_POINT('Ctrl Pts',(-1.048770067224,-0.7031337492895,-0.01909720742519));
#38147=CARTESIAN_POINT('Ctrl Pts',(-1.253924364317,0.1477647513361,-0.0697974810012));
#38148=CARTESIAN_POINT('Ctrl Pts',(-0.8565678764825,0.9276228000565,-0.1204977545772));
#38149=CARTESIAN_POINT('Ctrl Pts',(-0.04756607567816,1.261716376102,-0.1711980281532));
#38150=CARTESIAN_POINT('Ctrl Pts',(0.7842889377307,0.9894847497432,-0.2218983017292));
#38151=CARTESIAN_POINT('Ctrl Pts',(1.239252011228,0.2417528047674,-0.2725985753052));
#38152=CARTESIAN_POINT('Ctrl Pts',(1.098687137006,-0.6221545970643,-0.3232988488812));
#38153=CARTESIAN_POINT('Ctrl Pts',(0.4301437799104,-1.187083031034,-0.3739991224572));
#38154=CARTESIAN_POINT('Ctrl Pts',(-0.4451069467436,-1.181553893589,-0.4246993960332));
#38155=CARTESIAN_POINT('Ctrl Pts',(-1.106459711439,-0.6082242194561,-0.4753996696092));
#38156=CARTESIAN_POINT('Ctrl Pts',(-1.236098759301,0.2573900785259,-0.5260999431852));
#38157=CARTESIAN_POINT('Ctrl Pts',(-0.7717255158527,0.9993145266845,-0.5768002167612));
#38158=CARTESIAN_POINT('Ctrl Pts',(0.06350356573547,1.261014310865,-0.6275004903372));
#38159=CARTESIAN_POINT('Ctrl Pts',(0.8682157503269,0.9167285344986,-0.6782007639132));
#38160=CARTESIAN_POINT('Ctrl Pts',(1.25570332166,0.1319051289551,-0.7289010374892));
#38161=CARTESIAN_POINT('Ctrl Pts',(1.039757549919,-0.7163058232812,-0.7796013110652));
#38162=CARTESIAN_POINT('Ctrl Pts',(0.3241520547935,-1.220293096121,-0.8303015846412));
#38163=CARTESIAN_POINT('Ctrl Pts',(-0.5472260298195,-1.137863553924,-0.8810018582172));
#38164=CARTESIAN_POINT('Ctrl Pts',(-1.155632418233,-0.5086290487165,-0.9317021317932));
#38165=CARTESIAN_POINT('Ctrl Pts',(-1.208694943071,0.365029216316,-0.9824024053692));
#38166=CARTESIAN_POINT('Ctrl Pts',(-0.6809141944598,1.063271205892,-1.033102678945));
#38167=CARTESIAN_POINT('Ctrl Pts',(0.1740826494533,1.250553887333,-1.083802952521));
#38168=CARTESIAN_POINT('Ctrl Pts',(0.9454233405756,0.8368778135224,-1.134503226097));
#38169=CARTESIAN_POINT('Ctrl Pts',(1.262437097122,0.02103667643451,-1.185203499673));
#38170=CARTESIAN_POINT('Ctrl Pts',(0.9727811924131,-0.8049136348134,-1.235903773249));
#38171=CARTESIAN_POINT('Ctrl Pts',(0.2156527249721,-1.244059744342,-1.286604046825));
#38172=CARTESIAN_POINT('Ctrl Pts',(-0.6451137599409,-1.085366676723,-1.337304320401));
#38173=CARTESIAN_POINT('Ctrl Pts',(-1.195848710366,-0.4051007221447,-1.388004593977));
#38174=CARTESIAN_POINT('Ctrl Pts',(-1.17198643604,0.4698547829221,-1.438704867553));
#38175=CARTESIAN_POINT('Ctrl Pts',(-0.5846498349379,1.118957149958,-1.489405141129));
#38176=CARTESIAN_POINT('Ctrl Pts',(-0.006463631599642,1.193367977664,-1.523205323513));
#38177=CARTESIAN_POINT('Ctrl Pts',(0.2606232035759,1.13186877553,-1.540105414705));
#38178=CARTESIAN_POINT('Ctrl Pts',(0.533586455706,-1.146361601056,0.02285160709841));
#38179=CARTESIAN_POINT('Ctrl Pts',(0.2630797515613,-1.272271883969,0.005951515906407));
#38180=CARTESIAN_POINT('Ctrl Pts',(-0.3694600846542,-1.323829144095,-0.02784866647759));
#38181=CARTESIAN_POINT('Ctrl Pts',(-1.141750418355,-0.7654711718991,-0.0785489400536));
#38182=CARTESIAN_POINT('Ctrl Pts',(-1.365092990625,0.1608650665466,-0.1292492136296));
#38183=CARTESIAN_POINT('Ctrl Pts',(-0.932508241689,1.009862650679,-0.1799494872056));
#38184=CARTESIAN_POINT('Ctrl Pts',(-0.05178312053545,1.373575815405,-0.2306497607816));
#38185=CARTESIAN_POINT('Ctrl Pts',(0.8538213005404,1.0772090683,-0.2813500343576));
#38186=CARTESIAN_POINT('Ctrl Pts',(1.349119837117,0.2631857779009,-0.3320503079336));
#38187=CARTESIAN_POINT('Ctrl Pts',(1.196092964055,-0.67731268624,-0.3827505815096));
#38188=CARTESIAN_POINT('Ctrl Pts',(0.4682788496866,-1.292325734365,-0.4334508550856));
#38189=CARTESIAN_POINT('Ctrl Pts',(-0.4845685994856,-1.286306402589,-0.4841511286616));
#38190=CARTESIAN_POINT('Ctrl Pts',(-1.204554628234,-0.6621472892105,-0.5348514022376));
#38191=CARTESIAN_POINT('Ctrl Pts',(-1.345687028708,0.2802093986293,-0.5855516758136));
#38192=CARTESIAN_POINT('Ctrl Pts',(-0.84014404884,1.087910319495,-0.6362519493896));
#38193=CARTESIAN_POINT('Ctrl Pts',(0.0691335737083,1.372811507476,-0.6869522229656));
#38194=CARTESIAN_POINT('Ctrl Pts',(0.9451887760124,0.9980025369641,-0.7376524965416));
#38195=CARTESIAN_POINT('Ctrl Pts',(1.367029664214,0.1435993845308,-0.7883527701176));
#38196=CARTESIAN_POINT('Ctrl Pts',(1.131938882228,-0.7798110367185,-0.8390530436936));
#38197=CARTESIAN_POINT('Ctrl Pts',(0.3528902623533,-1.32848008973,-0.8897533172696));
#38198=CARTESIAN_POINT('Ctrl Pts',(-0.5957412096389,-1.238742627507,-0.9404535908456));
#38199=CARTESIAN_POINT('Ctrl Pts',(-1.258086818281,-0.5537223527904,-0.9911538644216));
#38200=CARTESIAN_POINT('Ctrl Pts',(-1.315853684276,0.3973914525837,-1.041854137998));
#38201=CARTESIAN_POINT('Ctrl Pts',(-0.7412817076731,1.157537178158,-1.092554411574));
#38202=CARTESIAN_POINT('Ctrl Pts',(0.1895162190963,1.36142369873,-1.14325468515));
#38203=CARTESIAN_POINT('Ctrl Pts',(1.029241325967,0.9110725253918,-1.193954958726));
#38204=CARTESIAN_POINT('Ctrl Pts',(1.374360433074,0.0229017158961,-1.244655232302));
#38205=CARTESIAN_POINT('Ctrl Pts',(1.059024630961,-0.8762745124107,-1.295355505878));
#38206=CARTESIAN_POINT('Ctrl Pts',(0.2347717546974,-1.354353807332,-1.346055779454));
#38207=CARTESIAN_POINT('Ctrl Pts',(-0.7023073296214,-1.181591557525,-1.39675605303));
#38208=CARTESIAN_POINT('Ctrl Pts',(-1.301868548712,-0.4410155604543,-1.447456326606));
#38209=CARTESIAN_POINT('Ctrl Pts',(-1.275890727122,0.5115104937989,-1.498156600182));
#38210=CARTESIAN_POINT('Ctrl Pts',(-0.6364828807503,1.218160046718,-1.548856873758));
#38211=CARTESIAN_POINT('Ctrl Pts',(-0.007036674971584,1.299167882771,-1.582657056142));
#38212=CARTESIAN_POINT('Ctrl Pts',(0.2837291614389,1.232216372655,-1.599557147334));
#38213=CARTESIAN_POINT('',(-6.27395596736609E-7,1.24997530203264,-0.225010645721405));
#38214=CARTESIAN_POINT('Ctrl Pts',(-0.259605225442742,1.2221096527782,-1.11018313383523));
#38215=CARTESIAN_POINT('Ctrl Pts',(-0.332793343799699,1.20658875041188,
-1.10592121754818));
#38216=CARTESIAN_POINT('Ctrl Pts',(-0.404627231171491,1.18460760228849,
-1.10163375818886));
#38217=CARTESIAN_POINT('Ctrl Pts',(-0.540907581423731,1.12907020932194,
-1.09310261960631));
#38218=CARTESIAN_POINT('Ctrl Pts',(-0.605051057074797,1.09610920194188,
-1.08886731166991));
#38219=CARTESIAN_POINT('Ctrl Pts',(-0.707773733444926,1.03133277602085,
-1.08183127853167));
#38220=CARTESIAN_POINT('Ctrl Pts',(-0.747876095420288,1.00251248508937,
-1.07901758676475));
#38221=CARTESIAN_POINT('Ctrl Pts',(-0.902490851934647,0.876949291775734,
-1.06774084144926));
#38222=CARTESIAN_POINT('Ctrl Pts',(-1.0138428358634,0.751833092841553,-1.0586505729085));
#38223=CARTESIAN_POINT('Ctrl Pts',(-1.15509080823289,0.491421217862387,
-1.0413068606991));
#38224=CARTESIAN_POINT('Ctrl Pts',(-1.19657771566736,0.379998490744453,
-1.03436574906601));
#38225=CARTESIAN_POINT('Ctrl Pts',(-1.2388812299059,0.183548531329244,-1.02304603182886));
#38226=CARTESIAN_POINT('Ctrl Pts',(-1.24822862158008,0.101353967219403,
-1.01848558150274));
#38227=CARTESIAN_POINT('Ctrl Pts',(-1.25064592547273,-0.0636385446959788,
-1.00914796937442));
#38228=CARTESIAN_POINT('Ctrl Pts',(-1.24360156558463,-0.146207101339098,
-1.00435180784633));
#38229=CARTESIAN_POINT('Ctrl Pts',(-1.21423532252292,-0.305473346970245,
-0.994882212107024));
#38230=CARTESIAN_POINT('Ctrl Pts',(-1.19240456889098,-0.382419882142272,
-0.990208810300233));
#38231=CARTESIAN_POINT('Ctrl Pts',(-1.12389530484134,-0.557706864720993,
-0.979389360044569));
#38232=CARTESIAN_POINT('Ctrl Pts',(-1.07140580908498,-0.652703390758001,
-0.973454062146158));
#38233=CARTESIAN_POINT('Ctrl Pts',(-0.957706313327495,-0.806805752769416,
-0.962575907373815));
#38234=CARTESIAN_POINT('Ctrl Pts',(-0.901724979600007,-0.868706008625303,
-0.95778528251258));
#38235=CARTESIAN_POINT('Ctrl Pts',(-0.760433678514357,-0.997215776308453,
-0.946724551610701));
#38236=CARTESIAN_POINT('Ctrl Pts',(-0.629136492052712,-1.09917336210828,
-0.937280108523909));
#38237=CARTESIAN_POINT('Ctrl Pts',(-0.286239863661689,-1.22739413114836,
-0.916469035572465));
#38238=CARTESIAN_POINT('Ctrl Pts',(-0.120960966641227,-1.2541031443743,
-0.907128686921723));
#38239=CARTESIAN_POINT('Ctrl Pts',(0.208839532035743,-1.24344135072375,
-0.888124527877101));
#38240=CARTESIAN_POINT('Ctrl Pts',(0.369351146014912,-1.20548598183773,
-0.878658033949627));
#38241=CARTESIAN_POINT('Ctrl Pts',(0.653530517151995,-1.0748595082132,-0.86097736285615));
#38242=CARTESIAN_POINT('Ctrl Pts',(0.790494633015143,-0.983540006369001,
-0.851915963648905));
#38243=CARTESIAN_POINT('Ctrl Pts',(0.953029280869852,-0.81090557025396,
-0.838012247102954));
#38244=CARTESIAN_POINT('Ctrl Pts',(0.991988826150089,-0.762820428211738,
-0.834376907931348));
#38245=CARTESIAN_POINT('Ctrl Pts',(1.07322924803779,-0.645542409563646,
-0.826147306672509));
#38246=CARTESIAN_POINT('Ctrl Pts',(1.11272193143574,-0.574484813871174,
-0.821616299393835));
#38247=CARTESIAN_POINT('Ctrl Pts',(1.17942583426961,-0.421500002001213,
-0.812271789218584));
#38248=CARTESIAN_POINT('Ctrl Pts',(1.20574918191328,-0.339071245799685,
-0.80744115527922));
#38249=CARTESIAN_POINT('Ctrl Pts',(1.23707666683118,-0.188495172720685,
-0.798542895360767));
#38250=CARTESIAN_POINT('Ctrl Pts',(1.24548240634588,-0.121339319207742,
-0.794572714122722));
#38251=CARTESIAN_POINT('Ctrl Pts',(1.25116016900615,0.00698728876904618,
-0.787045887630086));
#38252=CARTESIAN_POINT('Ctrl Pts',(1.24941924339205,0.0681398408708604,
-0.783485541818798));
#38253=CARTESIAN_POINT('Ctrl Pts',(1.2339249163468,0.218447452511582,-0.774855578245345));
#38254=CARTESIAN_POINT('Ctrl Pts',(1.21484458608801,0.306985921576119,-0.76988232292773));
#38255=CARTESIAN_POINT('Ctrl Pts',(1.13817170855602,0.537816874620536,-0.756169063891392));
#38256=CARTESIAN_POINT('Ctrl Pts',(1.06292716185562,0.674062946336455,-0.74715663760518));
#38257=CARTESIAN_POINT('Ctrl Pts',(0.863239166447923,0.918638712550113,
-0.728857496300459));
#38258=CARTESIAN_POINT('Ctrl Pts',(0.737765941036426,1.02175471207368,-0.719966828231533));
#38259=CARTESIAN_POINT('Ctrl Pts',(0.450407462399465,1.17664995234507,-0.701312819538328));
#38260=CARTESIAN_POINT('Ctrl Pts',(0.290549704395172,1.22653947134232,-0.691803216516644));
#38261=CARTESIAN_POINT('Ctrl Pts',(-0.0690464104451976,1.26381173939837,
-0.670928898290121));
#38262=CARTESIAN_POINT('Ctrl Pts',(-0.232457553950564,1.23284703202773,
-0.661775424726093));
#38263=CARTESIAN_POINT('Ctrl Pts',(-0.422221745520559,1.17880981536598,
-0.650567281786364));
#38264=CARTESIAN_POINT('Ctrl Pts',(-0.49988825970878,1.14823635435013,-0.645820122340236));
#38265=CARTESIAN_POINT('Ctrl Pts',(-0.675688210706989,1.05778575460495,
-0.63433732422714));
#38266=CARTESIAN_POINT('Ctrl Pts',(-0.769326149939173,0.991764411544746,
-0.627632995995563));
#38267=CARTESIAN_POINT('Ctrl Pts',(-0.940227857022287,0.831585618564714,
-0.614362618801111));
#38268=CARTESIAN_POINT('Ctrl Pts',(-1.01560232478908,0.737510606305067,
-0.607753301954979));
#38269=CARTESIAN_POINT('Ctrl Pts',(-1.11731256009701,0.565318137788229,
-0.596307515497301));
#38270=CARTESIAN_POINT('Ctrl Pts',(-1.15146949806823,0.492073084034203,
-0.591572524153841));
#38271=CARTESIAN_POINT('Ctrl Pts',(-1.23762695617272,0.248876879143746,
-0.576429879567165));
#38272=CARTESIAN_POINT('Ctrl Pts',(-1.25549403921304,0.0854208148786327,
-0.567497360503563));
#38273=CARTESIAN_POINT('Ctrl Pts',(-1.2435576294284,-0.151614161959077,
-0.554097694180581));
#38274=CARTESIAN_POINT('Ctrl Pts',(-1.22928407832564,-0.2406361994489,-0.548885683063481));
#38275=CARTESIAN_POINT('Ctrl Pts',(-1.18465125529801,-0.405610547927827,
-0.53890480609632));
#38276=CARTESIAN_POINT('Ctrl Pts',(-1.15574468996294,-0.482337194960969,
-0.534126831413352));
#38277=CARTESIAN_POINT('Ctrl Pts',(-1.08203534383963,-0.631471820430162,
-0.524572690598339));
#38278=CARTESIAN_POINT('Ctrl Pts',(-1.03702148565761,-0.702882648383947,
-0.519898968031909));
#38279=CARTESIAN_POINT('Ctrl Pts',(-0.910841802069064,-0.863842420970694,
-0.508352193175204));
#38280=CARTESIAN_POINT('Ctrl Pts',(-0.822947338097478,-0.947547974950528,
-0.501423235127909));
#38281=CARTESIAN_POINT('Ctrl Pts',(-0.630595413860702,-1.08499069844033,
-0.487744504217735));
#38282=CARTESIAN_POINT('Ctrl Pts',(-0.483561323942755,-1.17152246765561,
-0.478109711456321));
#38283=CARTESIAN_POINT('Ctrl Pts',(-0.124038455487387,-1.25358912017759,
-0.457131876544059));
#38284=CARTESIAN_POINT('Ctrl Pts',(0.0401015968144676,-1.25900722545789,
-0.447984992876773));
#38285=CARTESIAN_POINT('Ctrl Pts',(0.278334007624253,-1.22110149435487,
-0.434047780606309));
#38286=CARTESIAN_POINT('Ctrl Pts',(0.355786009597055,-1.20096149810893,
-0.429370639175397));
#38287=CARTESIAN_POINT('Ctrl Pts',(0.509700848956409,-1.14427501326509,
-0.419895090107493));
#38288=CARTESIAN_POINT('Ctrl Pts',(0.585431982044724,-1.10717498072944,
-0.415154599429063));
#38289=CARTESIAN_POINT('Ctrl Pts',(0.726440296136035,-1.01980746202791,
-0.405808910950304));
#38290=CARTESIAN_POINT('Ctrl Pts',(0.79193847440835,-0.969854266302534,
-0.401199774458878));
#38291=CARTESIAN_POINT('Ctrl Pts',(0.926169591232099,-0.84503220543306,
-0.390708198653976));
#38292=CARTESIAN_POINT('Ctrl Pts',(0.99128315661927,-0.76773893124781,-0.384765925133727));
#38293=CARTESIAN_POINT('Ctrl Pts',(1.1056674942179,-0.592740847284177,-0.372559831060587));
#38294=CARTESIAN_POINT('Ctrl Pts',(1.15251793540906,-0.494962026616307,
-0.366525724523134));
#38295=CARTESIAN_POINT('Ctrl Pts',(1.211992125177,-0.314944289016718,-0.355916308375784));
#38296=CARTESIAN_POINT('Ctrl Pts',(1.23008311876091,-0.234572869544146,
-0.351298961060406));
#38297=CARTESIAN_POINT('Ctrl Pts',(1.25162567813202,-0.0594674105239562,
-0.341082907897881));
#38298=CARTESIAN_POINT('Ctrl Pts',(1.25262045616465,0.0352488940142594,
-0.335515074999312));
#38299=CARTESIAN_POINT('Ctrl Pts',(1.23180559406545,0.23879103312473,-0.323618943883807));
#38300=CARTESIAN_POINT('Ctrl Pts',(1.20612903123305,0.345765504090371,-0.317532801802942));
#38301=CARTESIAN_POINT('Ctrl Pts',(1.11630809624336,0.578614762255521,-0.303513296923535));
#38302=CARTESIAN_POINT('Ctrl Pts',(1.04407223873877,0.69991393392008,-0.295409808134786));
#38303=CARTESIAN_POINT('Ctrl Pts',(0.901474408285513,0.869328395269686,
-0.282544897417378));
#38304=CARTESIAN_POINT('Ctrl Pts',(0.842103580503381,0.927316454384216,
-0.277758230779022));
#38305=CARTESIAN_POINT('Ctrl Pts',(0.7128421979089,1.03016942444653,-0.268352130319226));
#38306=CARTESIAN_POINT('Ctrl Pts',(0.643326063905394,1.07469652485503,-0.263721551697975));
#38307=CARTESIAN_POINT('Ctrl Pts',(0.481942935922786,1.15691777598009,-0.253411516358004));
#38308=CARTESIAN_POINT('Ctrl Pts',(0.388650741524565,1.19137466480566,-0.247759035619074));
#38309=CARTESIAN_POINT('Ctrl Pts',(0.197097186680785,1.23781549769892,-0.236421653898855));
#38310=CARTESIAN_POINT('Ctrl Pts',(0.098659664897847,1.24992163553485,-0.230723881923306));
#38311=CARTESIAN_POINT('Ctrl Pts',(-6.27396302407881E-7,1.24997530203264,
-0.225010645721364));
#38312=CARTESIAN_POINT('',(0.000261740803262159,-1.24944061383241,-1.10756895875068E-17));
#38313=CARTESIAN_POINT('Ctrl Pts',(0.000250820037674612,-1.24944062023903,
-8.31504902660109E-5));
#38314=CARTESIAN_POINT('Ctrl Pts',(-0.133757168394608,-1.24960261218778,
-0.00770034556823749));
#38315=CARTESIAN_POINT('Ctrl Pts',(-0.294458227534603,-1.22918577895942,
-0.0167176425491502));
#38316=CARTESIAN_POINT('Ctrl Pts',(-0.617257941985387,-1.09834322766392,
-0.0368409886524448));
#38317=CARTESIAN_POINT('Ctrl Pts',(-0.756097898427124,-1.00766451211646,
-0.0462884129246149));
#38318=CARTESIAN_POINT('Ctrl Pts',(-0.931307333688564,-0.837492637847146,
-0.0601764677254039));
#38319=CARTESIAN_POINT('Ctrl Pts',(-0.983901742932066,-0.775245228369939,
-0.0647038041558236));
#38320=CARTESIAN_POINT('Ctrl Pts',(-1.07689915920209,-0.639776624696279,
-0.0740181627002627));
#38321=CARTESIAN_POINT('Ctrl Pts',(-1.11671817330185,-0.566878286914523,
-0.0788188276728031));
#38322=CARTESIAN_POINT('Ctrl Pts',(-1.18393443259893,-0.408967913919388,
-0.0888250499830544));
#38323=CARTESIAN_POINT('Ctrl Pts',(-1.21017638688533,-0.323286163379387,
-0.0940389468331596));
#38324=CARTESIAN_POINT('Ctrl Pts',(-1.24216459446644,-0.157877480752195,
-0.103691420051535));
#38325=CARTESIAN_POINT('Ctrl Pts',(-1.24971357675157,-0.0790974806829304,
-0.108085773361406));
#38326=CARTESIAN_POINT('Ctrl Pts',(-1.24988593361916,0.180418214864625,
-0.122611971346616));
#38327=CARTESIAN_POINT('Ctrl Pts',(-1.21089420993376,0.339040334133182,
-0.132125186565245));
#38328=CARTESIAN_POINT('Ctrl Pts',(-1.1187141109918,0.566425990040005,-0.14640077042418));
#38329=CARTESIAN_POINT('Ctrl Pts',(-1.06707412558697,0.658374409984222,
-0.152274352254586));
#38330=CARTESIAN_POINT('Ctrl Pts',(-0.956624024988722,0.808168419043991,
-0.162709266732783));
#38331=CARTESIAN_POINT('Ctrl Pts',(-0.901806032273976,0.869170379558039,
-0.16729669577124));
#38332=CARTESIAN_POINT('Ctrl Pts',(-0.791635807660082,0.969568013609325,
-0.175918025352255));
#38333=CARTESIAN_POINT('Ctrl Pts',(-0.738127885519106,1.01083833790894,
-0.179895394613272));
#38334=CARTESIAN_POINT('Ctrl Pts',(-0.580657072298911,1.11300758383781,
-0.190853149459495));
#38335=CARTESIAN_POINT('Ctrl Pts',(-0.470261305987306,1.16362448208699,
-0.197671271948075));
#38336=CARTESIAN_POINT('Ctrl Pts',(-0.240422179831552,1.23203934577827,
-0.21123374577893));
#38337=CARTESIAN_POINT('Ctrl Pts',(-0.120522818343935,1.25004086036163,
-0.218031427147732));
#38338=CARTESIAN_POINT('Ctrl Pts',(-6.27395597339278E-7,1.24997530203264,
-0.225010645721405));
#38339=CARTESIAN_POINT('',(-0.750030728394555,0.614591155635446,2.91990672313832E-5));
#38340=CARTESIAN_POINT('Ctrl Pts',(-0.750067840413312,0.61462509807075,
1.40946282423116E-17));
#38341=CARTESIAN_POINT('Ctrl Pts',(-0.809882553799936,0.557747719474187,
1.47833675193833E-17));
#38342=CARTESIAN_POINT('Ctrl Pts',(-0.862349497861938,0.493132905553222,
-4.34146451643364E-14));
#38343=CARTESIAN_POINT('Ctrl Pts',(-0.951569996446674,0.351090626404901,
-4.34169746916308E-14));
#38344=CARTESIAN_POINT('Ctrl Pts',(-0.987840882420652,0.27321621504591,
-4.32888744424384E-14));
#38345=CARTESIAN_POINT('Ctrl Pts',(-1.06248896738419,0.0396486927506802,
-4.32921841402061E-14));
#38346=CARTESIAN_POINT('Ctrl Pts',(-1.06751788595683,-0.101067592918028,
-4.36369690381966E-14));
#38347=CARTESIAN_POINT('Ctrl Pts',(-1.04580751638871,-0.351127201170586,
-4.36369690381966E-14));
#38348=CARTESIAN_POINT('Ctrl Pts',(-1.0082451256689,-0.485854779973621,
-4.39388442066686E-14));
#38349=CARTESIAN_POINT('Ctrl Pts',(-0.87764068444681,-0.7489867036794,-4.39424836500747E-14));
#38350=CARTESIAN_POINT('Ctrl Pts',(-0.783955290032865,-0.861345679857431,
-4.37323788293753E-14));
#38351=CARTESIAN_POINT('Ctrl Pts',(-0.59508582408829,-1.03154986337642,
-4.37323788293753E-14));
#38352=CARTESIAN_POINT('Ctrl Pts',(-0.488478947016535,-1.10097347077607,
-4.37150315946155E-14));
#38353=CARTESIAN_POINT('Ctrl Pts',(-0.256010239028481,-1.20416167455751,
-4.37150315946155E-14));
#38354=CARTESIAN_POINT('Ctrl Pts',(-0.131274571541265,-1.23651444295296,
-9.87156134091518E-19));
#38355=CARTESIAN_POINT('Ctrl Pts',(0.000261567582557562,-1.24929773378779,
-1.551537897789E-18));
#38356=CARTESIAN_POINT('Ctrl Pts',(-0.749485555563958,0.615178325934084,
-1.00645712846747E-9));
#38357=CARTESIAN_POINT('Ctrl Pts',(-0.691520344892466,0.685982827107283,
-0.00665992653678659));
#38358=CARTESIAN_POINT('Ctrl Pts',(-0.626014663918608,0.746342019032374,
-0.0133903488232786));
#38359=CARTESIAN_POINT('Ctrl Pts',(-0.48111095763836,0.846675629347526,
-0.0266157197187053));
#38360=CARTESIAN_POINT('Ctrl Pts',(-0.402197526342482,0.886528754234619,
-0.0330223634080707));
#38361=CARTESIAN_POINT('Ctrl Pts',(-0.238934813994007,0.943471759217515,
-0.0456276817308198));
#38362=CARTESIAN_POINT('Ctrl Pts',(-0.115826409566955,0.975260036400719,
-0.0547106245734519));
#38363=CARTESIAN_POINT('Ctrl Pts',(0.164263817962017,0.964276610736639,
-0.0756311165135602));
#38364=CARTESIAN_POINT('Ctrl Pts',(0.290738210007054,0.93356407375508,-0.0850937529442948));
#38365=CARTESIAN_POINT('Ctrl Pts',(0.471484943071061,0.85048861220488,-0.0997098803749702));
#38366=CARTESIAN_POINT('Ctrl Pts',(0.553331236734125,0.804677385467775,
-0.106422351683403));
#38367=CARTESIAN_POINT('Ctrl Pts',(0.685919407220429,0.688542270735864,
-0.119427545256577));
#38368=CARTESIAN_POINT('Ctrl Pts',(0.730011830464401,0.641340091837972,
-0.124237753090772));
#38369=CARTESIAN_POINT('Ctrl Pts',(0.837073888756735,0.501697000330135,
-0.137407244034439));
#38370=CARTESIAN_POINT('Ctrl Pts',(0.890067026179102,0.401433006390183,
-0.145762637896906));
#38371=CARTESIAN_POINT('Ctrl Pts',(0.937995412326277,0.251339217130985,
-0.157129989608011));
#38372=CARTESIAN_POINT('Ctrl Pts',(0.948722183341347,0.206675013450165,
-0.160392202885067));
#38373=CARTESIAN_POINT('Ctrl Pts',(0.966841915727626,0.0978769514002914,
-0.16847170289435));
#38374=CARTESIAN_POINT('Ctrl Pts',(0.971099109898709,0.0332044837877513,
-0.173336332219429));
#38375=CARTESIAN_POINT('Ctrl Pts',(0.967109275650522,-0.0922210214390128,
-0.182824410034968));
#38376=CARTESIAN_POINT('Ctrl Pts',(0.959517392720682,-0.153054110414589,
-0.187448619923345));
#38377=CARTESIAN_POINT('Ctrl Pts',(0.93214355099431,-0.276126422630988,
-0.196804854482268));
#38378=CARTESIAN_POINT('Ctrl Pts',(0.911745488645913,-0.337497518214735,
-0.201414941440259));
#38379=CARTESIAN_POINT('Ctrl Pts',(0.871687644696651,-0.426322591305666,
-0.208342672883873));
#38380=CARTESIAN_POINT('Ctrl Pts',(0.856929712329002,-0.455088174577703,
-0.210646074157641));
#38381=CARTESIAN_POINT('Ctrl Pts',(0.79817844630675,-0.55688844568411,-0.219226576125532));
#38382=CARTESIAN_POINT('Ctrl Pts',(0.745902330282399,-0.625206381972658,
-0.225805894744982));
#38383=CARTESIAN_POINT('Ctrl Pts',(0.65741174802194,-0.714092647241932,
-0.235350413404771));
#38384=CARTESIAN_POINT('Ctrl Pts',(0.627290301908243,-0.740832051278823,
-0.238389348669223));
#38385=CARTESIAN_POINT('Ctrl Pts',(0.558112227078551,-0.794812864846272,
-0.244885578166819));
#38386=CARTESIAN_POINT('Ctrl Pts',(0.518730216599021,-0.820992168547267,
-0.248261446274541));
#38387=CARTESIAN_POINT('Ctrl Pts',(0.442762049537832,-0.863751369927401,
-0.254433632373426));
#38388=CARTESIAN_POINT('Ctrl Pts',(0.406828890414051,-0.881133535967991,
-0.257239594387939));
#38389=CARTESIAN_POINT('Ctrl Pts',(0.337922691941123,-0.909442434782747,
-0.262605528275797));
#38390=CARTESIAN_POINT('Ctrl Pts',(0.305172653215591,-0.920914951539425,
-0.265161727418624));
#38391=CARTESIAN_POINT('Ctrl Pts',(0.208833043339074,-0.949078965083362,
-0.272720576179139));
#38392=CARTESIAN_POINT('Ctrl Pts',(0.143883729565482,-0.961233950332467,
-0.277833572029439));
#38393=CARTESIAN_POINT('Ctrl Pts',(0.0474934194474711,-0.969260940555831,
-0.285200154333576));
#38394=CARTESIAN_POINT('Ctrl Pts',(0.0164729529270842,-0.970342851269044,
-0.287537796531342));
#38395=CARTESIAN_POINT('Ctrl Pts',(-0.0653424655873088,-0.969146078894895,
-0.293578410026805));
#38396=CARTESIAN_POINT('Ctrl Pts',(-0.115961921977653,-0.964260454480337,
-0.297175859780403));
#38397=CARTESIAN_POINT('Ctrl Pts',(-0.219326353346127,-0.946082009489617,
-0.304602214808625));
#38398=CARTESIAN_POINT('Ctrl Pts',(-0.272046588834085,-0.932185270994219,
-0.308438650414657));
#38399=CARTESIAN_POINT('Ctrl Pts',(-0.388457131395581,-0.89101105826433,
-0.317508561425316));
#38400=CARTESIAN_POINT('Ctrl Pts',(-0.451243879102635,-0.861103249574949,
-0.322888442321947));
#38401=CARTESIAN_POINT('Ctrl Pts',(-0.536924828764396,-0.80837273831466,
-0.330617878612817));
#38402=CARTESIAN_POINT('Ctrl Pts',(-0.56292256459701,-0.790562087639446,
-0.333020777544854));
#38403=CARTESIAN_POINT('Ctrl Pts',(-0.655459430115703,-0.720081713362681,
-0.341718175884925));
#38404=CARTESIAN_POINT('Ctrl Pts',(-0.715775943532788,-0.659618235498914,
-0.347651089220564));
#38405=CARTESIAN_POINT('Ctrl Pts',(-0.78938680568236,-0.564076306987063,
-0.356257395470773));
#38406=CARTESIAN_POINT('Ctrl Pts',(-0.809829274119129,-0.534301363634571,
-0.358851432426246));
#38407=CARTESIAN_POINT('Ctrl Pts',(-0.857148042928083,-0.456585611588798,
-0.36554070102133));
#38408=CARTESIAN_POINT('Ctrl Pts',(-0.881793208184187,-0.407291199819409,
-0.369757859596612));
#38409=CARTESIAN_POINT('Ctrl Pts',(-0.915140502090481,-0.323377452942217,
-0.376703795174359));
#38410=CARTESIAN_POINT('Ctrl Pts',(-0.926413362915516,-0.289723950008743,
-0.379424856895539));
#38411=CARTESIAN_POINT('Ctrl Pts',(-0.949217677992506,-0.206078634024043,
-0.385930058678096));
#38412=CARTESIAN_POINT('Ctrl Pts',(-0.95864053732603,-0.155610638698208,
-0.389652058555324));
#38413=CARTESIAN_POINT('Ctrl Pts',(-0.969801649691148,-0.0507346562473078,
-0.397241599742637));
#38414=CARTESIAN_POINT('Ctrl Pts',(-0.971042800459035,0.00372980374851009,
-0.401105959396232));
#38415=CARTESIAN_POINT('Ctrl Pts',(-0.964781747558175,0.108989751510079,
-0.408723240957605));
#38416=CARTESIAN_POINT('Ctrl Pts',(-0.957774403787605,0.159842111318367,
-0.412474409006774));
#38417=CARTESIAN_POINT('Ctrl Pts',(-0.936386151240434,0.257402756862024,
-0.420023567590751));
#38418=CARTESIAN_POINT('Ctrl Pts',(-0.922354447477273,0.304279775572638,
-0.423797646603852));
#38419=CARTESIAN_POINT('Ctrl Pts',(-0.876119748295039,0.423693609136073,
-0.433462572432769));
#38420=CARTESIAN_POINT('Ctrl Pts',(-0.838231267092757,0.493856015239188,
-0.439224044298467));
#38421=CARTESIAN_POINT('Ctrl Pts',(-0.750851903981765,0.617560390565297,
-0.45018890711371));
#38422=CARTESIAN_POINT('Ctrl Pts',(-0.702623906629978,0.672054807996416,
-0.455405243399353));
#38423=CARTESIAN_POINT('Ctrl Pts',(-0.61200683040724,0.754041925758708,
-0.464422790609882));
#38424=CARTESIAN_POINT('Ctrl Pts',(-0.572430898513051,0.784671935337174,
-0.468192630225527));
#38425=CARTESIAN_POINT('Ctrl Pts',(-0.42528387712119,0.880845379749878,
-0.481445694398355));
#38426=CARTESIAN_POINT('Ctrl Pts',(-0.306094576674206,0.928412167081991,
-0.490662182298744));
#38427=CARTESIAN_POINT('Ctrl Pts',(-0.0580387459248825,0.976280702919913,
-0.509137535815805));
#38428=CARTESIAN_POINT('Ctrl Pts',(0.0673226445171873,0.976182205587661,
-0.5182088722675));
#38429=CARTESIAN_POINT('Ctrl Pts',(0.316083555754992,0.925111746696705,
-0.537108943756486));
#38430=CARTESIAN_POINT('Ctrl Pts',(0.434544326120844,0.875853962304653,
-0.546484461318104));
#38431=CARTESIAN_POINT('Ctrl Pts',(0.595730525638291,0.768532624929862,
-0.560666972570654));
#38432=CARTESIAN_POINT('Ctrl Pts',(0.647507647599943,0.725427789814852,
-0.565481489071531));
#38433=CARTESIAN_POINT('Ctrl Pts',(0.771623016477007,0.597458990055328,
-0.578599412540456));
#38434=CARTESIAN_POINT('Ctrl Pts',(0.834953406182651,0.504894658297685,
-0.587009219997219));
#38435=CARTESIAN_POINT('Ctrl Pts',(0.913148157900059,0.335498841908481,
-0.600918696671118));
#38436=CARTESIAN_POINT('Ctrl Pts',(0.937025197171096,0.262572447747291,
-0.606489962377818));
#38437=CARTESIAN_POINT('Ctrl Pts',(0.96211804984445,0.133913557420753,-0.615862958247662));
#38438=CARTESIAN_POINT('Ctrl Pts',(0.96793885815068,0.0799127885607206,
-0.619764510095875));
#38439=CARTESIAN_POINT('Ctrl Pts',(0.971270407808221,-0.0536288537972403,
-0.629707374053931));
#38440=CARTESIAN_POINT('Ctrl Pts',(0.963618744815539,-0.133350948918856,
-0.635805461263067));
#38441=CARTESIAN_POINT('Ctrl Pts',(0.934684022216928,-0.264515812148018,
-0.645935617275956));
#38442=CARTESIAN_POINT('Ctrl Pts',(0.918344524967836,-0.317102670203463,
-0.650023894001686));
#38443=CARTESIAN_POINT('Ctrl Pts',(0.88093418694075,-0.408375981736267,
-0.657144069358296));
#38444=CARTESIAN_POINT('Ctrl Pts',(0.861505526854446,-0.447688550533692,
-0.660221153294291));
#38445=CARTESIAN_POINT('Ctrl Pts',(0.818634181423107,-0.521432643019005,
-0.666290778824999));
#38446=CARTESIAN_POINT('Ctrl Pts',(0.795448704704568,-0.556002997167771,
-0.669292859829739));
#38447=CARTESIAN_POINT('Ctrl Pts',(0.726083876580491,-0.646524696234794,
-0.677783861362529));
#38448=CARTESIAN_POINT('Ctrl Pts',(0.675617822908381,-0.699242006906682,
-0.683396820829173));
#38449=CARTESIAN_POINT('Ctrl Pts',(0.583580615244474,-0.776112140596742,
-0.692525787113359));
#38450=CARTESIAN_POINT('Ctrl Pts',(0.544956949962885,-0.803848212499719,
-0.696095953845777));
#38451=CARTESIAN_POINT('Ctrl Pts',(0.477884260938761,-0.844685356806632,
-0.701817575538396));
#38452=CARTESIAN_POINT('Ctrl Pts',(0.450525645314577,-0.85952961025533,
-0.704033736041437));
#38453=CARTESIAN_POINT('Ctrl Pts',(0.363625550595281,-0.901361797886043,
-0.710867230111145));
#38454=CARTESIAN_POINT('Ctrl Pts',(0.301857203280628,-0.923702600477772,
-0.715444995721303));
#38455=CARTESIAN_POINT('Ctrl Pts',(0.188452732200309,-0.952442397040851,
-0.724108234250529));
#38456=CARTESIAN_POINT('Ctrl Pts',(0.137386209506803,-0.96120634008556,
-0.728077126307842));
#38457=CARTESIAN_POINT('Ctrl Pts',(0.029045336628559,-0.971079074828047,
-0.736444084393938));
#38458=CARTESIAN_POINT('Ctrl Pts',(-0.0283379223967618,-0.971271313100352,
-0.740841700768136));
#38459=CARTESIAN_POINT('Ctrl Pts',(-0.137706274659779,-0.961615230071308,
-0.748946462498991));
#38460=CARTESIAN_POINT('Ctrl Pts',(-0.189712132252472,-0.952572327642054,
-0.752680183344212));
#38461=CARTESIAN_POINT('Ctrl Pts',(-0.297558271626115,-0.92469155413691,
-0.760570659714922));
#38462=CARTESIAN_POINT('Ctrl Pts',(-0.353134000454666,-0.904834935521383,
-0.764729186214));
#38463=CARTESIAN_POINT('Ctrl Pts',(-0.433587763705638,-0.867731809970381,
-0.771275474762301));
#38464=CARTESIAN_POINT('Ctrl Pts',(-0.460115617634662,-0.854008763357978,
-0.773532975406683));
#38465=CARTESIAN_POINT('Ctrl Pts',(-0.538944921022525,-0.808557613284767,
-0.780492826456917));
#38466=CARTESIAN_POINT('Ctrl Pts',(-0.589072542125404,-0.773045633364942,
-0.785266151052505));
#38467=CARTESIAN_POINT('Ctrl Pts',(-0.670211461650972,-0.702760392407441,
-0.793324680399299));
#38468=CARTESIAN_POINT('Ctrl Pts',(-0.702805900693151,-0.66999869322811,
-0.796672630188785));
#38469=CARTESIAN_POINT('Ctrl Pts',(-0.78233279965786,-0.577811931065102,
-0.805404264469002));
#38470=CARTESIAN_POINT('Ctrl Pts',(-0.825087301881679,-0.514676999541364,
-0.810728582252462));
#38471=CARTESIAN_POINT('Ctrl Pts',(-0.880434048504769,-0.408558473588861,
-0.819489984580917));
#38472=CARTESIAN_POINT('Ctrl Pts',(-0.898163875161468,-0.368204861415813,
-0.822804768713365));
#38473=CARTESIAN_POINT('Ctrl Pts',(-0.930208860998752,-0.279316122077531,
-0.830043067073164));
#38474=CARTESIAN_POINT('Ctrl Pts',(-0.943651535328424,-0.230373629098725,
-0.833956404373398));
#38475=CARTESIAN_POINT('Ctrl Pts',(-0.966335841184824,-0.109950723894625,
-0.843124312315739));
#38476=CARTESIAN_POINT('Ctrl Pts',(-0.97157941071164,-0.0380282375235174,
-0.848283775586799));
#38477=CARTESIAN_POINT('Ctrl Pts',(-0.966088027504813,0.114896524809793,
-0.859281137041708));
#38478=CARTESIAN_POINT('Ctrl Pts',(-0.95310172230759,0.195876161046513,
-0.865129935021918));
#38479=CARTESIAN_POINT('Ctrl Pts',(-0.918435757121371,0.314593071809577,
-0.87441646900891));
#38480=CARTESIAN_POINT('Ctrl Pts',(-0.903903884112642,0.354459195987018,
-0.877670783324424));
#38481=CARTESIAN_POINT('Ctrl Pts',(-0.860546750461119,0.452274810527204,
-0.885775133373804));
#38482=CARTESIAN_POINT('Ctrl Pts',(-0.828253384759571,0.50859402221818,
-0.890546529256785));
#38483=CARTESIAN_POINT('Ctrl Pts',(-0.720433024176727,0.65990956703673,
-0.90412234912441));
#38484=CARTESIAN_POINT('Ctrl Pts',(-0.631664981090838,0.745716425089765,
-0.912829925791812));
#38485=CARTESIAN_POINT('Ctrl Pts',(-0.476618706517394,0.847317999288356,
-0.926673505026629));
#38486=CARTESIAN_POINT('Ctrl Pts',(-0.419945460265682,0.876638661709985,
-0.93145667890111));
#38487=CARTESIAN_POINT('Ctrl Pts',(-0.243307508699527,0.94696398470386,
-0.945583159110242));
#38488=CARTESIAN_POINT('Ctrl Pts',(-0.11654790194724,0.970817054884752,
-0.954851035349461));
#38489=CARTESIAN_POINT('Ctrl Pts',(0.0727293711116787,0.969303096643114,
-0.968730319005118));
#38490=CARTESIAN_POINT('Ctrl Pts',(0.134962790795066,0.962658818848594,
-0.973292180744191));
#38491=CARTESIAN_POINT('Ctrl Pts',(0.316775418871325,0.924637990171389,
-0.98705329882165));
#38492=CARTESIAN_POINT('Ctrl Pts',(0.432175375890316,0.876436011350086,
-0.996300528584387));
#38493=CARTESIAN_POINT('Ctrl Pts',(0.639110439441325,0.740299900579539,
-1.01459255276467));
#38494=CARTESIAN_POINT('Ctrl Pts',(0.727700888215557,0.653091805650583,
-1.0232355501562));
#38495=CARTESIAN_POINT('Ctrl Pts',(0.871881721970838,0.443330411650751,
-1.04224793536479));
#38496=CARTESIAN_POINT('Ctrl Pts',(0.924412601499112,0.321183448355106,
-1.05225574397271));
#38497=CARTESIAN_POINT('Ctrl Pts',(0.960404105110912,0.145014724677346,
-1.06526952055553));
#38498=CARTESIAN_POINT('Ctrl Pts',(0.966421868613754,0.095847093404394,
-1.06874606528881));
#38499=CARTESIAN_POINT('Ctrl Pts',(0.970729240872516,0.00187689603276803,
-1.0755116092022));
#38500=CARTESIAN_POINT('Ctrl Pts',(0.969681721175105,-0.042983065569024,
-1.07881945506364));
#38501=CARTESIAN_POINT('Ctrl Pts',(0.959834904353882,-0.150613410626042,
-1.08694389716873));
#38502=CARTESIAN_POINT('Ctrl Pts',(0.947993986329022,-0.213147916679648,
-1.09180528355103));
#38503=CARTESIAN_POINT('Ctrl Pts',(0.91650765643918,-0.320938744543342,
-1.10030805612764));
#38504=CARTESIAN_POINT('Ctrl Pts',(0.899234303655736,-0.366914797765025,
-1.10397668870833));
#38505=CARTESIAN_POINT('Ctrl Pts',(0.863181522759483,-0.444015255370893,
-1.1101697508737));
#38506=CARTESIAN_POINT('Ctrl Pts',(0.846026395087111,-0.475758637002667,
-1.1127263083037));
#38507=CARTESIAN_POINT('Ctrl Pts',(0.798792801753869,-0.552547557874234,
-1.11910921362408));
#38508=CARTESIAN_POINT('Ctrl Pts',(0.766517069542252,-0.596285269892296,
-1.12294200679953));
#38509=CARTESIAN_POINT('Ctrl Pts',(0.709453468724753,-0.661624638763062,
-1.12936425172609));
#38510=CARTESIAN_POINT('Ctrl Pts',(0.686807319865723,-0.685101926287355,
-1.13182699222252));
#38511=CARTESIAN_POINT('Ctrl Pts',(0.61169482423289,-0.755632958071713,
-1.13968210824357));
#38512=CARTESIAN_POINT('Ctrl Pts',(0.555141377307848,-0.79838321724767,
-1.14515031283205));
#38513=CARTESIAN_POINT('Ctrl Pts',(0.460693609271441,-0.854546637786924,
-1.15335827155446));
#38514=CARTESIAN_POINT('Ctrl Pts',(0.425801821844024,-0.872433493271216,
-1.15620343196439));
#38515=CARTESIAN_POINT('Ctrl Pts',(0.332388309604862,-0.913226856010398,
-1.16347685538568));
#38516=CARTESIAN_POINT('Ctrl Pts',(0.272558685364116,-0.93264051043169,
-1.16783965424534));
#38517=CARTESIAN_POINT('Ctrl Pts',(0.178496355530374,-0.953565561825706,
-1.17481380345513));
#38518=CARTESIAN_POINT('Ctrl Pts',(0.145167214285422,-0.959204683225914,
-1.17731585786918));
#38519=CARTESIAN_POINT('Ctrl Pts',(0.0692468388711174,-0.968078113397592,
-1.1830999057879));
#38520=CARTESIAN_POINT('Ctrl Pts',(0.0265243779043479,-0.970282399643622,
-1.18639965660027));
#38521=CARTESIAN_POINT('Ctrl Pts',(-0.0595890125701362,-0.969042878863386,
-1.19302385637117));
#38522=CARTESIAN_POINT('Ctrl Pts',(-0.102993939759864,-0.96549738632567,
-1.19634798154522));
#38523=CARTESIAN_POINT('Ctrl Pts',(-0.20107109129166,-0.950564436110202,
-1.20370419682778));
#38524=CARTESIAN_POINT('Ctrl Pts',(-0.255406864398631,-0.937259321727124,
-1.20766967676982));
#38525=CARTESIAN_POINT('Ctrl Pts',(-0.368152213245982,-0.899195722399789,
-1.21611327792907));
#38526=CARTESIAN_POINT('Ctrl Pts',(-0.426127408467094,-0.873136977883424,
-1.22059321122393));
#38527=CARTESIAN_POINT('Ctrl Pts',(-0.522461577342956,-0.818207220712546,
-1.22881100441419));
#38528=CARTESIAN_POINT('Ctrl Pts',(-0.562146172966108,-0.791604600021575,
-1.2324777898972));
#38529=CARTESIAN_POINT('Ctrl Pts',(-0.641434912696933,-0.729513125602168,
-1.24023231918795));
#38530=CARTESIAN_POINT('Ctrl Pts',(-0.680474960080581,-0.693387406624301,
-1.24429626135695));
#38531=CARTESIAN_POINT('Ctrl Pts',(-0.743404971363553,-0.624247255645805,
-1.25119387979881));
#38532=CARTESIAN_POINT('Ctrl Pts',(-0.768483395909982,-0.592929417872231,
-1.25408423581254));
#38533=CARTESIAN_POINT('Ctrl Pts',(-0.841810780459252,-0.488842643262975,
-1.26320858723048));
#38534=CARTESIAN_POINT('Ctrl Pts',(-0.882534380138505,-0.410710524809581,
-1.26937889325325));
#38535=CARTESIAN_POINT('Ctrl Pts',(-0.924615817339235,-0.294621768222479,
-1.27859240981985));
#38536=CARTESIAN_POINT('Ctrl Pts',(-0.935069062702998,-0.259889965944934,
-1.28136301627869));
#38537=CARTESIAN_POINT('Ctrl Pts',(-0.957698601773173,-0.165675486443003,
-1.2887871053272));
#38538=CARTESIAN_POINT('Ctrl Pts',(-0.966086884769573,-0.105988567500736,
-1.29333243383832));
#38539=CARTESIAN_POINT('Ctrl Pts',(-0.971698370569345,0.0191806258173882,
-1.30254126644064));
#38540=CARTESIAN_POINT('Ctrl Pts',(-0.968077282694246,0.0841725751854099,
-1.30719622877896));
#38541=CARTESIAN_POINT('Ctrl Pts',(-0.948242901745456,0.212255169708748,
-1.31655232412133));
#38542=CARTESIAN_POINT('Ctrl Pts',(-0.932004641003878,0.275387666342886,
-1.321259447385));
#38543=CARTESIAN_POINT('Ctrl Pts',(-0.892092351256462,0.384106329597992,
-1.32990535923517));
#38544=CARTESIAN_POINT('Ctrl Pts',(-0.870726395993944,0.430625752678655,
-1.33382068132123));
#38545=CARTESIAN_POINT('Ctrl Pts',(-0.806284444068375,0.544987834505778,
-1.34369202911898));
#38546=CARTESIAN_POINT('Ctrl Pts',(-0.758204956847398,0.609636286270502,
-1.34956506288098));
#38547=CARTESIAN_POINT('Ctrl Pts',(-0.636948315443397,0.737144060549658,
-1.3624084876591));
#38548=CARTESIAN_POINT('Ctrl Pts',(-0.560587252664674,0.797127369094058,
-1.36937786797394));
#38549=CARTESIAN_POINT('Ctrl Pts',(-0.370613295808071,0.904890897651286,
-1.38555811559755));
#38550=CARTESIAN_POINT('Ctrl Pts',(-0.272904921177973,0.933380625736226,
-1.39307688337039));
#38551=CARTESIAN_POINT('Ctrl Pts',(-0.201493905888848,0.948457169294521,
-1.39848693227111));
#38552=CARTESIAN_POINT('Ctrl Pts',(0.6384670947158,1.091429885542,0.1954399664911));
#38553=CARTESIAN_POINT('Ctrl Pts',(0.8484087081986,0.9686177710893,0.1816635794825));
#38554=CARTESIAN_POINT('Ctrl Pts',(1.194967633217,0.5987185795046,0.1541108054654));
#38555=CARTESIAN_POINT('Ctrl Pts',(1.328153666836,-0.150240885146,0.1127816444398));
#38556=CARTESIAN_POINT('Ctrl Pts',(1.031103739632,-0.8504871930036,0.07145248341419));
#38557=CARTESIAN_POINT('Ctrl Pts',(0.4001420220925,-1.275306320712,0.03012332238856));
#38558=CARTESIAN_POINT('Ctrl Pts',(-0.3604180561742,-1.287095826843,-0.01120583863706));
#38559=CARTESIAN_POINT('Ctrl Pts',(-1.004249922984,-0.8820425745732,-0.05253499966269));
#38560=CARTESIAN_POINT('Ctrl Pts',(-1.322842019319,-0.1913273198153,-0.09386416068832));
#38561=CARTESIAN_POINT('Ctrl Pts',(-1.213013257137,0.5613518632076,-0.1351933217139));
#38562=CARTESIAN_POINT('Ctrl Pts',(-0.710333370038,1.13222948353,-0.1765224827396));
#38563=CARTESIAN_POINT('Ctrl Pts',(0.02239783615318,1.33641888331,-0.2178516437652));
#38564=CARTESIAN_POINT('Ctrl Pts',(0.7478751900674,1.107790501614,-0.2591808047908));
#38565=CARTESIAN_POINT('Ctrl Pts',(1.231142796103,0.5203888075962,-0.3005099658165));
#38566=CARTESIAN_POINT('Ctrl Pts',(1.315687739353,-0.2355480161242,-0.3418391268421));
#38567=CARTESIAN_POINT('Ctrl Pts',(0.9741289680772,-0.9151993493049,-0.3831682878677));
#38568=CARTESIAN_POINT('Ctrl Pts',(0.3170850255305,-1.298450685237,-0.4244974488933));
#38569=CARTESIAN_POINT('Ctrl Pts',(-0.442651298475,-1.26118076554,-0.465826609919));
#38570=CARTESIAN_POINT('Ctrl Pts',(-1.059028862723,-0.815459970401,-0.5071557709446));
#38571=CARTESIAN_POINT('Ctrl Pts',(-1.332425247817,-0.1056411586267,-0.5484849319702));
#38572=CARTESIAN_POINT('Ctrl Pts',(-1.174297244163,0.6383910069347,-0.5898140929959));
#38573=CARTESIAN_POINT('Ctrl Pts',(-0.6358567980407,1.175671394503,-0.6311432540215));
#38574=CARTESIAN_POINT('Ctrl Pts',(0.1085146876066,1.332194301879,-0.6724724150471));
#38575=CARTESIAN_POINT('Ctrl Pts',(0.8177421864919,1.057267615679,-0.7138015760727));
#38576=CARTESIAN_POINT('Ctrl Pts',(1.262132544314,0.4399301541693,-0.7551307370984));
#38577=CARTESIAN_POINT('Ctrl Pts',(1.297763769147,-0.3198847852044,-0.796459898124));
#38578=CARTESIAN_POINT('Ctrl Pts',(0.9130962459419,-0.9761006080475,-0.8377890591496));
#38579=CARTESIAN_POINT('Ctrl Pts',(0.232709694298,-1.316192694613,-0.8791182201752));
#38580=CARTESIAN_POINT('Ctrl Pts',(-0.5230425568228,-1.23001761225,-0.9204473812009));
#38581=CARTESIAN_POINT('Ctrl Pts',(-1.109402319153,-0.7454839661251,-0.9617765422265));
#38582=CARTESIAN_POINT('Ctrl Pts',(-1.336458943337,-0.01951615025343,-1.003105703252));
#38583=CARTESIAN_POINT('Ctrl Pts',(-1.130713983139,0.7127765250298,-1.044434864278));
#38584=CARTESIAN_POINT('Ctrl Pts',(-0.5586627502186,1.214210654458,-1.085764025303));
#38585=CARTESIAN_POINT('Ctrl Pts',(-0.05694569140623,1.286380546669,-1.11331679932));
#38586=CARTESIAN_POINT('Ctrl Pts',(0.1836986798923,1.251045251418,-1.127093186329));
#38587=CARTESIAN_POINT('Ctrl Pts',(0.5864724611271,1.002547470996,0.1359882338627));
#38588=CARTESIAN_POINT('Ctrl Pts',(0.779317128881,0.889736766082,0.1222118468541));
#38589=CARTESIAN_POINT('Ctrl Pts',(1.097653449364,0.5499609326004,0.09465907283704));
#38590=CARTESIAN_POINT('Ctrl Pts',(1.219993256021,-0.1380057678818,0.05332991181142));
#38591=CARTESIAN_POINT('Ctrl Pts',(0.9471340854743,-0.7812263488064,0.01200075078579));
#38592=CARTESIAN_POINT('Ctrl Pts',(0.3675557886055,-1.171449621741,-0.02932841023984));
#38593=CARTESIAN_POINT('Ctrl Pts',(-0.3310668101591,-1.182279029761,-0.07065757126547));
#38594=CARTESIAN_POINT('Ctrl Pts',(-0.9224671542099,-0.8102119652057,-0.1119867322911));
#38595=CARTESIAN_POINT('Ctrl Pts',(-1.215114171385,-0.1757462601622,-0.1533158933167));
#38596=CARTESIAN_POINT('Ctrl Pts',(-1.114229497778,0.5156372372177,-0.1946450543423));
#38597=CARTESIAN_POINT('Ctrl Pts',(-0.6524861863591,1.040024485619,-0.235974215368));
#38598=CARTESIAN_POINT('Ctrl Pts',(0.02057383097953,1.227585380795,-0.2773033763936));
#38599=CARTESIAN_POINT('Ctrl Pts',(0.6869707256095,1.017575732989,-0.3186325374192));
#38600=CARTESIAN_POINT('Ctrl Pts',(1.130882627476,0.4780100764156,-0.3599616984449));
#38601=CARTESIAN_POINT('Ctrl Pts',(1.20854251215,-0.2163657702539,-0.4012908594705));
#38602=CARTESIAN_POINT('Ctrl Pts',(0.8947991495438,-0.8406685626417,-0.4426200204961));
#38603=CARTESIAN_POINT('Ctrl Pts',(0.2912626771974,-1.192709186308,-0.4839491815217));
#38604=CARTESIAN_POINT('Ctrl Pts',(-0.4066032511093,-1.158474404732,-0.5252783425474));
#38605=CARTESIAN_POINT('Ctrl Pts',(-0.9727850795543,-0.749051626544,-0.566607503573));
#38606=CARTESIAN_POINT('Ctrl Pts',(-1.223916973674,-0.0970380945375,-0.6079366645986));
#38607=CARTESIAN_POINT('Ctrl Pts',(-1.078666387945,0.5864025696815,-0.6492658256243));
#38608=CARTESIAN_POINT('Ctrl Pts',(-0.5840747383189,1.079928632059,-0.6905949866499));
#38609=CARTESIAN_POINT('Ctrl Pts',(0.09967761288844,1.223704835204,-0.7319241476755));
#38610=CARTESIAN_POINT('Ctrl Pts',(0.751147986558,0.9711672626034,-0.7732533087011));
#38611=CARTESIAN_POINT('Ctrl Pts',(1.159348673814,0.4041037077322,-0.8145824697268));
#38612=CARTESIAN_POINT('Ctrl Pts',(1.192078210377,-0.293834433769,-0.8559116307524));
#38613=CARTESIAN_POINT('Ctrl Pts',(0.8387367290116,-0.8966102257221,-0.897240791778));
#38614=CARTESIAN_POINT('Ctrl Pts',(0.2137585919034,-1.209006345536,-0.9385699528036));
#38615=CARTESIAN_POINT('Ctrl Pts',(-0.4804477131443,-1.129849074849,-0.9798991138293));
#38616=CARTESIAN_POINT('Ctrl Pts',(-1.019056289477,-0.6847742349804,-1.021228274855));
#38617=CARTESIAN_POINT('Ctrl Pts',(-1.227622178466,-0.01792681998115,-1.062557435881));
#38618=CARTESIAN_POINT('Ctrl Pts',(-1.038632402532,0.654730378946,-1.103886596906));
#38619=CARTESIAN_POINT('Ctrl Pts',(-0.5131671166336,1.115329383049,-1.145215757932));
#38620=CARTESIAN_POINT('Ctrl Pts',(-0.0523082239727,1.181621999622,-1.172768531949));
#38621=CARTESIAN_POINT('Ctrl Pts',(0.1687388712651,1.149164293121,-1.186544918957));
#38622=CARTESIAN_POINT('Ctrl Pts',(0.5344778275383,0.91366505645,0.07653650123427));
#38623=CARTESIAN_POINT('Ctrl Pts',(0.7102255495633,0.8108557610746,0.06276011422573));
#38624=CARTESIAN_POINT('Ctrl Pts',(1.00033926551,0.5012032856962,0.03520734020864));
#38625=CARTESIAN_POINT('Ctrl Pts',(1.111832845205,-0.1257706506175,-0.006121820816984));
#38626=CARTESIAN_POINT('Ctrl Pts',(0.863164431317,-0.7119655046093,-0.04745098184261));
#38627=CARTESIAN_POINT('Ctrl Pts',(0.3349695551186,-1.06759292277,-0.08878014286824));
#38628=CARTESIAN_POINT('Ctrl Pts',(-0.301715564144,-1.077462232679,-0.1301093038939));
#38629=CARTESIAN_POINT('Ctrl Pts',(-0.8406843854358,-0.7383813558381,-0.1714384649195));
#38630=CARTESIAN_POINT('Ctrl Pts',(-1.107386323452,-0.1601652005091,-0.2127676259451));
#38631=CARTESIAN_POINT('Ctrl Pts',(-1.015445738419,0.4699226112277,-0.2540967869707));
#38632=CARTESIAN_POINT('Ctrl Pts',(-0.5946390026802,0.947819487708,-0.2954259479964));
#38633=CARTESIAN_POINT('Ctrl Pts',(0.01874982580589,1.11875187828,-0.336755109022));
#38634=CARTESIAN_POINT('Ctrl Pts',(0.6260662611517,0.9273609643639,-0.3780842700476));
#38635=CARTESIAN_POINT('Ctrl Pts',(1.03062245885,0.435631345235,-0.4194134310733));
#38636=CARTESIAN_POINT('Ctrl Pts',(1.101397284947,-0.1971835243837,-0.4607425920989));
#38637=CARTESIAN_POINT('Ctrl Pts',(0.8154693310105,-0.7661377759785,-0.5020717531245));
#38638=CARTESIAN_POINT('Ctrl Pts',(0.2654403288644,-1.086967687379,-0.5434009141501));
#38639=CARTESIAN_POINT('Ctrl Pts',(-0.3705552037435,-1.055768043925,-0.5847300751758));
#38640=CARTESIAN_POINT('Ctrl Pts',(-0.8865412963853,-0.682643282687,-0.6260592362014));
#38641=CARTESIAN_POINT('Ctrl Pts',(-1.115408699531,-0.08843503044831,-0.667388397227));
#38642=CARTESIAN_POINT('Ctrl Pts',(-0.9830355317275,0.5344141324282,-0.7087175582527));
#38643=CARTESIAN_POINT('Ctrl Pts',(-0.532292678597,0.9841858696144,-0.7500467192783));
#38644=CARTESIAN_POINT('Ctrl Pts',(0.09084053817027,1.115215368529,-0.7913758803039));
#38645=CARTESIAN_POINT('Ctrl Pts',(0.6845537866242,0.8850669095274,-0.8327050413295));
#38646=CARTESIAN_POINT('Ctrl Pts',(1.056564803313,0.3682772612952,-0.8740342023552));
#38647=CARTESIAN_POINT('Ctrl Pts',(1.086392651607,-0.2677840823335,-0.9153633633808));
#38648=CARTESIAN_POINT('Ctrl Pts',(0.7643772120813,-0.8171198433967,-0.9566925244064));
#38649=CARTESIAN_POINT('Ctrl Pts',(0.1948074895087,-1.101819996459,-0.998021685432));
#38650=CARTESIAN_POINT('Ctrl Pts',(-0.4378528694657,-1.029680537447,-1.039350846458));
#38651=CARTESIAN_POINT('Ctrl Pts',(-0.9287102597998,-0.6240645038357,-1.080680007483));
#38652=CARTESIAN_POINT('Ctrl Pts',(-1.118785413596,-0.01633748970886,-1.122009168509));
#38653=CARTESIAN_POINT('Ctrl Pts',(-0.9465508219251,0.5966842328622,-1.163338329535));
#38654=CARTESIAN_POINT('Ctrl Pts',(-0.4676714830486,1.016448111641,-1.20466749056));
#38655=CARTESIAN_POINT('Ctrl Pts',(-0.04767075653918,1.076863452575,-1.232220264577));
#38656=CARTESIAN_POINT('Ctrl Pts',(0.1537790626378,1.047283334825,-1.245996651586));
#38657=CARTESIAN_POINT('Ctrl Pts',(0.4824831939496,0.824782641904,0.01708476860587));
#38658=CARTESIAN_POINT('Ctrl Pts',(0.6411339702457,0.7319747560673,0.003308381597328));
#38659=CARTESIAN_POINT('Ctrl Pts',(0.9030250816571,0.452445638792,-0.02424439241976));
#38660=CARTESIAN_POINT('Ctrl Pts',(1.00367243439,-0.1135355333533,-0.06557355344538));
#38661=CARTESIAN_POINT('Ctrl Pts',(0.7791947771597,-0.6427046604121,-0.106902714471));
#38662=CARTESIAN_POINT('Ctrl Pts',(0.3023833216316,-0.963736223799,-0.1482318754966));
#38663=CARTESIAN_POINT('Ctrl Pts',(-0.2723643181289,-0.9726454355976,-0.1895610365223));
#38664=CARTESIAN_POINT('Ctrl Pts',(-0.7589016166616,-0.6665507464705,-0.2308901975479));
#38665=CARTESIAN_POINT('Ctrl Pts',(-0.9996584755179,-0.144584140856,-0.2722193585735));
#38666=CARTESIAN_POINT('Ctrl Pts',(-0.9166619790597,0.4242079852378,-0.3135485195992));
#38667=CARTESIAN_POINT('Ctrl Pts',(-0.5367918190013,0.8556144897971,-0.3548776806248));
#38668=CARTESIAN_POINT('Ctrl Pts',(0.01692582063224,1.009918375764,-0.3962068416504));
#38669=CARTESIAN_POINT('Ctrl Pts',(0.5651617966938,0.8371461957389,-0.437536002676));
#38670=CARTESIAN_POINT('Ctrl Pts',(0.930362290223,0.3932526140544,-0.4788651637017));
#38671=CARTESIAN_POINT('Ctrl Pts',(0.9942520577446,-0.1780012785134,-0.5201943247273));
#38672=CARTESIAN_POINT('Ctrl Pts',(0.7361395124771,-0.6916069893153,-0.5615234857529));
#38673=CARTESIAN_POINT('Ctrl Pts',(0.2396179805314,-0.9812261884506,-0.6028526467785));
#38674=CARTESIAN_POINT('Ctrl Pts',(-0.3345071563778,-0.9530616831182,-0.6441818078042));
#38675=CARTESIAN_POINT('Ctrl Pts',(-0.8002975132164,-0.61623493883,-0.6855109688298));
#38676=CARTESIAN_POINT('Ctrl Pts',(-1.006900425388,-0.07983196635911,-0.7268401298554));
#38677=CARTESIAN_POINT('Ctrl Pts',(-0.8874046755098,0.482425695175,-0.7681692908811));
#38678=CARTESIAN_POINT('Ctrl Pts',(-0.4805106188751,0.88844310717,-0.8094984519067));
#38679=CARTESIAN_POINT('Ctrl Pts',(0.0820034634521,1.006725901854,-0.8508276129323));
#38680=CARTESIAN_POINT('Ctrl Pts',(0.6179595866904,0.7989665564513,-0.8921567739579));
#38681=CARTESIAN_POINT('Ctrl Pts',(0.953780932813,0.3324508148581,-0.9334859349836));
#38682=CARTESIAN_POINT('Ctrl Pts',(0.9807070928362,-0.2417337308981,-0.9748150960092));
#38683=CARTESIAN_POINT('Ctrl Pts',(0.6900176951509,-0.7376294610713,-1.016144257035));
#38684=CARTESIAN_POINT('Ctrl Pts',(0.1758563871141,-0.9946336473814,-1.05747341806));
#38685=CARTESIAN_POINT('Ctrl Pts',(-0.3952580257872,-0.929512000046,-1.098802579086));
#38686=CARTESIAN_POINT('Ctrl Pts',(-0.838364230123,-0.563354772691,-1.140131740112));
#38687=CARTESIAN_POINT('Ctrl Pts',(-1.009948648725,-0.01474815943658,-1.181460901137));
#38688=CARTESIAN_POINT('Ctrl Pts',(-0.8544692413182,0.5386380867785,-1.222790062163));
#38689=CARTESIAN_POINT('Ctrl Pts',(-0.4221758494636,0.917566840232,-1.264119223189));
#38690=CARTESIAN_POINT('Ctrl Pts',(-0.04303328910565,0.9721049055279,-1.291671997206));
#38691=CARTESIAN_POINT('Ctrl Pts',(0.1388192540106,0.9454023765286,-1.305448384214));
#38692=CARTESIAN_POINT('',(0.74999306484827,0.614597305574217,-4.00551630894776E-5));
#38693=CARTESIAN_POINT('Ctrl Pts',(0.749942259149723,0.614550663048058,
-8.01103261789551E-5));
#38694=CARTESIAN_POINT('Ctrl Pts',(0.791983524359411,0.563130688889933,
-0.00506365794800816));
#38695=CARTESIAN_POINT('Ctrl Pts',(0.828853698246298,0.507432374712272,
-0.0100335934428759));
#38696=CARTESIAN_POINT('Ctrl Pts',(0.883652016474552,0.40296070733887,-0.01863173248958));
#38697=CARTESIAN_POINT('Ctrl Pts',(0.903976280274475,0.355428000376728,
-0.0222930935158685));
#38698=CARTESIAN_POINT('Ctrl Pts',(0.945112425463336,0.232125211536002,
-0.0317283958672095));
#38699=CARTESIAN_POINT('Ctrl Pts',(0.960463073437942,0.15487698483769,-0.037641304524705));
#38700=CARTESIAN_POINT('Ctrl Pts',(0.972136041926485,0.00566423762840502,
-0.0489416354037443));
#38701=CARTESIAN_POINT('Ctrl Pts',(0.969920363139232,-0.0664489906790064,
-0.0543314837744917));
#38702=CARTESIAN_POINT('Ctrl Pts',(0.952845641494024,-0.187463666740853,
-0.0631691753546404));
#38703=CARTESIAN_POINT('Ctrl Pts',(0.941911392506289,-0.236942726623874,
-0.0667515552081078));
#38704=CARTESIAN_POINT('Ctrl Pts',(0.910032892029366,-0.340886784729333,
-0.0746354041702569));
#38705=CARTESIAN_POINT('Ctrl Pts',(0.887879663818006,-0.39458678324541,
-0.078978483112223));
#38706=CARTESIAN_POINT('Ctrl Pts',(0.837190085734205,-0.491974936808162,
-0.0872933748465481));
#38707=CARTESIAN_POINT('Ctrl Pts',(0.809447932280059,-0.536225496558952,
-0.0912601761201217));
#38708=CARTESIAN_POINT('Ctrl Pts',(0.745727613947211,-0.622018883008426,
-0.0992342754801228));
#38709=CARTESIAN_POINT('Ctrl Pts',(0.709374774495646,-0.663315871701172,
-0.103193347360063));
#38710=CARTESIAN_POINT('Ctrl Pts',(0.639665749887592,-0.730196799627268,
-0.110110728583079));
#38711=CARTESIAN_POINT('Ctrl Pts',(0.607654488054685,-0.757179480716653,
-0.113094028586163));
#38712=CARTESIAN_POINT('Ctrl Pts',(0.515932509582186,-0.824619428772014,
-0.12140492900092));
#38713=CARTESIAN_POINT('Ctrl Pts',(0.453268841285773,-0.860336599303275,
-0.126895272802062));
#38714=CARTESIAN_POINT('Ctrl Pts',(0.350267581391511,-0.90503139921325,
-0.135421322538143));
#38715=CARTESIAN_POINT('Ctrl Pts',(0.311820637222686,-0.918937827419921,
-0.138498935117359));
#38716=CARTESIAN_POINT('Ctrl Pts',(0.201231201838853,-0.951361775068941,
-0.146975200161323));
#38717=CARTESIAN_POINT('Ctrl Pts',(0.127398061288026,-0.964243706377321,
-0.152233261936751));
#38718=CARTESIAN_POINT('Ctrl Pts',(-0.0336134095385275,-0.973378111806249,
-0.163901967566458));
#38719=CARTESIAN_POINT('Ctrl Pts',(-0.123625851787474,-0.96679156459634,
-0.170751849284573));
#38720=CARTESIAN_POINT('Ctrl Pts',(-0.316887057539714,-0.92183570319369,
-0.185752030374903));
#38721=CARTESIAN_POINT('Ctrl Pts',(-0.412369132536766,-0.883411422569636,
-0.1929868936821));
#38722=CARTESIAN_POINT('Ctrl Pts',(-0.546681183057338,-0.803098998306091,
-0.204307268407498));
#38723=CARTESIAN_POINT('Ctrl Pts',(-0.591282134992225,-0.770982938595183,
-0.208336742454701));
#38724=CARTESIAN_POINT('Ctrl Pts',(-0.660253360078768,-0.711392617957626,
-0.215229605273813));
#38725=CARTESIAN_POINT('Ctrl Pts',(-0.686096589098383,-0.68637400301508,
-0.217973597276779));
#38726=CARTESIAN_POINT('Ctrl Pts',(-0.773158243241712,-0.592240477703788,
-0.227664066266423));
#38727=CARTESIAN_POINT('Ctrl Pts',(-0.826261125605108,-0.51551052279722,
-0.234333483418219));
#38728=CARTESIAN_POINT('Ctrl Pts',(-0.891002385709881,-0.386433201759339,
-0.244785638657728));
#38729=CARTESIAN_POINT('Ctrl Pts',(-0.910634463542769,-0.338015506376734,
-0.248568477582743));
#38730=CARTESIAN_POINT('Ctrl Pts',(-0.941663311231948,-0.23862283217278,
-0.256301109307229));
#38731=CARTESIAN_POINT('Ctrl Pts',(-0.952940373909301,-0.187919019203186,
-0.260257442745707));
#38732=CARTESIAN_POINT('Ctrl Pts',(-0.976579884718872,-0.0191923880794445,
-0.273064045851657));
#38733=CARTESIAN_POINT('Ctrl Pts',(-0.971486452655273,0.101515762448749,
-0.281615508345684));
#38734=CARTESIAN_POINT('Ctrl Pts',(-0.916250609043354,0.344322935157297,
-0.29983581525101));
#38735=CARTESIAN_POINT('Ctrl Pts',(-0.863336468372821,0.459566612118886,
-0.309279469701199));
#38736=CARTESIAN_POINT('Ctrl Pts',(-0.718479399789711,0.662138109821643,
-0.327620527323536));
#38737=CARTESIAN_POINT('Ctrl Pts',(-0.62926076313351,0.748204380563924,
-0.336486135655537));
#38738=CARTESIAN_POINT('Ctrl Pts',(-0.419514882340921,0.883880734586201,
-0.355016179589254));
#38739=CARTESIAN_POINT('Ctrl Pts',(-0.297907992893379,0.931346865568005,
-0.364531941465149));
#38740=CARTESIAN_POINT('Ctrl Pts',(-0.0747702911518417,0.97190093761318,
-0.381256259175794));
#38741=CARTESIAN_POINT('Ctrl Pts',(0.0548610048127376,0.980868053947884,
-0.390482407034185));
#38742=CARTESIAN_POINT('Ctrl Pts',(0.305117797151989,0.925811521815035,
-0.409544191108791));
#38743=CARTESIAN_POINT('Ctrl Pts',(0.400680065497012,0.888629667696109,
-0.417137232122319));
#38744=CARTESIAN_POINT('Ctrl Pts',(0.539981830635489,0.807861115764787,
-0.428956507776047));
#38745=CARTESIAN_POINT('Ctrl Pts',(0.589067024577443,0.773041452413226,
-0.433253104806547));
#38746=CARTESIAN_POINT('Ctrl Pts',(0.682940467548811,0.69172444342647,-0.442355819649039));
#38747=CARTESIAN_POINT('Ctrl Pts',(0.727022565187571,0.6449176869188,-0.447147826651843));
#38748=CARTESIAN_POINT('Ctrl Pts',(0.823468275286885,0.520157342563299,
-0.458978900547134));
#38749=CARTESIAN_POINT('Ctrl Pts',(0.870238754511863,0.437739837279528,
-0.466015568909245));
#38750=CARTESIAN_POINT('Ctrl Pts',(0.921483109890555,0.306373388564749,
-0.476189946572354));
#38751=CARTESIAN_POINT('Ctrl Pts',(0.935462861091772,0.261002090651833,
-0.479570604180273));
#38752=CARTESIAN_POINT('Ctrl Pts',(0.9599443780831,0.152734089995508,-0.487718202795412));
#38753=CARTESIAN_POINT('Ctrl Pts',(0.967683840302401,0.0894680808929378,
-0.492505558444665));
#38754=CARTESIAN_POINT('Ctrl Pts',(0.971177436970066,-0.0491146553268897,
-0.502969086788959));
#38755=CARTESIAN_POINT('Ctrl Pts',(0.964444230504448,-0.124564260901227,
-0.508635168130123));
#38756=CARTESIAN_POINT('Ctrl Pts',(0.939038261849135,-0.247481041764794,
-0.517709582193673));
#38757=CARTESIAN_POINT('Ctrl Pts',(0.925059000873544,-0.295947373429156,
-0.521275659929971));
#38758=CARTESIAN_POINT('Ctrl Pts',(0.886885808674521,-0.397192666158041,
-0.529121629020463));
#38759=CARTESIAN_POINT('Ctrl Pts',(0.861547358587474,-0.449146237612015,
-0.53344245588854));
#38760=CARTESIAN_POINT('Ctrl Pts',(0.804855469806404,-0.54330017437357,
-0.541764954413461));
#38761=CARTESIAN_POINT('Ctrl Pts',(0.774161129252339,-0.586052779452843,
-0.545762573621421));
#38762=CARTESIAN_POINT('Ctrl Pts',(0.704972516616502,-0.66784568297347,
-0.553757270164554));
#38763=CARTESIAN_POINT('Ctrl Pts',(0.666184984261621,-0.706672470628262,
-0.557708044978171));
#38764=CARTESIAN_POINT('Ctrl Pts',(0.592531416782339,-0.768938598262087,
-0.564614415613664));
#38765=CARTESIAN_POINT('Ctrl Pts',(0.55890727215155,-0.793843373949183,
-0.567595783171078));
#38766=CARTESIAN_POINT('Ctrl Pts',(0.482442285068433,-0.842982043982225,
-0.574230428205313));
#38767=CARTESIAN_POINT('Ctrl Pts',(0.439226062869622,-0.866150678023914,
-0.577914785710056));
#38768=CARTESIAN_POINT('Ctrl Pts',(0.351273383110356,-0.905088258260573,
-0.585220395996211));
#38769=CARTESIAN_POINT('Ctrl Pts',(0.306537912905923,-0.921090214720483,
-0.588842029064422));
#38770=CARTESIAN_POINT('Ctrl Pts',(0.212318111789294,-0.947333946871234,
-0.596161639099133));
#38771=CARTESIAN_POINT('Ctrl Pts',(0.162693879292811,-0.957145637324262,
-0.599822161736598));
#38772=CARTESIAN_POINT('Ctrl Pts',(0.0630807526456533,-0.968979995725448,
-0.607028244911473));
#38773=CARTESIAN_POINT('Ctrl Pts',(0.0130963722548543,-0.971086087328877,
-0.610583547815589));
#38774=CARTESIAN_POINT('Ctrl Pts',(-0.0948203098140028,-0.967146775844488,
-0.618454240488956));
#38775=CARTESIAN_POINT('Ctrl Pts',(-0.152163307377428,-0.959666261898805,
-0.622811432133744));
#38776=CARTESIAN_POINT('Ctrl Pts',(-0.246590878698771,-0.938661050813737,
-0.630175650382095));
#38777=CARTESIAN_POINT('Ctrl Pts',(-0.284225753088723,-0.927866370246119,
-0.633153675375206));
#38778=CARTESIAN_POINT('Ctrl Pts',(-0.383838222143453,-0.892771238153227,
-0.641033652516603));
#38779=CARTESIAN_POINT('Ctrl Pts',(-0.444388465973063,-0.864294935496258,
-0.645816195732069));
#38780=CARTESIAN_POINT('Ctrl Pts',(-0.555347902358027,-0.797578903642003,
-0.655132530400022));
#38781=CARTESIAN_POINT('Ctrl Pts',(-0.606265079112514,-0.759872162087916,
-0.65968352933207));
#38782=CARTESIAN_POINT('Ctrl Pts',(-0.685742102906565,-0.687430621601045,
-0.667745538161171));
#38783=CARTESIAN_POINT('Ctrl Pts',(-0.716337706344111,-0.655319110682923,
-0.67113286930802));
#38784=CARTESIAN_POINT('Ctrl Pts',(-0.808431881110594,-0.544440049093277,
-0.682047581387006));
#38785=CARTESIAN_POINT('Ctrl Pts',(-0.860482686265615,-0.457700340596788,
-0.689255051361111));
#38786=CARTESIAN_POINT('Ctrl Pts',(-0.956498986002975,-0.222988363490985,
-0.707619665221014));
#38787=CARTESIAN_POINT('Ctrl Pts',(-0.970872220697877,-0.0926079183447355,
-0.717487448773803));
#38788=CARTESIAN_POINT('Ctrl Pts',(-0.968471358047173,0.0968236024967683,
-0.731486319252523));
#38789=CARTESIAN_POINT('Ctrl Pts',(-0.956077990535885,0.18282017286137,
-0.737708137479027));
#38790=CARTESIAN_POINT('Ctrl Pts',(-0.897463278185653,0.390384619048993,
-0.753470239990772));
#38791=CARTESIAN_POINT('Ctrl Pts',(-0.839165556372643,0.502339013087694,
-0.762874973552972));
#38792=CARTESIAN_POINT('Ctrl Pts',(-0.681628130937872,0.700824545961502,
-0.781551104288793));
#38793=CARTESIAN_POINT('Ctrl Pts',(-0.58382868541532,0.784948724465537,
-0.790752835947921));
#38794=CARTESIAN_POINT('Ctrl Pts',(-0.367879607316997,0.905580061152143,
-0.809112470384984));
#38795=CARTESIAN_POINT('Ctrl Pts',(-0.251227423629182,0.944074570175999,
-0.818081691658179));
#38796=CARTESIAN_POINT('Ctrl Pts',(-0.0414591985823136,0.973069690006431,
-0.833704184817049));
#38797=CARTESIAN_POINT('Ctrl Pts',(0.0914991124827709,0.979358329861489,
-0.843139905578241));
#38798=CARTESIAN_POINT('Ctrl Pts',(0.366894717045133,0.905774711964452,
-0.86432281438767));
#38799=CARTESIAN_POINT('Ctrl Pts',(0.479709653824472,0.851493263089896,
-0.873558629646538));
#38800=CARTESIAN_POINT('Ctrl Pts',(0.613243488570379,0.752718937475823,
-0.885668616486831));
#38801=CARTESIAN_POINT('Ctrl Pts',(0.646332450220662,0.724629142748078,
-0.888781829972234));
#38802=CARTESIAN_POINT('Ctrl Pts',(0.723720361021099,0.64901667464327,-0.896708056507243));
#38803=CARTESIAN_POINT('Ctrl Pts',(0.76532774394799,0.599040606791593,-0.901552489526432));
#38804=CARTESIAN_POINT('Ctrl Pts',(0.837280957327974,0.492922625274083,
-0.911169298602814));
#38805=CARTESIAN_POINT('Ctrl Pts',(0.867844069777876,0.436877849438058,
-0.915942103711501));
#38806=CARTESIAN_POINT('Ctrl Pts',(0.919704693491599,0.315108995311966,
-0.925696753666225));
#38807=CARTESIAN_POINT('Ctrl Pts',(0.940019434097609,0.248948964472203,
-0.930583205817245));
#38808=CARTESIAN_POINT('Ctrl Pts',(0.962038031158095,0.133358754910732,
-0.939148061290653));
#38809=CARTESIAN_POINT('Ctrl Pts',(0.967403938251554,0.0847432434698806,
-0.942785265685722));
#38810=CARTESIAN_POINT('Ctrl Pts',(0.972891026474809,-0.0722954589448364,
-0.954601302008364));
#38811=CARTESIAN_POINT('Ctrl Pts',(0.958551136764753,-0.181393992542052,
-0.962853996903281));
#38812=CARTESIAN_POINT('Ctrl Pts',(0.913251694825849,-0.329836589486158,
-0.974011839960728));
#38813=CARTESIAN_POINT('Ctrl Pts',(0.89638517457652,-0.373562923404985,
-0.977335956267267));
#38814=CARTESIAN_POINT('Ctrl Pts',(0.84934792524559,-0.472776728484108,
-0.9853447168436));
#38815=CARTESIAN_POINT('Ctrl Pts',(0.816640996218955,-0.52686934189899,
-0.990108581234102));
#38816=CARTESIAN_POINT('Ctrl Pts',(0.739823597464444,-0.630112006451014,
-0.999865949489146));
#38817=CARTESIAN_POINT('Ctrl Pts',(0.695147302894014,-0.679014457321637,
-1.00486018760927));
#38818=CARTESIAN_POINT('Ctrl Pts',(0.612977208335645,-0.752633887809531,
-1.01289439295814));
#38819=CARTESIAN_POINT('Ctrl Pts',(0.577871549805956,-0.780050049767168,
-1.01606063470027));
#38820=CARTESIAN_POINT('Ctrl Pts',(0.49706649081279,-0.83462082236835,-1.02304974459024));
#38821=CARTESIAN_POINT('Ctrl Pts',(0.450801544925927,-0.8605767780256,-1.02688818266538));
#38822=CARTESIAN_POINT('Ctrl Pts',(0.355596389864133,-0.903785060190799,
-1.03473028500779));
#38823=CARTESIAN_POINT('Ctrl Pts',(0.307265162344229,-0.921182218996251,
-1.03865156049473));
#38824=CARTESIAN_POINT('Ctrl Pts',(0.207636054043817,-0.948485892976383,
-1.04648091965244));
#38825=CARTESIAN_POINT('Ctrl Pts',(0.15627754791737,-0.958263403146292,
-1.05036439257441));
#38826=CARTESIAN_POINT('Ctrl Pts',(0.0452409221182438,-0.970418428176485,
-1.05846212592755));
#38827=CARTESIAN_POINT('Ctrl Pts',(-0.014592215616271,-0.971535239894634,
-1.06268803907717));
#38828=CARTESIAN_POINT('Ctrl Pts',(-0.121223996625228,-0.963571095923621,
-1.07043210119647));
#38829=CARTESIAN_POINT('Ctrl Pts',(-0.167744946763637,-0.956571121920403,
-1.07391006816536));
#38830=CARTESIAN_POINT('Ctrl Pts',(-0.249386558305709,-0.937956544665916,
-1.0802478199119));
#38831=CARTESIAN_POINT('Ctrl Pts',(-0.284409709922977,-0.927838590886795,
-1.08303157260172));
#38832=CARTESIAN_POINT('Ctrl Pts',(-0.370096933566187,-0.897817774242533,
-1.08991847173514));
#38833=CARTESIAN_POINT('Ctrl Pts',(-0.419951230586404,-0.875543746334502,
-1.09395546676393));
#38834=CARTESIAN_POINT('Ctrl Pts',(-0.53718092214749,-0.811100788087201,
-1.10366225027211));
#38835=CARTESIAN_POINT('Ctrl Pts',(-0.602145102563672,-0.764469256881141,
-1.10928973709699));
#38836=CARTESIAN_POINT('Ctrl Pts',(-0.694162572215653,-0.679135878923541,
-1.11853453562391));
#38837=CARTESIAN_POINT('Ctrl Pts',(-0.725451186358578,-0.645480474978077,
-1.12200914481219));
#38838=CARTESIAN_POINT('Ctrl Pts',(-0.797876204012436,-0.555501978720714,
-1.13079010844328));
#38839=CARTESIAN_POINT('Ctrl Pts',(-0.835686460518628,-0.496481257598879,
-1.13600950543592));
#38840=CARTESIAN_POINT('Ctrl Pts',(-0.903359586564656,-0.361389621174484,
-1.14701804001649));
#38841=CARTESIAN_POINT('Ctrl Pts',(-0.947933188046413,-0.250988328500812,
-1.15526661898464));
#38842=CARTESIAN_POINT('Ctrl Pts',(-0.96863761515076,-0.0660972046724641,
-1.16930417636519));
#38843=CARTESIAN_POINT('Ctrl Pts',(-0.970507420996907,-0.0228215652799758,
-1.17259199202591));
#38844=CARTESIAN_POINT('Ctrl Pts',(-0.967880972425023,0.0906473176846458,
-1.18106168070997));
#38845=CARTESIAN_POINT('Ctrl Pts',(-0.958669179681034,0.160761742191593,
-1.18618840283058));
#38846=CARTESIAN_POINT('Ctrl Pts',(-0.927176450774154,0.291022169363798,
-1.19594157664097));
#38847=CARTESIAN_POINT('Ctrl Pts',(-0.906184283733861,0.351524969776246,
-1.20057529257284));
#38848=CARTESIAN_POINT('Ctrl Pts',(-0.846738408387065,0.479668453351846,
-1.21103506207018));
#38849=CARTESIAN_POINT('Ctrl Pts',(-0.805691619443741,0.545257313881333,
-1.21686511129903));
#38850=CARTESIAN_POINT('Ctrl Pts',(-0.688381393394236,0.691533926080835,
-1.23075331546858));
#38851=CARTESIAN_POINT('Ctrl Pts',(-0.604306969817395,0.766315083863186,
-1.23882509336762));
#38852=CARTESIAN_POINT('Ctrl Pts',(-0.414950826661446,0.884032183373647,
-1.25522713697232));
#38853=CARTESIAN_POINT('Ctrl Pts',(-0.312130052609453,0.925099829793529,
-1.26336940557668));
#38854=CARTESIAN_POINT('Ctrl Pts',(-0.201489314110026,0.948458138715504,
-1.27174112566436));
#38855=CARTESIAN_POINT('Ctrl Pts',(0.000261914023966756,-1.24958349387703,
-2.05998412772246E-17));
#38856=CARTESIAN_POINT('Ctrl Pts',(0.156016439362075,-1.23406571896253,
-1.91588362189685E-17));
#38857=CARTESIAN_POINT('Ctrl Pts',(0.309361253433594,-1.19037621015537,
6.20163642661709E-16));
#38858=CARTESIAN_POINT('Ctrl Pts',(0.58815550652336,-1.04085178026832,6.20163642661709E-16));
#38859=CARTESIAN_POINT('Ctrl Pts',(0.708122763155166,-0.943561790489167,
2.60208521396521E-17));
#38860=CARTESIAN_POINT('Ctrl Pts',(0.928835256908631,-0.678043480207547,
2.60208521396521E-17));
#38861=CARTESIAN_POINT('Ctrl Pts',(0.985613606267667,-0.53354825918773,
1.31001685194088E-10));
#38862=CARTESIAN_POINT('Ctrl Pts',(1.05519459948604,-0.306237812616919,
1.31001685194088E-10));
#38863=CARTESIAN_POINT('Ctrl Pts',(1.07176070683132,-0.165494960865087,
-1.73472347597681E-17));
#38864=CARTESIAN_POINT('Ctrl Pts',(1.04494763475789,0.102321842499411,-1.73472347597681E-17));
#38865=CARTESIAN_POINT('Ctrl Pts',(1.01124950363173,0.222287506844967,2.51534904016637E-15));
#38866=CARTESIAN_POINT('Ctrl Pts',(0.892911145490497,0.464634040295056,
2.51534904016637E-15));
#38867=CARTESIAN_POINT('Ctrl Pts',(0.813327676481858,0.554951540676525,
0.));
#38868=CARTESIAN_POINT('Ctrl Pts',(0.750043870546816,0.614643948100375,
0.));
#38869=CARTESIAN_POINT('Origin',(0.,0.,0.));
#38870=CARTESIAN_POINT('Ctrl Pts',(0.749944789178387,0.614547568599164,
-3.81639164714898E-17));
#38871=CARTESIAN_POINT('Ctrl Pts',(0.730682841831246,0.638106731811761,
-3.84621583023737E-17));
#38872=CARTESIAN_POINT('Ctrl Pts',(0.71051437582472,0.660555707618496,1.10349477427045E-17));
#38873=CARTESIAN_POINT('Ctrl Pts',(0.689467072170113,0.681929481619668,
0.));
#38874=CARTESIAN_POINT('Ctrl Pts',(0.672065821349576,0.699600647887774,
-9.12334884379743E-18));
#38875=CARTESIAN_POINT('Ctrl Pts',(0.654061014915041,0.716538155044498,
-4.71483132268289E-17));
#38876=CARTESIAN_POINT('Ctrl Pts',(0.635452996963201,0.732740730419006,
-1.04083408558608E-17));
#38877=CARTESIAN_POINT('Ctrl Pts',(0.614550903662948,0.750940827982265,
3.08610910811809E-17));
#38878=CARTESIAN_POINT('Ctrl Pts',(0.592891705743417,0.768209749170047,
-4.16188708512546E-17));
#38879=CARTESIAN_POINT('Ctrl Pts',(0.570482844003363,0.784505783724916,
-3.46944695195361E-17));
#38880=CARTESIAN_POINT('Ctrl Pts',(0.55812694614723,0.793491163739113,-3.68990344897851E-17));
#38881=CARTESIAN_POINT('Ctrl Pts',(0.545544606031477,0.802179299411958,
7.41430263895259E-17));
#38882=CARTESIAN_POINT('Ctrl Pts',(0.532735933416764,0.810573129558699,
5.55111512312578E-17));
#38883=CARTESIAN_POINT('Ctrl Pts',(0.513532008218362,0.823157921996984,
2.75765519477732E-17));
#38884=CARTESIAN_POINT('Ctrl Pts',(0.49380962086728,0.835091709771066,-1.22052527852199E-17));
#38885=CARTESIAN_POINT('Ctrl Pts',(0.473457409740538,0.846417134999195,
-6.93889390390723E-18));
#38886=CARTESIAN_POINT('Ctrl Pts',(0.455793315912445,0.856246699591803,
-2.36811499282974E-18));
#38887=CARTESIAN_POINT('Ctrl Pts',(0.437653628660792,0.865617731461489,
7.3032627247367E-17));
#38888=CARTESIAN_POINT('Ctrl Pts',(0.418956034393796,0.874528239752056,
4.16333634234434E-17));
#38889=CARTESIAN_POINT('Ctrl Pts',(0.395466891195609,0.885722204184967,
2.18755056934525E-18));
#38890=CARTESIAN_POINT('Ctrl Pts',(0.371103317522214,0.89618643526344,-1.13375735736027E-17));
#38891=CARTESIAN_POINT('Ctrl Pts',(0.345777858685626,0.905826232280199,
1.38777878078145E-17));
#38892=CARTESIAN_POINT('Ctrl Pts',(0.323399828563073,0.914344129997601,
3.61585338422832E-17));
#38893=CARTESIAN_POINT('Ctrl Pts',(0.300270073851916,0.922218006361476,
5.83990733107664E-17));
#38894=CARTESIAN_POINT('Ctrl Pts',(0.276333460210171,0.929346534537895,
4.16333634234434E-17));
#38895=CARTESIAN_POINT('Ctrl Pts',(0.254600684654987,0.935818740891543,
2.6411268290944E-17));
#38896=CARTESIAN_POINT('Ctrl Pts',(0.232200474936726,0.941678715556752,
7.26819386870289E-18));
#38897=CARTESIAN_POINT('Ctrl Pts',(0.209029079790626,0.946833180007271,
1.38777878078145E-17));
#38898=CARTESIAN_POINT('Ctrl Pts',(0.192470401980619,0.950516649025046,
1.86011174046147E-17));
#38899=CARTESIAN_POINT('Ctrl Pts',(0.175517891095409,0.953838936393204,
-1.55953622066509E-17));
#38900=CARTESIAN_POINT('Ctrl Pts',(0.15813628128911,0.95675004350001,-1.38777878078145E-17));
#38901=CARTESIAN_POINT('Ctrl Pts',(0.144196498316047,0.959084706499147,
-1.25003196315819E-17));
#38902=CARTESIAN_POINT('Ctrl Pts',(0.129979600100864,0.961154811600588,
2.22457029106987E-17));
#38903=CARTESIAN_POINT('Ctrl Pts',(0.115472874029535,0.962927165407642,
2.77555756156289E-17));
#38904=CARTESIAN_POINT('Ctrl Pts',(0.090329044023351,0.965999103391187,
3.73055803491087E-17));
#38905=CARTESIAN_POINT('Ctrl Pts',(0.0643321939263775,0.968169205716358,
1.79555613037849E-17));
#38906=CARTESIAN_POINT('Ctrl Pts',(0.0377310960825474,0.969238009639096,
-1.38777878078145E-17));
#38907=CARTESIAN_POINT('Ctrl Pts',(0.0234354151615083,0.969812394949669,
-3.09853299182623E-17));
#38908=CARTESIAN_POINT('Ctrl Pts',(0.0089657315485847,0.970069420136057,
-3.34851907640562E-17));
#38909=CARTESIAN_POINT('Ctrl Pts',(-0.00563632681277814,0.969983624511508,
-5.55111512312578E-17));
#38910=CARTESIAN_POINT('Ctrl Pts',(-0.0297733890182163,0.969841805168272,
-7.80420644965808E-17));
#38911=CARTESIAN_POINT('Ctrl Pts',(-0.0542700208752427,0.968761074770255,
5.50656997416883E-17));
#38912=CARTESIAN_POINT('Ctrl Pts',(-0.0789382482361072,0.966698551285329,
4.16333634234434E-17));
#38913=CARTESIAN_POINT('Ctrl Pts',(-0.105720565843984,0.964459267601142,
2.70498632704578E-17));
#38914=CARTESIAN_POINT('Ctrl Pts',(-0.132708401591014,0.961061724830605,
1.50291167672607E-17));
#38915=CARTESIAN_POINT('Ctrl Pts',(-0.159653017437302,0.956501006938883,
1.38777878078145E-17));
#38916=CARTESIAN_POINT('Ctrl Pts',(-0.181599435693551,0.952786297366793,
1.294002914617E-17));
#38917=CARTESIAN_POINT('Ctrl Pts',(-0.203516867164854,0.948300956670757,
-5.31396574931834E-18));
#38918=CARTESIAN_POINT('Ctrl Pts',(-0.225271705910235,0.943067776032336,
0.));
#38919=CARTESIAN_POINT('Ctrl Pts',(-0.239913324915326,0.939545698117194,
3.57644856936239E-18));
#38920=CARTESIAN_POINT('Ctrl Pts',(-0.254479084059815,0.935686010161577,
6.34983178660048E-17));
#38921=CARTESIAN_POINT('Ctrl Pts',(-0.26893705135892,0.931498981315315,
6.93889390390723E-17));
#38922=CARTESIAN_POINT('Ctrl Pts',(-0.302363902922641,0.921818561596446,
8.30080678900847E-17));
#38923=CARTESIAN_POINT('Ctrl Pts',(-0.335243053394182,0.910386042359239,
-2.12046701469247E-17));
#38924=CARTESIAN_POINT('Ctrl Pts',(-0.367493440333633,0.897221403951318,
-4.16333634234434E-17));
#38925=CARTESIAN_POINT('Ctrl Pts',(-0.386971348403746,0.889270503480971,
-5.397145444789E-17));
#38926=CARTESIAN_POINT('Ctrl Pts',(-0.406219625336411,0.880686830958701,
9.6942143763509E-18));
#38927=CARTESIAN_POINT('Ctrl Pts',(-0.42521626419776,0.871466546064191,
0.));
#38928=CARTESIAN_POINT('Ctrl Pts',(-0.438835063269308,0.864856471077914,
-6.94983774296248E-18));
#38929=CARTESIAN_POINT('Ctrl Pts',(-0.452327762572579,0.857917215840695,
4.71089931603229E-17));
#38930=CARTESIAN_POINT('Ctrl Pts',(-0.465671631291066,0.850652922959293,
4.16333634234434E-17));
#38931=CARTESIAN_POINT('Ctrl Pts',(-0.491771919138885,0.836444139943257,
3.09231627091158E-17));
#38932=CARTESIAN_POINT('Ctrl Pts',(-0.517289162072855,0.820994711100186,
4.19174349399959E-17));
#38933=CARTESIAN_POINT('Ctrl Pts',(-0.541979559119698,0.804412747338752,
5.55111512312578E-17));
#38934=CARTESIAN_POINT('Ctrl Pts',(-0.554737268949053,0.795844724650907,
6.25351244633398E-17));
#38935=CARTESIAN_POINT('Ctrl Pts',(-0.567274624913577,0.786975062654238,
3.61841045289072E-18));
#38936=CARTESIAN_POINT('Ctrl Pts',(-0.579561138071597,0.777823172216688,
0.));
#38937=CARTESIAN_POINT('Ctrl Pts',(-0.591997021826605,0.768560019672416,
-5.96044223634771E-17));
#38938=CARTESIAN_POINT('Ctrl Pts',(-0.604175244810911,0.759008321414952,
2.9479058197616E-17));
#38939=CARTESIAN_POINT('Ctrl Pts',(-0.616075811532905,0.749198177128338,
2.77555756156289E-17));
#38940=CARTESIAN_POINT('Ctrl Pts',(-0.636745216472705,0.732159505818413,
2.47621585602927E-17));
#38941=CARTESIAN_POINT('Ctrl Pts',(-0.656592760626642,0.714334970677369,
5.70078597589259E-17));
#38942=CARTESIAN_POINT('Ctrl Pts',(-0.675690425296587,0.69570759103261,
5.55111512312578E-17));
#38943=CARTESIAN_POINT('Ctrl Pts',(-0.694906682459675,0.676964539266104,
5.40051484574673E-17));
#38944=CARTESIAN_POINT('Ctrl Pts',(-0.713364184544054,0.657408093760942,
-5.91853539566696E-18));
#38945=CARTESIAN_POINT('Ctrl Pts',(-0.731099444893425,0.636983809797649,
-2.77555756156289E-17));
#38946=CARTESIAN_POINT('Ctrl Pts',(-0.737317170045828,0.629823351951712,
-3.54113253229913E-17));
#38947=CARTESIAN_POINT('Ctrl Pts',(-0.743445761422563,0.622555934095105,
3.31673986846265E-17));
#38948=CARTESIAN_POINT('Ctrl Pts',(-0.749485555517556,0.615178325990764,
2.77555756156289E-17));
#38949=CARTESIAN_POINT('Ctrl Pts',(-0.9278486567136,0.2828371797248,0.1713479786129));
#38950=CARTESIAN_POINT('Ctrl Pts',(-0.8680237607561,0.4790930234802,0.1561991832375));
#38951=CARTESIAN_POINT('Ctrl Pts',(-0.6198030816887,0.8317102040798,0.1259015924865));
#38952=CARTESIAN_POINT('Ctrl Pts',(-0.006020401385728,1.0373137838,0.08045520636017));
#38953=CARTESIAN_POINT('Ctrl Pts',(0.6100667263548,0.8389364077892,0.03500882023379));
#38954=CARTESIAN_POINT('Ctrl Pts',(0.9886505599867,0.3139752873927,-0.01043756589259));
#38955=CARTESIAN_POINT('Ctrl Pts',(0.9823257752865,-0.3332333632255,-0.05588395201896));
#38956=CARTESIAN_POINT('Ctrl Pts',(0.5935583558294,-0.8507036453223,-0.1013303381453));
#38957=CARTESIAN_POINT('Ctrl Pts',(-0.02629601796974,-1.036974907694,-0.1467767242717));
#38958=CARTESIAN_POINT('Ctrl Pts',(-0.6359126558604,-0.8195263571088,-0.1922231103981));
#38959=CARTESIAN_POINT('Ctrl Pts',(-0.9979529948525,-0.2830162467567,-0.2376694965245));
#38960=CARTESIAN_POINT('Ctrl Pts',(-0.9714658785124,0.363679007019,-0.2831158826508));
#38961=CARTESIAN_POINT('Ctrl Pts',(-0.5667633924888,0.8687851459845,-0.3285622687772));
#38962=CARTESIAN_POINT('Ctrl Pts',(0.05859391180608,1.035652029771,-0.3740086549036));
#38963=CARTESIAN_POINT('Ctrl Pts',(0.6611391764405,0.7993143077222,-0.41945504103));
#38964=CARTESIAN_POINT('Ctrl Pts',(1.006286827598,0.2517840220961,-0.4649014271564));
#38965=CARTESIAN_POINT('Ctrl Pts',(0.9596624628927,-0.3937719269989,-0.5103478132827));
#38966=CARTESIAN_POINT('Ctrl Pts',(0.5394180851663,-0.8860228566873,-0.5557941994091));
#38967=CARTESIAN_POINT('Ctrl Pts',(-0.09083491517071,-1.033323468892,-0.6012405855355));
#38968=CARTESIAN_POINT('Ctrl Pts',(-0.6857236666216,-0.7783260410752,-0.6466869716619));
#38969=CARTESIAN_POINT('Ctrl Pts',(-1.013643462657,-0.2203072939477,-0.6921333577882));
#38970=CARTESIAN_POINT('Ctrl Pts',(-0.9469271253684,0.4234824583282,-0.7375797439146));
#38971=CARTESIAN_POINT('Ctrl Pts',(-0.5115489524506,0.9024001563583,-0.783026130041));
#38972=CARTESIAN_POINT('Ctrl Pts',(0.1229877087451,1.029991454701,-0.8284725161674));
#38973=CARTESIAN_POINT('Ctrl Pts',(0.7096422575036,0.7565819468032,-0.8739189022937));
#38974=CARTESIAN_POINT('Ctrl Pts',(1.020015746615,0.1886166284744,-0.9193652884201));
#38975=CARTESIAN_POINT('Ctrl Pts',(0.9332722659451,-0.4527817546746,-0.9648116745465));
#38976=CARTESIAN_POINT('Ctrl Pts',(0.4831829360834,-0.9179011189761,-1.010258060673));
#38977=CARTESIAN_POINT('Ctrl Pts',(-0.1550206148297,-1.025659306074,-1.055704446799));
#38978=CARTESIAN_POINT('Ctrl Pts',(-0.7328734174699,-0.7341028298687,-1.101150832926));
#38979=CARTESIAN_POINT('Ctrl Pts',(-1.025391163463,-0.1567439594124,-1.146597219052));
#38980=CARTESIAN_POINT('Ctrl Pts',(-0.9187347609085,0.481645689685,-1.192043605178));
#38981=CARTESIAN_POINT('Ctrl Pts',(-0.4542594454663,0.9324945468184,-1.237489991305));
#38982=CARTESIAN_POINT('Ctrl Pts',(-0.02703741779296,0.9910925044735,-1.267787582056));
#38983=CARTESIAN_POINT('Ctrl Pts',(0.1747761851207,0.9541243551627,-1.282936377431));
#38984=CARTESIAN_POINT('Ctrl Pts',(-0.9278486567136,0.2828371797248,0.1179886138536));
#38985=CARTESIAN_POINT('Ctrl Pts',(-0.8680237607561,0.4790930234802,0.1028398184781));
#38986=CARTESIAN_POINT('Ctrl Pts',(-0.6198030816887,0.8317102040798,0.0725422277272));
#38987=CARTESIAN_POINT('Ctrl Pts',(-0.006020401385728,1.0373137838,0.02709584160082));
#38988=CARTESIAN_POINT('Ctrl Pts',(0.6100667263548,0.8389364077892,-0.01835054452555));
#38989=CARTESIAN_POINT('Ctrl Pts',(0.9886505599867,0.3139752873927,-0.06379693065193));
#38990=CARTESIAN_POINT('Ctrl Pts',(0.9823257752865,-0.3332333632255,-0.1092433167783));
#38991=CARTESIAN_POINT('Ctrl Pts',(0.5935583558294,-0.8507036453223,-0.1546897029047));
#38992=CARTESIAN_POINT('Ctrl Pts',(-0.02629601796974,-1.036974907694,-0.2001360890311));
#38993=CARTESIAN_POINT('Ctrl Pts',(-0.6359126558604,-0.8195263571088,-0.2455824751574));
#38994=CARTESIAN_POINT('Ctrl Pts',(-0.9979529948525,-0.2830162467567,-0.2910288612838));
#38995=CARTESIAN_POINT('Ctrl Pts',(-0.9714658785124,0.363679007019,-0.3364752474102));
#38996=CARTESIAN_POINT('Ctrl Pts',(-0.5667633924888,0.8687851459845,-0.3819216335366));
#38997=CARTESIAN_POINT('Ctrl Pts',(0.05859391180608,1.035652029771,-0.4273680196629));
#38998=CARTESIAN_POINT('Ctrl Pts',(0.6611391764405,0.7993143077222,-0.4728144057893));
#38999=CARTESIAN_POINT('Ctrl Pts',(1.006286827598,0.2517840220961,-0.5182607919157));
#39000=CARTESIAN_POINT('Ctrl Pts',(0.9596624628927,-0.3937719269989,-0.5637071780421));
#39001=CARTESIAN_POINT('Ctrl Pts',(0.5394180851663,-0.8860228566873,-0.6091535641684));
#39002=CARTESIAN_POINT('Ctrl Pts',(-0.09083491517071,-1.033323468892,-0.6545999502948));
#39003=CARTESIAN_POINT('Ctrl Pts',(-0.6857236666216,-0.7783260410752,-0.7000463364212));
#39004=CARTESIAN_POINT('Ctrl Pts',(-1.013643462657,-0.2203072939477,-0.7454927225476));
#39005=CARTESIAN_POINT('Ctrl Pts',(-0.9469271253684,0.4234824583282,-0.790939108674));
#39006=CARTESIAN_POINT('Ctrl Pts',(-0.5115489524506,0.9024001563583,-0.8363854948003));
#39007=CARTESIAN_POINT('Ctrl Pts',(0.1229877087451,1.029991454701,-0.8818318809267));
#39008=CARTESIAN_POINT('Ctrl Pts',(0.7096422575036,0.7565819468032,-0.9272782670531));
#39009=CARTESIAN_POINT('Ctrl Pts',(1.020015746615,0.1886166284744,-0.9727246531795));
#39010=CARTESIAN_POINT('Ctrl Pts',(0.9332722659451,-0.4527817546746,-1.018171039306));
#39011=CARTESIAN_POINT('Ctrl Pts',(0.4831829360834,-0.9179011189761,-1.063617425432));
#39012=CARTESIAN_POINT('Ctrl Pts',(-0.1550206148297,-1.025659306074,-1.109063811559));
#39013=CARTESIAN_POINT('Ctrl Pts',(-0.7328734174699,-0.7341028298687,-1.154510197685));
#39014=CARTESIAN_POINT('Ctrl Pts',(-1.025391163463,-0.1567439594124,-1.199956583811));
#39015=CARTESIAN_POINT('Ctrl Pts',(-0.9187347609085,0.481645689685,-1.245402969938));
#39016=CARTESIAN_POINT('Ctrl Pts',(-0.4542594454663,0.9324945468184,-1.290849356064));
#39017=CARTESIAN_POINT('Ctrl Pts',(-0.02703741779296,0.9910925044735,-1.321146946815));
#39018=CARTESIAN_POINT('Ctrl Pts',(0.1747761851207,0.9541243551627,-1.33629574219));
#39019=CARTESIAN_POINT('Ctrl Pts',(-0.9278486567136,0.2828371797248,0.06462924909423));
#39020=CARTESIAN_POINT('Ctrl Pts',(-0.8680237607561,0.4790930234802,0.04948045371878));
#39021=CARTESIAN_POINT('Ctrl Pts',(-0.6198030816887,0.8317102040798,0.01918286296786));
#39022=CARTESIAN_POINT('Ctrl Pts',(-0.006020401385728,1.0373137838,-0.02626352315852));
#39023=CARTESIAN_POINT('Ctrl Pts',(0.6100667263548,0.8389364077892,-0.07170990928489));
#39024=CARTESIAN_POINT('Ctrl Pts',(0.9886505599867,0.3139752873927,-0.1171562954113));
#39025=CARTESIAN_POINT('Ctrl Pts',(0.9823257752865,-0.3332333632255,-0.1626026815376));
#39026=CARTESIAN_POINT('Ctrl Pts',(0.5935583558294,-0.8507036453223,-0.208049067664));
#39027=CARTESIAN_POINT('Ctrl Pts',(-0.02629601796974,-1.036974907694,-0.2534954537904));
#39028=CARTESIAN_POINT('Ctrl Pts',(-0.6359126558604,-0.8195263571088,-0.2989418399168));
#39029=CARTESIAN_POINT('Ctrl Pts',(-0.9979529948525,-0.2830162467567,-0.3443882260432));
#39030=CARTESIAN_POINT('Ctrl Pts',(-0.9714658785124,0.363679007019,-0.3898346121695));
#39031=CARTESIAN_POINT('Ctrl Pts',(-0.5667633924888,0.8687851459845,-0.4352809982959));
#39032=CARTESIAN_POINT('Ctrl Pts',(0.05859391180608,1.035652029771,-0.4807273844223));
#39033=CARTESIAN_POINT('Ctrl Pts',(0.6611391764405,0.7993143077222,-0.5261737705487));
#39034=CARTESIAN_POINT('Ctrl Pts',(1.006286827598,0.2517840220961,-0.571620156675));
#39035=CARTESIAN_POINT('Ctrl Pts',(0.9596624628927,-0.3937719269989,-0.6170665428014));
#39036=CARTESIAN_POINT('Ctrl Pts',(0.5394180851663,-0.8860228566873,-0.6625129289278));
#39037=CARTESIAN_POINT('Ctrl Pts',(-0.09083491517071,-1.033323468892,-0.7079593150542));
#39038=CARTESIAN_POINT('Ctrl Pts',(-0.6857236666216,-0.7783260410752,-0.7534057011805));
#39039=CARTESIAN_POINT('Ctrl Pts',(-1.013643462657,-0.2203072939477,-0.7988520873069));
#39040=CARTESIAN_POINT('Ctrl Pts',(-0.9469271253684,0.4234824583282,-0.8442984734333));
#39041=CARTESIAN_POINT('Ctrl Pts',(-0.5115489524506,0.9024001563583,-0.8897448595597));
#39042=CARTESIAN_POINT('Ctrl Pts',(0.1229877087451,1.029991454701,-0.935191245686));
#39043=CARTESIAN_POINT('Ctrl Pts',(0.7096422575036,0.7565819468032,-0.9806376318124));
#39044=CARTESIAN_POINT('Ctrl Pts',(1.020015746615,0.1886166284744,-1.026084017939));
#39045=CARTESIAN_POINT('Ctrl Pts',(0.9332722659451,-0.4527817546746,-1.071530404065));
#39046=CARTESIAN_POINT('Ctrl Pts',(0.4831829360834,-0.9179011189761,-1.116976790192));
#39047=CARTESIAN_POINT('Ctrl Pts',(-0.1550206148297,-1.025659306074,-1.162423176318));
#39048=CARTESIAN_POINT('Ctrl Pts',(-0.7328734174699,-0.7341028298688,-1.207869562444));
#39049=CARTESIAN_POINT('Ctrl Pts',(-1.025391163463,-0.1567439594124,-1.253315948571));
#39050=CARTESIAN_POINT('Ctrl Pts',(-0.9187347609085,0.481645689685,-1.298762334697));
#39051=CARTESIAN_POINT('Ctrl Pts',(-0.4542594454663,0.9324945468184,-1.344208720823));
#39052=CARTESIAN_POINT('Ctrl Pts',(-0.02703741779297,0.9910925044735,-1.374506311574));
#39053=CARTESIAN_POINT('Ctrl Pts',(0.1747761851207,0.9541243551627,-1.38965510695));
#39054=CARTESIAN_POINT('Ctrl Pts',(-0.9278486567136,0.2828371797248,0.01126988433489));
#39055=CARTESIAN_POINT('Ctrl Pts',(-0.8680237607561,0.4790930234802,-0.003878911040566));
#39056=CARTESIAN_POINT('Ctrl Pts',(-0.6198030816887,0.8317102040798,-0.03417650179148));
#39057=CARTESIAN_POINT('Ctrl Pts',(-0.006020401385728,1.0373137838,-0.07962288791786));
#39058=CARTESIAN_POINT('Ctrl Pts',(0.6100667263548,0.8389364077892,-0.1250692740442));
#39059=CARTESIAN_POINT('Ctrl Pts',(0.9886505599867,0.3139752873927,-0.1705156601706));
#39060=CARTESIAN_POINT('Ctrl Pts',(0.9823257752865,-0.3332333632255,-0.215962046297));
#39061=CARTESIAN_POINT('Ctrl Pts',(0.5935583558294,-0.8507036453223,-0.2614084324234));
#39062=CARTESIAN_POINT('Ctrl Pts',(-0.02629601796974,-1.036974907694,-0.3068548185497));
#39063=CARTESIAN_POINT('Ctrl Pts',(-0.6359126558604,-0.8195263571088,-0.3523012046761));
#39064=CARTESIAN_POINT('Ctrl Pts',(-0.9979529948525,-0.2830162467567,-0.3977475908025));
#39065=CARTESIAN_POINT('Ctrl Pts',(-0.9714658785124,0.363679007019,-0.4431939769289));
#39066=CARTESIAN_POINT('Ctrl Pts',(-0.5667633924888,0.8687851459845,-0.4886403630552));
#39067=CARTESIAN_POINT('Ctrl Pts',(0.05859391180608,1.035652029771,-0.5340867491816));
#39068=CARTESIAN_POINT('Ctrl Pts',(0.6611391764405,0.7993143077222,-0.579533135308));
#39069=CARTESIAN_POINT('Ctrl Pts',(1.006286827598,0.2517840220961,-0.6249795214344));
#39070=CARTESIAN_POINT('Ctrl Pts',(0.9596624628927,-0.3937719269989,-0.6704259075608));
#39071=CARTESIAN_POINT('Ctrl Pts',(0.5394180851663,-0.8860228566873,-0.7158722936871));
#39072=CARTESIAN_POINT('Ctrl Pts',(-0.09083491517071,-1.033323468892,-0.7613186798135));
#39073=CARTESIAN_POINT('Ctrl Pts',(-0.6857236666216,-0.7783260410752,-0.8067650659399));
#39074=CARTESIAN_POINT('Ctrl Pts',(-1.013643462657,-0.2203072939477,-0.8522114520663));
#39075=CARTESIAN_POINT('Ctrl Pts',(-0.9469271253684,0.4234824583282,-0.8976578381926));
#39076=CARTESIAN_POINT('Ctrl Pts',(-0.5115489524506,0.9024001563583,-0.943104224319));
#39077=CARTESIAN_POINT('Ctrl Pts',(0.1229877087451,1.029991454701,-0.9885506104454));
#39078=CARTESIAN_POINT('Ctrl Pts',(0.7096422575036,0.7565819468032,-1.033996996572));
#39079=CARTESIAN_POINT('Ctrl Pts',(1.020015746615,0.1886166284744,-1.079443382698));
#39080=CARTESIAN_POINT('Ctrl Pts',(0.9332722659451,-0.4527817546746,-1.124889768825));
#39081=CARTESIAN_POINT('Ctrl Pts',(0.4831829360834,-0.9179011189761,-1.170336154951));
#39082=CARTESIAN_POINT('Ctrl Pts',(-0.1550206148297,-1.025659306074,-1.215782541077));
#39083=CARTESIAN_POINT('Ctrl Pts',(-0.7328734174699,-0.7341028298688,-1.261228927204));
#39084=CARTESIAN_POINT('Ctrl Pts',(-1.025391163463,-0.1567439594124,-1.30667531333));
#39085=CARTESIAN_POINT('Ctrl Pts',(-0.9187347609085,0.481645689685,-1.352121699456));
#39086=CARTESIAN_POINT('Ctrl Pts',(-0.4542594454663,0.9324945468184,-1.397568085583));
#39087=CARTESIAN_POINT('Ctrl Pts',(-0.02703741779297,0.9910925044735,-1.427865676334));
#39088=CARTESIAN_POINT('Ctrl Pts',(0.1747761851207,0.9541243551627,-1.443014471709));
#39089=CARTESIAN_POINT('',(-0.2015628224599,0.948826869667,-1.271666493096));
#39090=CARTESIAN_POINT('Ctrl Pts',(-0.5831303237782,0.7751509694829,-1.22376920223));
#39091=CARTESIAN_POINT('Ctrl Pts',(-0.400218113725,0.9127521084488,-1.240669293422));
#39092=CARTESIAN_POINT('Ctrl Pts',(0.06620921823847,1.052270487825,-1.274469475806));
#39093=CARTESIAN_POINT('Ctrl Pts',(0.7347269571914,0.7563971597966,-1.325169749382));
#39094=CARTESIAN_POINT('Ctrl Pts',(1.049982749214,0.09689423608854,-1.375870022958));
#39095=CARTESIAN_POINT('Ctrl Pts',(0.8607148729301,-0.6091341314935,-1.426570296534));
#39096=CARTESIAN_POINT('Ctrl Pts',(0.2578136123524,-1.022450654046,-1.47727057011));
#39097=CARTESIAN_POINT('Ctrl Pts',(-0.4689774525342,-0.944421661856,-1.527970843686));
#39098=CARTESIAN_POINT('Ctrl Pts',(-0.9704004517988,-0.4125477163584,-1.578671117262));
#39099=CARTESIAN_POINT('Ctrl Pts',(-1.005493306747,0.317577906859,-1.629371390838));
#39100=CARTESIAN_POINT('Ctrl Pts',(-0.5573923286712,0.8950901223419,-1.680071664414));
#39101=CARTESIAN_POINT('Ctrl Pts',(0.1585658204783,1.042463149571,-1.73077193799));
#39102=CARTESIAN_POINT('Ctrl Pts',(0.7983245141496,0.6888762627836,-1.781472211566));
#39103=CARTESIAN_POINT('Ctrl Pts',(1.054445113962,0.004247084557393,-1.832172485142));
#39104=CARTESIAN_POINT('Ctrl Pts',(0.8038478213541,-0.6824230477092,-1.882872758718));
#39105=CARTESIAN_POINT('Ctrl Pts',(0.1669581858966,-1.041152006244,-1.933573032294));
#39106=CARTESIAN_POINT('Ctrl Pts',(-0.5501638854909,-0.8995511297614,-1.98427330587));
#39107=CARTESIAN_POINT('Ctrl Pts',(-1.00290246203,-0.3256672958743,-2.034973579446));
#39108=CARTESIAN_POINT('Ctrl Pts',(-0.9736921777191,0.4047172828064,-2.085673853022));
#39109=CARTESIAN_POINT('Ctrl Pts',(-0.4765701535821,0.9406133236668,-2.136374126598));
#39110=CARTESIAN_POINT('Ctrl Pts',(0.2495695979012,1.024493802687,-2.187074400174));
#39111=CARTESIAN_POINT('Ctrl Pts',(0.8557776632566,0.6160496142012,-2.23777467375));
#39112=CARTESIAN_POINT('Ctrl Pts',(1.050738288296,-0.0884397242642,-2.288474947326));
#39113=CARTESIAN_POINT('Ctrl Pts',(0.7407623530892,-0.7504289932324,-2.339175220902));
#39114=CARTESIAN_POINT('Ctrl Pts',(0.07481004734727,-1.051796554468,-2.389875494478));
#39115=CARTESIAN_POINT('Ctrl Pts',(-0.6270925081245,-0.847719000077,-2.440575768054));
#39116=CARTESIAN_POINT('Ctrl Pts',(-1.02764329207,-0.2362666277473,-2.49127604163));
#39117=CARTESIAN_POINT('Ctrl Pts',(-0.9343555872731,0.4887246289065,-2.541976315206));
#39118=CARTESIAN_POINT('Ctrl Pts',(-0.3920607004213,0.9788572959625,-2.592676588782));
#39119=CARTESIAN_POINT('Ctrl Pts',(0.3386450271169,0.9985960285533,-2.643376862358));
#39120=CARTESIAN_POINT('Ctrl Pts',(0.9065968071483,0.5384556582503,-2.694077135934));
#39121=CARTESIAN_POINT('Ctrl Pts',(1.038942130304,-0.1804428298701,-2.74477740951));
#39122=CARTESIAN_POINT('Ctrl Pts',(0.6717869665382,-0.8126248283907,-2.795477683086));
#39123=CARTESIAN_POINT('Ctrl Pts',(0.212375641378,-0.9737492166778,-2.82927786547));
#39124=CARTESIAN_POINT('Ctrl Pts',(-0.01648200808866,-0.9698599607208,-2.846177956662));
#39125=CARTESIAN_POINT('Ctrl Pts',(-0.5831303237782,0.7751509694829,-1.277128566989));
#39126=CARTESIAN_POINT('Ctrl Pts',(-0.400218113725,0.9127521084488,-1.294028658181));
#39127=CARTESIAN_POINT('Ctrl Pts',(0.06620921823847,1.052270487825,-1.327828840565));
#39128=CARTESIAN_POINT('Ctrl Pts',(0.7347269571914,0.7563971597966,-1.378529114141));
#39129=CARTESIAN_POINT('Ctrl Pts',(1.049982749214,0.09689423608854,-1.429229387717));
#39130=CARTESIAN_POINT('Ctrl Pts',(0.8607148729301,-0.6091341314935,-1.479929661293));
#39131=CARTESIAN_POINT('Ctrl Pts',(0.2578136123524,-1.022450654046,-1.530629934869));
#39132=CARTESIAN_POINT('Ctrl Pts',(-0.4689774525342,-0.944421661856,-1.581330208445));
#39133=CARTESIAN_POINT('Ctrl Pts',(-0.9704004517988,-0.4125477163584,-1.632030482021));
#39134=CARTESIAN_POINT('Ctrl Pts',(-1.005493306747,0.317577906859,-1.682730755597));
#39135=CARTESIAN_POINT('Ctrl Pts',(-0.5573923286712,0.8950901223419,-1.733431029173));
#39136=CARTESIAN_POINT('Ctrl Pts',(0.1585658204783,1.042463149571,-1.784131302749));
#39137=CARTESIAN_POINT('Ctrl Pts',(0.7983245141496,0.6888762627836,-1.834831576325));
#39138=CARTESIAN_POINT('Ctrl Pts',(1.054445113962,0.004247084557393,-1.885531849901));
#39139=CARTESIAN_POINT('Ctrl Pts',(0.8038478213541,-0.6824230477092,-1.936232123477));
#39140=CARTESIAN_POINT('Ctrl Pts',(0.1669581858966,-1.041152006244,-1.986932397053));
#39141=CARTESIAN_POINT('Ctrl Pts',(-0.5501638854909,-0.8995511297614,-2.037632670629));
#39142=CARTESIAN_POINT('Ctrl Pts',(-1.00290246203,-0.3256672958743,-2.088332944205));
#39143=CARTESIAN_POINT('Ctrl Pts',(-0.9736921777191,0.4047172828064,-2.139033217781));
#39144=CARTESIAN_POINT('Ctrl Pts',(-0.4765701535821,0.9406133236668,-2.189733491357));
#39145=CARTESIAN_POINT('Ctrl Pts',(0.2495695979012,1.024493802687,-2.240433764933));
#39146=CARTESIAN_POINT('Ctrl Pts',(0.8557776632566,0.6160496142012,-2.291134038509));
#39147=CARTESIAN_POINT('Ctrl Pts',(1.050738288296,-0.0884397242642,-2.341834312085));
#39148=CARTESIAN_POINT('Ctrl Pts',(0.7407623530892,-0.7504289932324,-2.392534585661));
#39149=CARTESIAN_POINT('Ctrl Pts',(0.07481004734727,-1.051796554468,-2.443234859237));
#39150=CARTESIAN_POINT('Ctrl Pts',(-0.6270925081245,-0.847719000077,-2.493935132813));
#39151=CARTESIAN_POINT('Ctrl Pts',(-1.02764329207,-0.2362666277473,-2.544635406389));
#39152=CARTESIAN_POINT('Ctrl Pts',(-0.9343555872731,0.4887246289065,-2.595335679965));
#39153=CARTESIAN_POINT('Ctrl Pts',(-0.3920607004213,0.9788572959625,-2.646035953541));
#39154=CARTESIAN_POINT('Ctrl Pts',(0.3386450271169,0.9985960285533,-2.696736227117));
#39155=CARTESIAN_POINT('Ctrl Pts',(0.9065968071483,0.5384556582503,-2.747436500693));
#39156=CARTESIAN_POINT('Ctrl Pts',(1.038942130304,-0.1804428298701,-2.798136774269));
#39157=CARTESIAN_POINT('Ctrl Pts',(0.6717869665382,-0.8126248283907,-2.848837047845));
#39158=CARTESIAN_POINT('Ctrl Pts',(0.212375641378,-0.9737492166778,-2.882637230229));
#39159=CARTESIAN_POINT('Ctrl Pts',(-0.01648200808866,-0.9698599607208,-2.899537321421));
#39160=CARTESIAN_POINT('Ctrl Pts',(-0.5831303237782,0.7751509694829,-1.330487931748));
#39161=CARTESIAN_POINT('Ctrl Pts',(-0.400218113725,0.9127521084488,-1.34738802294));
#39162=CARTESIAN_POINT('Ctrl Pts',(0.06620921823847,1.052270487825,-1.381188205324));
#39163=CARTESIAN_POINT('Ctrl Pts',(0.7347269571914,0.7563971597966,-1.4318884789));
#39164=CARTESIAN_POINT('Ctrl Pts',(1.049982749214,0.09689423608854,-1.482588752476));
#39165=CARTESIAN_POINT('Ctrl Pts',(0.8607148729301,-0.6091341314935,-1.533289026052));
#39166=CARTESIAN_POINT('Ctrl Pts',(0.2578136123524,-1.022450654046,-1.583989299628));
#39167=CARTESIAN_POINT('Ctrl Pts',(-0.4689774525342,-0.944421661856,-1.634689573204));
#39168=CARTESIAN_POINT('Ctrl Pts',(-0.9704004517988,-0.4125477163584,-1.68538984678));
#39169=CARTESIAN_POINT('Ctrl Pts',(-1.005493306747,0.317577906859,-1.736090120356));
#39170=CARTESIAN_POINT('Ctrl Pts',(-0.5573923286712,0.8950901223419,-1.786790393932));
#39171=CARTESIAN_POINT('Ctrl Pts',(0.1585658204783,1.042463149571,-1.837490667508));
#39172=CARTESIAN_POINT('Ctrl Pts',(0.7983245141496,0.6888762627836,-1.888190941084));
#39173=CARTESIAN_POINT('Ctrl Pts',(1.054445113962,0.004247084557393,-1.93889121466));
#39174=CARTESIAN_POINT('Ctrl Pts',(0.8038478213541,-0.6824230477092,-1.989591488236));
#39175=CARTESIAN_POINT('Ctrl Pts',(0.1669581858966,-1.041152006244,-2.040291761812));
#39176=CARTESIAN_POINT('Ctrl Pts',(-0.5501638854909,-0.8995511297614,-2.090992035388));
#39177=CARTESIAN_POINT('Ctrl Pts',(-1.00290246203,-0.3256672958743,-2.141692308964));
#39178=CARTESIAN_POINT('Ctrl Pts',(-0.9736921777191,0.4047172828064,-2.19239258254));
#39179=CARTESIAN_POINT('Ctrl Pts',(-0.4765701535821,0.9406133236668,-2.243092856116));
#39180=CARTESIAN_POINT('Ctrl Pts',(0.2495695979012,1.024493802687,-2.293793129692));
#39181=CARTESIAN_POINT('Ctrl Pts',(0.8557776632566,0.6160496142012,-2.344493403268));
#39182=CARTESIAN_POINT('Ctrl Pts',(1.050738288296,-0.0884397242642,-2.395193676844));
#39183=CARTESIAN_POINT('Ctrl Pts',(0.7407623530892,-0.7504289932324,-2.44589395042));
#39184=CARTESIAN_POINT('Ctrl Pts',(0.07481004734727,-1.051796554468,-2.496594223996));
#39185=CARTESIAN_POINT('Ctrl Pts',(-0.6270925081245,-0.847719000077,-2.547294497572));
#39186=CARTESIAN_POINT('Ctrl Pts',(-1.02764329207,-0.2362666277473,-2.597994771148));
#39187=CARTESIAN_POINT('Ctrl Pts',(-0.9343555872731,0.4887246289065,-2.648695044724));
#39188=CARTESIAN_POINT('Ctrl Pts',(-0.3920607004213,0.9788572959625,-2.6993953183));
#39189=CARTESIAN_POINT('Ctrl Pts',(0.3386450271169,0.9985960285533,-2.750095591876));
#39190=CARTESIAN_POINT('Ctrl Pts',(0.9065968071483,0.5384556582503,-2.800795865452));
#39191=CARTESIAN_POINT('Ctrl Pts',(1.038942130304,-0.1804428298701,-2.851496139028));
#39192=CARTESIAN_POINT('Ctrl Pts',(0.6717869665382,-0.8126248283907,-2.902196412604));
#39193=CARTESIAN_POINT('Ctrl Pts',(0.212375641378,-0.9737492166778,-2.935996594988));
#39194=CARTESIAN_POINT('Ctrl Pts',(-0.01648200808866,-0.9698599607208,-2.95289668618));
#39195=CARTESIAN_POINT('Ctrl Pts',(-0.5831303237782,0.7751509694829,-1.383847296508));
#39196=CARTESIAN_POINT('Ctrl Pts',(-0.400218113725,0.9127521084488,-1.4007473877));
#39197=CARTESIAN_POINT('Ctrl Pts',(0.06620921823847,1.052270487825,-1.434547570084));
#39198=CARTESIAN_POINT('Ctrl Pts',(0.7347269571914,0.7563971597966,-1.48524784366));
#39199=CARTESIAN_POINT('Ctrl Pts',(1.049982749214,0.09689423608854,-1.535948117236));
#39200=CARTESIAN_POINT('Ctrl Pts',(0.8607148729301,-0.6091341314935,-1.586648390812));
#39201=CARTESIAN_POINT('Ctrl Pts',(0.2578136123524,-1.022450654046,-1.637348664388));
#39202=CARTESIAN_POINT('Ctrl Pts',(-0.4689774525342,-0.944421661856,-1.688048937964));
#39203=CARTESIAN_POINT('Ctrl Pts',(-0.9704004517988,-0.4125477163584,-1.73874921154));
#39204=CARTESIAN_POINT('Ctrl Pts',(-1.005493306747,0.317577906859,-1.789449485116));
#39205=CARTESIAN_POINT('Ctrl Pts',(-0.5573923286712,0.8950901223419,-1.840149758692));
#39206=CARTESIAN_POINT('Ctrl Pts',(0.1585658204783,1.042463149571,-1.890850032268));
#39207=CARTESIAN_POINT('Ctrl Pts',(0.7983245141496,0.6888762627836,-1.941550305844));
#39208=CARTESIAN_POINT('Ctrl Pts',(1.054445113962,0.004247084557393,-1.99225057942));
#39209=CARTESIAN_POINT('Ctrl Pts',(0.8038478213541,-0.6824230477092,-2.042950852996));
#39210=CARTESIAN_POINT('Ctrl Pts',(0.1669581858966,-1.041152006244,-2.093651126572));
#39211=CARTESIAN_POINT('Ctrl Pts',(-0.5501638854909,-0.8995511297614,-2.144351400148));
#39212=CARTESIAN_POINT('Ctrl Pts',(-1.00290246203,-0.3256672958743,-2.195051673724));
#39213=CARTESIAN_POINT('Ctrl Pts',(-0.9736921777191,0.4047172828064,-2.2457519473));
#39214=CARTESIAN_POINT('Ctrl Pts',(-0.4765701535821,0.9406133236668,-2.296452220876));
#39215=CARTESIAN_POINT('Ctrl Pts',(0.2495695979012,1.024493802687,-2.347152494452));
#39216=CARTESIAN_POINT('Ctrl Pts',(0.8557776632566,0.6160496142012,-2.397852768028));
#39217=CARTESIAN_POINT('Ctrl Pts',(1.050738288296,-0.0884397242642,-2.448553041604));
#39218=CARTESIAN_POINT('Ctrl Pts',(0.7407623530892,-0.7504289932324,-2.49925331518));
#39219=CARTESIAN_POINT('Ctrl Pts',(0.07481004734727,-1.051796554468,-2.549953588756));
#39220=CARTESIAN_POINT('Ctrl Pts',(-0.6270925081245,-0.847719000077,-2.600653862332));
#39221=CARTESIAN_POINT('Ctrl Pts',(-1.02764329207,-0.2362666277473,-2.651354135908));
#39222=CARTESIAN_POINT('Ctrl Pts',(-0.9343555872731,0.4887246289065,-2.702054409484));
#39223=CARTESIAN_POINT('Ctrl Pts',(-0.3920607004213,0.9788572959625,-2.75275468306));
#39224=CARTESIAN_POINT('Ctrl Pts',(0.3386450271169,0.9985960285533,-2.803454956636));
#39225=CARTESIAN_POINT('Ctrl Pts',(0.9065968071483,0.5384556582503,-2.854155230212));
#39226=CARTESIAN_POINT('Ctrl Pts',(1.038942130304,-0.1804428298701,-2.904855503788));
#39227=CARTESIAN_POINT('Ctrl Pts',(0.6717869665382,-0.8126248283907,-2.955555777364));
#39228=CARTESIAN_POINT('Ctrl Pts',(0.212375641378,-0.9737492166778,-2.989355959748));
#39229=CARTESIAN_POINT('Ctrl Pts',(-0.01648200808866,-0.9698599607208,-3.00625605094));
#39230=CARTESIAN_POINT('',(0.3943262306718,-0.8862318115506,-2.831674910819));
#39231=CARTESIAN_POINT('Ctrl Pts',(0.7314756051133,-0.6370584267743,-2.783777619953));
#39232=CARTESIAN_POINT('Ctrl Pts',(0.581149063108,-0.8096645703499,-2.800677711145));
#39233=CARTESIAN_POINT('Ctrl Pts',(0.1538943548793,-1.043059618461,-2.834477893529));
#39234=CARTESIAN_POINT('Ctrl Pts',(-0.5615125076522,-0.8925604006017,-2.885178167105));
#39235=CARTESIAN_POINT('Ctrl Pts',(-1.006929453025,-0.3129622074044,-2.935878440681));
#39236=CARTESIAN_POINT('Ctrl Pts',(-0.9685032921222,0.4169842392488,-2.986578714257));
#39237=CARTESIAN_POINT('Ctrl Pts',(-0.4646479612591,0.9465598083437,-3.037278987833));
#39238=CARTESIAN_POINT('Ctrl Pts',(0.2624928994603,1.021258833059,-3.087979261409));
#39239=CARTESIAN_POINT('Ctrl Pts',(0.8634925163867,0.6051886724552,-3.138679534985));
#39240=CARTESIAN_POINT('Ctrl Pts',(1.049537078319,-0.1017076106887,-3.189379808561));
#39241=CARTESIAN_POINT('Ctrl Pts',(0.7312223812419,-0.7597278225434,-3.240080082137));
#39242=CARTESIAN_POINT('Ctrl Pts',(0.06151577696635,-1.052657753889,-3.290780355713));
#39243=CARTESIAN_POINT('Ctrl Pts',(-0.6377524802956,-0.8397287116657,-3.341480629289));
#39244=CARTESIAN_POINT('Ctrl Pts',(-1.030546188006,-0.2232646198403,-3.392180902865));
#39245=CARTESIAN_POINT('Ctrl Pts',(-0.9281067295174,0.5004901942744,-3.442881176441));
#39246=CARTESIAN_POINT('Ctrl Pts',(-0.3796618039978,0.98373240799,-3.493581450017));
#39247=CARTESIAN_POINT('Ctrl Pts',(0.3512311470232,0.9942380083834,-3.544281723593));
#39248=CARTESIAN_POINT('Ctrl Pts',(0.9133385405055,0.5269584863877,-3.594981997169));
#39249=CARTESIAN_POINT('Ctrl Pts',(1.036537380232,-0.1935530814404,-3.645682270745));
#39250=CARTESIAN_POINT('Ctrl Pts',(0.6616239622285,-0.8210519280471,-3.696382544321));
#39251=CARTESIAN_POINT('Ctrl Pts',(-0.03123554420463,-1.053990928196,-3.747082817897));
#39252=CARTESIAN_POINT('Ctrl Pts',(-0.7090846828299,-0.7804302971197,-3.797783091473));
#39253=CARTESIAN_POINT('Ctrl Pts',(-1.046180290065,-0.1318307096162,-3.848483365049));
#39254=CARTESIAN_POINT('Ctrl Pts',(-0.8805297016293,0.5801206617478,-3.899183638625));
#39255=CARTESIAN_POINT('Ctrl Pts',(-0.2917369744498,1.013292688671,-3.949883912201));
#39256=CARTESIAN_POINT('Ctrl Pts',(0.4372511207908,0.9595227846198,-4.000584185777));
#39257=CARTESIAN_POINT('Ctrl Pts',(0.9561164944406,0.4446503167462,-4.051284459353));
#39258=CARTESIAN_POINT('Ctrl Pts',(1.015515879006,-0.2839007323944,-4.101984732929));
#39259=CARTESIAN_POINT('Ctrl Pts',(0.5869061509895,-0.8760218996147,-4.152685006505));
#39260=CARTESIAN_POINT('Ctrl Pts',(-0.1237481103043,-1.04716803228,-4.203385280081));
#39261=CARTESIAN_POINT('Ctrl Pts',(-0.7749183178661,-0.7150901112928,-4.254085553657));
#39262=CARTESIAN_POINT('Ctrl Pts',(-1.053759562209,-0.03938464199691,-4.304785827233));
#39263=CARTESIAN_POINT('Ctrl Pts',(-0.8259839985102,0.6552917474932,-4.355486100809));
#39264=CARTESIAN_POINT('Ctrl Pts',(-0.4100818097771,0.9083632859827,-4.389286283193));
#39265=CARTESIAN_POINT('Ctrl Pts',(-0.1854114834362,0.9521147944497,-4.406186374385));
#39266=CARTESIAN_POINT('Ctrl Pts',(0.7314756051133,-0.6370584267743,-2.837136984712));
#39267=CARTESIAN_POINT('Ctrl Pts',(0.581149063108,-0.8096645703499,-2.854037075904));
#39268=CARTESIAN_POINT('Ctrl Pts',(0.1538943548793,-1.043059618461,-2.887837258288));
#39269=CARTESIAN_POINT('Ctrl Pts',(-0.5615125076522,-0.8925604006017,-2.938537531864));
#39270=CARTESIAN_POINT('Ctrl Pts',(-1.006929453025,-0.3129622074044,-2.98923780544));
#39271=CARTESIAN_POINT('Ctrl Pts',(-0.9685032921222,0.4169842392488,-3.039938079016));
#39272=CARTESIAN_POINT('Ctrl Pts',(-0.4646479612591,0.9465598083437,-3.090638352592));
#39273=CARTESIAN_POINT('Ctrl Pts',(0.2624928994603,1.021258833059,-3.141338626168));
#39274=CARTESIAN_POINT('Ctrl Pts',(0.8634925163867,0.6051886724552,-3.192038899744));
#39275=CARTESIAN_POINT('Ctrl Pts',(1.049537078319,-0.1017076106887,-3.24273917332));
#39276=CARTESIAN_POINT('Ctrl Pts',(0.7312223812419,-0.7597278225434,-3.293439446896));
#39277=CARTESIAN_POINT('Ctrl Pts',(0.06151577696635,-1.052657753889,-3.344139720472));
#39278=CARTESIAN_POINT('Ctrl Pts',(-0.6377524802956,-0.8397287116657,-3.394839994048));
#39279=CARTESIAN_POINT('Ctrl Pts',(-1.030546188006,-0.2232646198403,-3.445540267624));
#39280=CARTESIAN_POINT('Ctrl Pts',(-0.9281067295174,0.5004901942744,-3.4962405412));
#39281=CARTESIAN_POINT('Ctrl Pts',(-0.3796618039978,0.98373240799,-3.546940814776));
#39282=CARTESIAN_POINT('Ctrl Pts',(0.3512311470232,0.9942380083834,-3.597641088352));
#39283=CARTESIAN_POINT('Ctrl Pts',(0.9133385405055,0.5269584863877,-3.648341361928));
#39284=CARTESIAN_POINT('Ctrl Pts',(1.036537380232,-0.1935530814404,-3.699041635504));
#39285=CARTESIAN_POINT('Ctrl Pts',(0.6616239622285,-0.8210519280471,-3.74974190908));
#39286=CARTESIAN_POINT('Ctrl Pts',(-0.03123554420463,-1.053990928196,-3.800442182656));
#39287=CARTESIAN_POINT('Ctrl Pts',(-0.7090846828299,-0.7804302971197,-3.851142456232));
#39288=CARTESIAN_POINT('Ctrl Pts',(-1.046180290065,-0.1318307096162,-3.901842729808));
#39289=CARTESIAN_POINT('Ctrl Pts',(-0.8805297016293,0.5801206617478,-3.952543003384));
#39290=CARTESIAN_POINT('Ctrl Pts',(-0.2917369744498,1.013292688671,-4.00324327696));
#39291=CARTESIAN_POINT('Ctrl Pts',(0.4372511207908,0.9595227846198,-4.053943550536));
#39292=CARTESIAN_POINT('Ctrl Pts',(0.9561164944406,0.4446503167462,-4.104643824112));
#39293=CARTESIAN_POINT('Ctrl Pts',(1.015515879006,-0.2839007323944,-4.155344097688));
#39294=CARTESIAN_POINT('Ctrl Pts',(0.5869061509895,-0.8760218996147,-4.206044371264));
#39295=CARTESIAN_POINT('Ctrl Pts',(-0.1237481103043,-1.04716803228,-4.25674464484));
#39296=CARTESIAN_POINT('Ctrl Pts',(-0.7749183178661,-0.7150901112928,-4.307444918416));
#39297=CARTESIAN_POINT('Ctrl Pts',(-1.053759562209,-0.03938464199691,-4.358145191992));
#39298=CARTESIAN_POINT('Ctrl Pts',(-0.8259839985102,0.6552917474932,-4.408845465568));
#39299=CARTESIAN_POINT('Ctrl Pts',(-0.4100818097771,0.9083632859827,-4.442645647952));
#39300=CARTESIAN_POINT('Ctrl Pts',(-0.1854114834362,0.9521147944497,-4.459545739144));
#39301=CARTESIAN_POINT('Ctrl Pts',(0.7314756051133,-0.6370584267743,-2.890496349471));
#39302=CARTESIAN_POINT('Ctrl Pts',(0.581149063108,-0.8096645703499,-2.907396440663));
#39303=CARTESIAN_POINT('Ctrl Pts',(0.1538943548793,-1.043059618461,-2.941196623047));
#39304=CARTESIAN_POINT('Ctrl Pts',(-0.5615125076522,-0.8925604006017,-2.991896896623));
#39305=CARTESIAN_POINT('Ctrl Pts',(-1.006929453025,-0.3129622074044,-3.042597170199));
#39306=CARTESIAN_POINT('Ctrl Pts',(-0.9685032921222,0.4169842392488,-3.093297443775));
#39307=CARTESIAN_POINT('Ctrl Pts',(-0.4646479612591,0.9465598083437,-3.143997717351));
#39308=CARTESIAN_POINT('Ctrl Pts',(0.2624928994603,1.021258833059,-3.194697990927));
#39309=CARTESIAN_POINT('Ctrl Pts',(0.8634925163867,0.6051886724552,-3.245398264503));
#39310=CARTESIAN_POINT('Ctrl Pts',(1.049537078319,-0.1017076106887,-3.29609853808));
#39311=CARTESIAN_POINT('Ctrl Pts',(0.7312223812419,-0.7597278225434,-3.346798811656));
#39312=CARTESIAN_POINT('Ctrl Pts',(0.06151577696635,-1.052657753889,-3.397499085232));
#39313=CARTESIAN_POINT('Ctrl Pts',(-0.6377524802956,-0.8397287116657,-3.448199358808));
#39314=CARTESIAN_POINT('Ctrl Pts',(-1.030546188006,-0.2232646198403,-3.498899632384));
#39315=CARTESIAN_POINT('Ctrl Pts',(-0.9281067295174,0.5004901942744,-3.54959990596));
#39316=CARTESIAN_POINT('Ctrl Pts',(-0.3796618039978,0.98373240799,-3.600300179536));
#39317=CARTESIAN_POINT('Ctrl Pts',(0.3512311470232,0.9942380083834,-3.651000453112));
#39318=CARTESIAN_POINT('Ctrl Pts',(0.9133385405055,0.5269584863877,-3.701700726688));
#39319=CARTESIAN_POINT('Ctrl Pts',(1.036537380232,-0.1935530814404,-3.752401000264));
#39320=CARTESIAN_POINT('Ctrl Pts',(0.6616239622285,-0.8210519280471,-3.80310127384));
#39321=CARTESIAN_POINT('Ctrl Pts',(-0.03123554420463,-1.053990928196,-3.853801547416));
#39322=CARTESIAN_POINT('Ctrl Pts',(-0.7090846828299,-0.7804302971197,-3.904501820992));
#39323=CARTESIAN_POINT('Ctrl Pts',(-1.046180290065,-0.1318307096162,-3.955202094568));
#39324=CARTESIAN_POINT('Ctrl Pts',(-0.8805297016293,0.5801206617478,-4.005902368144));
#39325=CARTESIAN_POINT('Ctrl Pts',(-0.2917369744498,1.013292688671,-4.05660264172));
#39326=CARTESIAN_POINT('Ctrl Pts',(0.4372511207908,0.9595227846198,-4.107302915296));
#39327=CARTESIAN_POINT('Ctrl Pts',(0.9561164944406,0.4446503167462,-4.158003188872));
#39328=CARTESIAN_POINT('Ctrl Pts',(1.015515879006,-0.2839007323944,-4.208703462448));
#39329=CARTESIAN_POINT('Ctrl Pts',(0.5869061509895,-0.8760218996147,-4.259403736024));
#39330=CARTESIAN_POINT('Ctrl Pts',(-0.1237481103043,-1.04716803228,-4.3101040096));
#39331=CARTESIAN_POINT('Ctrl Pts',(-0.7749183178661,-0.7150901112928,-4.360804283176));
#39332=CARTESIAN_POINT('Ctrl Pts',(-1.053759562209,-0.03938464199691,-4.411504556752));
#39333=CARTESIAN_POINT('Ctrl Pts',(-0.8259839985102,0.6552917474932,-4.462204830328));
#39334=CARTESIAN_POINT('Ctrl Pts',(-0.4100818097771,0.9083632859827,-4.496005012712));
#39335=CARTESIAN_POINT('Ctrl Pts',(-0.1854114834362,0.9521147944497,-4.512905103904));
#39336=CARTESIAN_POINT('Ctrl Pts',(0.7314756051133,-0.6370584267743,-2.943855714231));
#39337=CARTESIAN_POINT('Ctrl Pts',(0.581149063108,-0.8096645703499,-2.960755805423));
#39338=CARTESIAN_POINT('Ctrl Pts',(0.1538943548793,-1.043059618461,-2.994555987807));
#39339=CARTESIAN_POINT('Ctrl Pts',(-0.5615125076522,-0.8925604006017,-3.045256261383));
#39340=CARTESIAN_POINT('Ctrl Pts',(-1.006929453025,-0.3129622074044,-3.095956534959));
#39341=CARTESIAN_POINT('Ctrl Pts',(-0.9685032921222,0.4169842392488,-3.146656808535));
#39342=CARTESIAN_POINT('Ctrl Pts',(-0.4646479612591,0.9465598083437,-3.197357082111));
#39343=CARTESIAN_POINT('Ctrl Pts',(0.2624928994603,1.021258833059,-3.248057355687));
#39344=CARTESIAN_POINT('Ctrl Pts',(0.8634925163867,0.6051886724552,-3.298757629263));
#39345=CARTESIAN_POINT('Ctrl Pts',(1.049537078319,-0.1017076106887,-3.349457902839));
#39346=CARTESIAN_POINT('Ctrl Pts',(0.7312223812419,-0.7597278225434,-3.400158176415));
#39347=CARTESIAN_POINT('Ctrl Pts',(0.06151577696635,-1.052657753889,-3.450858449991));
#39348=CARTESIAN_POINT('Ctrl Pts',(-0.6377524802956,-0.8397287116657,-3.501558723567));
#39349=CARTESIAN_POINT('Ctrl Pts',(-1.030546188006,-0.2232646198403,-3.552258997143));
#39350=CARTESIAN_POINT('Ctrl Pts',(-0.9281067295174,0.5004901942744,-3.602959270719));
#39351=CARTESIAN_POINT('Ctrl Pts',(-0.3796618039978,0.98373240799,-3.653659544295));
#39352=CARTESIAN_POINT('Ctrl Pts',(0.3512311470232,0.9942380083834,-3.704359817871));
#39353=CARTESIAN_POINT('Ctrl Pts',(0.9133385405055,0.5269584863877,-3.755060091447));
#39354=CARTESIAN_POINT('Ctrl Pts',(1.036537380232,-0.1935530814404,-3.805760365023));
#39355=CARTESIAN_POINT('Ctrl Pts',(0.6616239622285,-0.8210519280471,-3.856460638599));
#39356=CARTESIAN_POINT('Ctrl Pts',(-0.03123554420463,-1.053990928196,-3.907160912175));
#39357=CARTESIAN_POINT('Ctrl Pts',(-0.7090846828299,-0.7804302971197,-3.957861185751));
#39358=CARTESIAN_POINT('Ctrl Pts',(-1.046180290065,-0.1318307096162,-4.008561459327));
#39359=CARTESIAN_POINT('Ctrl Pts',(-0.8805297016293,0.5801206617478,-4.059261732903));
#39360=CARTESIAN_POINT('Ctrl Pts',(-0.2917369744498,1.013292688671,-4.109962006479));
#39361=CARTESIAN_POINT('Ctrl Pts',(0.4372511207908,0.9595227846198,-4.160662280055));
#39362=CARTESIAN_POINT('Ctrl Pts',(0.9561164944406,0.4446503167462,-4.211362553631));
#39363=CARTESIAN_POINT('Ctrl Pts',(1.015515879006,-0.2839007323944,-4.262062827207));
#39364=CARTESIAN_POINT('Ctrl Pts',(0.5869061509895,-0.8760218996147,-4.312763100783));
#39365=CARTESIAN_POINT('Ctrl Pts',(-0.1237481103043,-1.04716803228,-4.363463374359));
#39366=CARTESIAN_POINT('Ctrl Pts',(-0.7749183178661,-0.7150901112928,-4.414163647935));
#39367=CARTESIAN_POINT('Ctrl Pts',(-1.053759562209,-0.03938464199691,-4.464863921511));
#39368=CARTESIAN_POINT('Ctrl Pts',(-0.8259839985102,0.6552917474932,-4.515564195087));
#39369=CARTESIAN_POINT('Ctrl Pts',(-0.4100818097771,0.9083632859827,-4.549364377471));
#39370=CARTESIAN_POINT('Ctrl Pts',(-0.1854114834362,0.9521147944497,-4.566264468663));
#39371=CARTESIAN_POINT('',(-0.5698749570781,0.784947471679,-4.391683328543));
#39372=CARTESIAN_POINT('Ctrl Pts',(-0.8478876321751,0.4711545003548,-4.343786037676));
#39373=CARTESIAN_POINT('Ctrl Pts',(-0.7367094045404,0.6712303652943,-4.360686128868));
#39374=CARTESIAN_POINT('Ctrl Pts',(-0.3672795254541,0.9883130021961,-4.394486311252));
#39375=CARTESIAN_POINT('Ctrl Pts',(0.3637847024261,0.9897580791551,-4.445186584828));
#39376=CARTESIAN_POINT('Ctrl Pts',(0.9199177062286,0.5153675197374,-4.495886858404));
#39377=CARTESIAN_POINT('Ctrl Pts',(1.034010790836,-0.2066305085619,-4.54658713198));
#39378=CARTESIAN_POINT('Ctrl Pts',(0.6511976671912,-0.8293460055482,-4.597287405556));
#39379=CARTESIAN_POINT('Ctrl Pts',(-0.04454897242399,-1.053511991116,-4.647987679132));
#39380=CARTESIAN_POINT('Ctrl Pts',(-0.7188880044982,-0.771409548886,-4.698687952708));
#39381=CARTESIAN_POINT('Ctrl Pts',(-1.047762323398,-0.1186028267124,-4.749388226284));
#39382=CARTESIAN_POINT('Ctrl Pts',(-0.8731302342653,0.5911988913957,-4.80008849986));
#39383=CARTESIAN_POINT('Ctrl Pts',(-0.2789118454146,1.016897595693,-4.850788773436));
#39384=CARTESIAN_POINT('Ctrl Pts',(0.4493387631725,0.9539220152767,-4.901489047012));
#39385=CARTESIAN_POINT('Ctrl Pts',(0.9616578007037,0.4325353285362,-4.952189320588));
#39386=CARTESIAN_POINT('Ctrl Pts',(1.011848267068,-0.2967079715329,-5.002889594164));
#39387=CARTESIAN_POINT('Ctrl Pts',(0.5757909296073,-0.8833670479063,-5.05358986774));
#39388=CARTESIAN_POINT('Ctrl Pts',(-0.1369650830855,-1.045520493328,-5.104290141316));
#39389=CARTESIAN_POINT('Ctrl Pts',(-0.7839019675243,-0.7052448094529,-5.154990414892));
#39390=CARTESIAN_POINT('Ctrl Pts',(-1.054131570278,-0.02606086140956,-5.205690688468));
#39391=CARTESIAN_POINT('Ctrl Pts',(-0.8177939556507,0.6656467396795,-5.256390962044));
#39392=CARTESIAN_POINT('Ctrl Pts',(-0.1884621264991,1.037475090215,-5.30709123562));
#39393=CARTESIAN_POINT('Ctrl Pts',(0.5314359448635,0.9107405627254,-5.357791509196));
#39394=CARTESIAN_POINT('Ctrl Pts',(0.9959503090853,0.3463459501016,-5.408491782772));
#39395=CARTESIAN_POINT('Ctrl Pts',(0.9818566993762,-0.3844866181393,-5.459192056348));
#39396=CARTESIAN_POINT('Ctrl Pts',(0.4959278500411,-0.9305525792395,-5.509892329924));
#39397=CARTESIAN_POINT('Ctrl Pts',(-0.228321125274,-1.02943770117,-5.5605926035));
#39398=CARTESIAN_POINT('Ctrl Pts',(-0.8428495336144,-0.6336223787161,-5.611292877076));
#39399=CARTESIAN_POINT('Ctrl Pts',(-1.052342871644,0.06668288287484,-5.661993150652));
#39400=CARTESIAN_POINT('Ctrl Pts',(-0.7561296625306,0.7349429448028,-5.712693424228));
#39401=CARTESIAN_POINT('Ctrl Pts',(-0.09655114644213,1.050024932444,-5.763393697804));
#39402=CARTESIAN_POINT('Ctrl Pts',(0.6094100419002,0.860506634178,-5.81409397138));
#39403=CARTESIAN_POINT('Ctrl Pts',(1.022574131124,0.2574927403421,-5.864794244956));
#39404=CARTESIAN_POINT('Ctrl Pts',(0.9441219235678,-0.4693512901507,-5.915494518532));
#39405=CARTESIAN_POINT('Ctrl Pts',(0.5898854717729,-0.8033219032384,-5.949294700916));
#39406=CARTESIAN_POINT('Ctrl Pts',(0.3792106625816,-0.892804162952,-5.966194792108));
#39407=CARTESIAN_POINT('Ctrl Pts',(-0.8478876321751,0.4711545003548,-4.397145402435));
#39408=CARTESIAN_POINT('Ctrl Pts',(-0.7367094045404,0.6712303652943,-4.414045493627));
#39409=CARTESIAN_POINT('Ctrl Pts',(-0.3672795254541,0.9883130021961,-4.447845676011));
#39410=CARTESIAN_POINT('Ctrl Pts',(0.3637847024261,0.9897580791551,-4.498545949587));
#39411=CARTESIAN_POINT('Ctrl Pts',(0.9199177062286,0.5153675197374,-4.549246223163));
#39412=CARTESIAN_POINT('Ctrl Pts',(1.034010790836,-0.2066305085619,-4.599946496739));
#39413=CARTESIAN_POINT('Ctrl Pts',(0.6511976671912,-0.8293460055482,-4.650646770315));
#39414=CARTESIAN_POINT('Ctrl Pts',(-0.04454897242399,-1.053511991116,-4.701347043891));
#39415=CARTESIAN_POINT('Ctrl Pts',(-0.7188880044982,-0.771409548886,-4.752047317467));
#39416=CARTESIAN_POINT('Ctrl Pts',(-1.047762323398,-0.1186028267124,-4.802747591043));
#39417=CARTESIAN_POINT('Ctrl Pts',(-0.8731302342653,0.5911988913957,-4.853447864619));
#39418=CARTESIAN_POINT('Ctrl Pts',(-0.2789118454146,1.016897595693,-4.904148138195));
#39419=CARTESIAN_POINT('Ctrl Pts',(0.4493387631725,0.9539220152767,-4.954848411771));
#39420=CARTESIAN_POINT('Ctrl Pts',(0.9616578007037,0.4325353285362,-5.005548685347));
#39421=CARTESIAN_POINT('Ctrl Pts',(1.011848267068,-0.2967079715329,-5.056248958923));
#39422=CARTESIAN_POINT('Ctrl Pts',(0.5757909296073,-0.8833670479063,-5.106949232499));
#39423=CARTESIAN_POINT('Ctrl Pts',(-0.1369650830855,-1.045520493328,-5.157649506075));
#39424=CARTESIAN_POINT('Ctrl Pts',(-0.7839019675243,-0.7052448094529,-5.208349779651));
#39425=CARTESIAN_POINT('Ctrl Pts',(-1.054131570278,-0.02606086140956,-5.259050053227));
#39426=CARTESIAN_POINT('Ctrl Pts',(-0.8177939556507,0.6656467396795,-5.309750326803));
#39427=CARTESIAN_POINT('Ctrl Pts',(-0.1884621264991,1.037475090215,-5.360450600379));
#39428=CARTESIAN_POINT('Ctrl Pts',(0.5314359448635,0.9107405627254,-5.411150873955));
#39429=CARTESIAN_POINT('Ctrl Pts',(0.9959503090853,0.3463459501016,-5.461851147531));
#39430=CARTESIAN_POINT('Ctrl Pts',(0.9818566993762,-0.3844866181393,-5.512551421107));
#39431=CARTESIAN_POINT('Ctrl Pts',(0.4959278500411,-0.9305525792395,-5.563251694683));
#39432=CARTESIAN_POINT('Ctrl Pts',(-0.228321125274,-1.02943770117,-5.613951968259));
#39433=CARTESIAN_POINT('Ctrl Pts',(-0.8428495336144,-0.6336223787161,-5.664652241835));
#39434=CARTESIAN_POINT('Ctrl Pts',(-1.052342871644,0.06668288287484,-5.715352515411));
#39435=CARTESIAN_POINT('Ctrl Pts',(-0.7561296625306,0.7349429448028,-5.766052788987));
#39436=CARTESIAN_POINT('Ctrl Pts',(-0.09655114644213,1.050024932444,-5.816753062563));
#39437=CARTESIAN_POINT('Ctrl Pts',(0.6094100419002,0.860506634178,-5.867453336139));
#39438=CARTESIAN_POINT('Ctrl Pts',(1.022574131124,0.2574927403421,-5.918153609715));
#39439=CARTESIAN_POINT('Ctrl Pts',(0.9441219235678,-0.4693512901507,-5.968853883291));
#39440=CARTESIAN_POINT('Ctrl Pts',(0.5898854717729,-0.8033219032384,-6.002654065675));
#39441=CARTESIAN_POINT('Ctrl Pts',(0.3792106625816,-0.892804162952,-6.019554156867));
#39442=CARTESIAN_POINT('Ctrl Pts',(-0.8478876321751,0.4711545003548,-4.450504767195));
#39443=CARTESIAN_POINT('Ctrl Pts',(-0.7367094045404,0.6712303652943,-4.467404858387));
#39444=CARTESIAN_POINT('Ctrl Pts',(-0.3672795254541,0.9883130021961,-4.501205040771));
#39445=CARTESIAN_POINT('Ctrl Pts',(0.3637847024261,0.9897580791551,-4.551905314347));
#39446=CARTESIAN_POINT('Ctrl Pts',(0.9199177062286,0.5153675197374,-4.602605587923));
#39447=CARTESIAN_POINT('Ctrl Pts',(1.034010790836,-0.2066305085619,-4.653305861499));
#39448=CARTESIAN_POINT('Ctrl Pts',(0.6511976671912,-0.8293460055482,-4.704006135075));
#39449=CARTESIAN_POINT('Ctrl Pts',(-0.04454897242399,-1.053511991116,-4.754706408651));
#39450=CARTESIAN_POINT('Ctrl Pts',(-0.7188880044982,-0.771409548886,-4.805406682227));
#39451=CARTESIAN_POINT('Ctrl Pts',(-1.047762323398,-0.1186028267124,-4.856106955803));
#39452=CARTESIAN_POINT('Ctrl Pts',(-0.8731302342653,0.5911988913957,-4.906807229379));
#39453=CARTESIAN_POINT('Ctrl Pts',(-0.2789118454146,1.016897595693,-4.957507502955));
#39454=CARTESIAN_POINT('Ctrl Pts',(0.4493387631725,0.9539220152767,-5.008207776531));
#39455=CARTESIAN_POINT('Ctrl Pts',(0.9616578007037,0.4325353285362,-5.058908050107));
#39456=CARTESIAN_POINT('Ctrl Pts',(1.011848267068,-0.2967079715329,-5.109608323683));
#39457=CARTESIAN_POINT('Ctrl Pts',(0.5757909296073,-0.8833670479063,-5.160308597259));
#39458=CARTESIAN_POINT('Ctrl Pts',(-0.1369650830855,-1.045520493328,-5.211008870835));
#39459=CARTESIAN_POINT('Ctrl Pts',(-0.7839019675243,-0.7052448094529,-5.261709144411));
#39460=CARTESIAN_POINT('Ctrl Pts',(-1.054131570278,-0.02606086140956,-5.312409417987));
#39461=CARTESIAN_POINT('Ctrl Pts',(-0.8177939556507,0.6656467396795,-5.363109691563));
#39462=CARTESIAN_POINT('Ctrl Pts',(-0.1884621264991,1.037475090215,-5.413809965139));
#39463=CARTESIAN_POINT('Ctrl Pts',(0.5314359448635,0.9107405627254,-5.464510238715));
#39464=CARTESIAN_POINT('Ctrl Pts',(0.9959503090853,0.3463459501016,-5.515210512291));
#39465=CARTESIAN_POINT('Ctrl Pts',(0.9818566993762,-0.3844866181393,-5.565910785867));
#39466=CARTESIAN_POINT('Ctrl Pts',(0.4959278500411,-0.9305525792395,-5.616611059443));
#39467=CARTESIAN_POINT('Ctrl Pts',(-0.228321125274,-1.02943770117,-5.667311333019));
#39468=CARTESIAN_POINT('Ctrl Pts',(-0.8428495336144,-0.6336223787161,-5.718011606595));
#39469=CARTESIAN_POINT('Ctrl Pts',(-1.052342871644,0.06668288287484,-5.768711880171));
#39470=CARTESIAN_POINT('Ctrl Pts',(-0.7561296625306,0.7349429448028,-5.819412153747));
#39471=CARTESIAN_POINT('Ctrl Pts',(-0.09655114644213,1.050024932444,-5.870112427323));
#39472=CARTESIAN_POINT('Ctrl Pts',(0.6094100419002,0.860506634178,-5.920812700899));
#39473=CARTESIAN_POINT('Ctrl Pts',(1.022574131124,0.2574927403421,-5.971512974475));
#39474=CARTESIAN_POINT('Ctrl Pts',(0.9441219235678,-0.4693512901507,-6.022213248051));
#39475=CARTESIAN_POINT('Ctrl Pts',(0.5898854717729,-0.8033219032384,-6.056013430435));
#39476=CARTESIAN_POINT('Ctrl Pts',(0.3792106625816,-0.892804162952,-6.072913521627));
#39477=CARTESIAN_POINT('Ctrl Pts',(-0.8478876321751,0.4711545003548,-4.503864131954));
#39478=CARTESIAN_POINT('Ctrl Pts',(-0.7367094045404,0.6712303652943,-4.520764223146));
#39479=CARTESIAN_POINT('Ctrl Pts',(-0.3672795254541,0.9883130021961,-4.55456440553));
#39480=CARTESIAN_POINT('Ctrl Pts',(0.3637847024261,0.9897580791551,-4.605264679106));
#39481=CARTESIAN_POINT('Ctrl Pts',(0.9199177062286,0.5153675197374,-4.655964952682));
#39482=CARTESIAN_POINT('Ctrl Pts',(1.034010790836,-0.2066305085619,-4.706665226258));
#39483=CARTESIAN_POINT('Ctrl Pts',(0.6511976671912,-0.8293460055482,-4.757365499834));
#39484=CARTESIAN_POINT('Ctrl Pts',(-0.04454897242399,-1.053511991116,-4.80806577341));
#39485=CARTESIAN_POINT('Ctrl Pts',(-0.7188880044982,-0.771409548886,-4.858766046986));
#39486=CARTESIAN_POINT('Ctrl Pts',(-1.047762323398,-0.1186028267124,-4.909466320562));
#39487=CARTESIAN_POINT('Ctrl Pts',(-0.8731302342653,0.5911988913957,-4.960166594138));
#39488=CARTESIAN_POINT('Ctrl Pts',(-0.2789118454146,1.016897595693,-5.010866867714));
#39489=CARTESIAN_POINT('Ctrl Pts',(0.4493387631725,0.9539220152767,-5.06156714129));
#39490=CARTESIAN_POINT('Ctrl Pts',(0.9616578007037,0.4325353285362,-5.112267414866));
#39491=CARTESIAN_POINT('Ctrl Pts',(1.011848267068,-0.2967079715329,-5.162967688442));
#39492=CARTESIAN_POINT('Ctrl Pts',(0.5757909296073,-0.8833670479063,-5.213667962018));
#39493=CARTESIAN_POINT('Ctrl Pts',(-0.1369650830855,-1.045520493328,-5.264368235594));
#39494=CARTESIAN_POINT('Ctrl Pts',(-0.7839019675243,-0.7052448094529,-5.31506850917));
#39495=CARTESIAN_POINT('Ctrl Pts',(-1.054131570278,-0.02606086140956,-5.365768782746));
#39496=CARTESIAN_POINT('Ctrl Pts',(-0.8177939556507,0.6656467396795,-5.416469056322));
#39497=CARTESIAN_POINT('Ctrl Pts',(-0.1884621264991,1.037475090215,-5.467169329898));
#39498=CARTESIAN_POINT('Ctrl Pts',(0.5314359448635,0.9107405627254,-5.517869603474));
#39499=CARTESIAN_POINT('Ctrl Pts',(0.9959503090853,0.3463459501016,-5.56856987705));
#39500=CARTESIAN_POINT('Ctrl Pts',(0.9818566993762,-0.3844866181393,-5.619270150626));
#39501=CARTESIAN_POINT('Ctrl Pts',(0.4959278500411,-0.9305525792395,-5.669970424202));
#39502=CARTESIAN_POINT('Ctrl Pts',(-0.228321125274,-1.02943770117,-5.720670697778));
#39503=CARTESIAN_POINT('Ctrl Pts',(-0.8428495336144,-0.6336223787161,-5.771370971354));
#39504=CARTESIAN_POINT('Ctrl Pts',(-1.052342871644,0.06668288287484,-5.82207124493));
#39505=CARTESIAN_POINT('Ctrl Pts',(-0.7561296625306,0.7349429448028,-5.872771518506));
#39506=CARTESIAN_POINT('Ctrl Pts',(-0.09655114644213,1.050024932444,-5.923471792082));
#39507=CARTESIAN_POINT('Ctrl Pts',(0.6094100419002,0.860506634178,-5.974172065658));
#39508=CARTESIAN_POINT('Ctrl Pts',(1.022574131124,0.2574927403421,-6.024872339234));
#39509=CARTESIAN_POINT('Ctrl Pts',(0.9441219235678,-0.4693512901507,-6.07557261281));
#39510=CARTESIAN_POINT('Ctrl Pts',(0.5898854717729,-0.8033219032384,-6.109372795194));
#39511=CARTESIAN_POINT('Ctrl Pts',(0.3792106625816,-0.892804162952,-6.126272886386));
#39512=CARTESIAN_POINT('',(0.7205452572168,-0.6493955129983,-5.951691746266));
#39513=CARTESIAN_POINT('Ctrl Pts',(0.9272843286311,-0.2846818818877,-5.903794455399));
#39514=CARTESIAN_POINT('Ctrl Pts',(0.8601080052719,-0.5034929684698,-5.920694546591));
#39515=CARTESIAN_POINT('Ctrl Pts',(0.5646307635317,-0.8904206539615,-5.954494728975));
#39516=CARTESIAN_POINT('Ctrl Pts',(-0.1501755344832,-1.043746939548,-6.005195002551));
#39517=CARTESIAN_POINT('Ctrl Pts',(-0.7927460883193,-0.6952739791533,-6.055895276127));
#39518=CARTESIAN_POINT('Ctrl Pts',(-1.054377577714,-0.01274387096732,-6.106595549703));
#39519=CARTESIAN_POINT('Ctrl Pts',(-0.8093187275974,0.6759263242647,-6.157295823279));
#39520=CARTESIAN_POINT('Ctrl Pts',(-0.1753397818274,1.03977309413,-6.207996096855));
#39521=CARTESIAN_POINT('Ctrl Pts',(0.542899761859,0.903953817237,-6.258696370431));
#39522=CARTESIAN_POINT('Ctrl Pts',(1.000246520579,0.3337355463655,-6.309396644007));
#39523=CARTESIAN_POINT('Ctrl Pts',(0.9769207671901,-0.3968606176082,-6.360096917583));
#39524=CARTESIAN_POINT('Ctrl Pts',(0.4841317554003,-0.9367438182615,-6.410797191159));
#39525=CARTESIAN_POINT('Ctrl Pts',(-0.2413087404899,-1.026470957739,-6.461497464735));
#39526=CARTESIAN_POINT('Ctrl Pts',(-0.8507873392775,-0.6229233013874,-6.512197738311));
#39527=CARTESIAN_POINT('Ctrl Pts',(-1.051416618566,0.07997268373542,-6.562898011887));
#39528=CARTESIAN_POINT('Ctrl Pts',(-0.7467833616144,0.7444374700139,-6.613598285463));
#39529=CARTESIAN_POINT('Ctrl Pts',(-0.08328032014135,1.051159799569,-6.664298559039));
#39530=CARTESIAN_POINT('Ctrl Pts',(0.6202434181993,0.8527430082558,-6.714998832615));
#39531=CARTESIAN_POINT('Ctrl Pts',(1.025706656971,0.2445370928879,-6.765699106191));
#39532=CARTESIAN_POINT('Ctrl Pts',(0.9382623861687,-0.4811821179614,-6.816399379767));
#39533=CARTESIAN_POINT('Ctrl Pts',(0.3999323061365,-0.9756673031565,-6.867099653343));
#39534=CARTESIAN_POINT('Ctrl Pts',(-0.3305868717956,-1.001291594034,-6.917799926919));
#39535=CARTESIAN_POINT('Ctrl Pts',(-0.9022411823332,-0.545741132975,-6.968500200495));
#39536=CARTESIAN_POINT('Ctrl Pts',(-1.040319821114,0.172067450248,-7.019200474071));
#39537=CARTESIAN_POINT('Ctrl Pts',(-0.6784685297463,0.8071883233295,-7.069900747647));
#39538=CARTESIAN_POINT('Ctrl Pts',(0.009423556678434,1.054411548408,-7.120601021223));
#39539=CARTESIAN_POINT('Ctrl Pts',(0.6927871851051,0.7949330608788,-7.171301294799));
#39540=CARTESIAN_POINT('Ctrl Pts',(1.043228848248,0.1534460705006,-7.222001568375));
#39541=CARTESIAN_POINT('Ctrl Pts',(0.8923436237759,-0.5617793657482,-7.272701841951));
#39542=CARTESIAN_POINT('Ctrl Pts',(0.3126353722454,-1.007042008386,-7.323402115527));
#39543=CARTESIAN_POINT('Ctrl Pts',(-0.4172973984221,-0.9683569320779,-7.374102389103));
#39544=CARTESIAN_POINT('Ctrl Pts',(-0.9467472663198,-0.4643597513654,-7.424802662679));
#39545=CARTESIAN_POINT('Ctrl Pts',(-1.021043319681,0.2629208615952,-7.475502936255));
#39546=CARTESIAN_POINT('Ctrl Pts',(-0.7439371296958,0.6632107486247,-7.509303118639));
#39547=CARTESIAN_POINT('Ctrl Pts',(-0.5564550442372,0.7945173275284,-7.526203209831));
#39548=CARTESIAN_POINT('Ctrl Pts',(0.9272843286311,-0.2846818818877,-5.957153820158));
#39549=CARTESIAN_POINT('Ctrl Pts',(0.8601080052719,-0.5034929684698,-5.97405391135));
#39550=CARTESIAN_POINT('Ctrl Pts',(0.5646307635317,-0.8904206539615,-6.007854093734));
#39551=CARTESIAN_POINT('Ctrl Pts',(-0.1501755344832,-1.043746939548,-6.05855436731));
#39552=CARTESIAN_POINT('Ctrl Pts',(-0.7927460883193,-0.6952739791533,-6.109254640886));
#39553=CARTESIAN_POINT('Ctrl Pts',(-1.054377577714,-0.01274387096732,-6.159954914462));
#39554=CARTESIAN_POINT('Ctrl Pts',(-0.8093187275974,0.6759263242647,-6.210655188038));
#39555=CARTESIAN_POINT('Ctrl Pts',(-0.1753397818274,1.03977309413,-6.261355461614));
#39556=CARTESIAN_POINT('Ctrl Pts',(0.542899761859,0.903953817237,-6.31205573519));
#39557=CARTESIAN_POINT('Ctrl Pts',(1.000246520579,0.3337355463655,-6.362756008766));
#39558=CARTESIAN_POINT('Ctrl Pts',(0.9769207671901,-0.3968606176082,-6.413456282342));
#39559=CARTESIAN_POINT('Ctrl Pts',(0.4841317554003,-0.9367438182615,-6.464156555918));
#39560=CARTESIAN_POINT('Ctrl Pts',(-0.2413087404899,-1.026470957739,-6.514856829494));
#39561=CARTESIAN_POINT('Ctrl Pts',(-0.8507873392775,-0.6229233013874,-6.56555710307));
#39562=CARTESIAN_POINT('Ctrl Pts',(-1.051416618566,0.07997268373542,-6.616257376646));
#39563=CARTESIAN_POINT('Ctrl Pts',(-0.7467833616144,0.7444374700139,-6.666957650222));
#39564=CARTESIAN_POINT('Ctrl Pts',(-0.08328032014135,1.051159799569,-6.717657923798));
#39565=CARTESIAN_POINT('Ctrl Pts',(0.6202434181993,0.8527430082558,-6.768358197374));
#39566=CARTESIAN_POINT('Ctrl Pts',(1.025706656971,0.2445370928879,-6.81905847095));
#39567=CARTESIAN_POINT('Ctrl Pts',(0.9382623861687,-0.4811821179614,-6.869758744526));
#39568=CARTESIAN_POINT('Ctrl Pts',(0.3999323061365,-0.9756673031565,-6.920459018102));
#39569=CARTESIAN_POINT('Ctrl Pts',(-0.3305868717956,-1.001291594034,-6.971159291678));
#39570=CARTESIAN_POINT('Ctrl Pts',(-0.9022411823332,-0.545741132975,-7.021859565254));
#39571=CARTESIAN_POINT('Ctrl Pts',(-1.040319821114,0.172067450248,-7.07255983883));
#39572=CARTESIAN_POINT('Ctrl Pts',(-0.6784685297463,0.8071883233295,-7.123260112406));
#39573=CARTESIAN_POINT('Ctrl Pts',(0.009423556678434,1.054411548408,-7.173960385982));
#39574=CARTESIAN_POINT('Ctrl Pts',(0.6927871851051,0.7949330608788,-7.224660659558));
#39575=CARTESIAN_POINT('Ctrl Pts',(1.043228848248,0.1534460705006,-7.275360933134));
#39576=CARTESIAN_POINT('Ctrl Pts',(0.8923436237759,-0.5617793657482,-7.32606120671));
#39577=CARTESIAN_POINT('Ctrl Pts',(0.3126353722454,-1.007042008386,-7.376761480286));
#39578=CARTESIAN_POINT('Ctrl Pts',(-0.4172973984221,-0.9683569320779,-7.427461753862));
#39579=CARTESIAN_POINT('Ctrl Pts',(-0.9467472663198,-0.4643597513654,-7.478162027438));
#39580=CARTESIAN_POINT('Ctrl Pts',(-1.021043319681,0.2629208615952,-7.528862301014));
#39581=CARTESIAN_POINT('Ctrl Pts',(-0.7439371296958,0.6632107486247,-7.562662483398));
#39582=CARTESIAN_POINT('Ctrl Pts',(-0.5564550442372,0.7945173275284,-7.57956257459));
#39583=CARTESIAN_POINT('Ctrl Pts',(0.9272843286311,-0.2846818818877,-6.010513184918));
#39584=CARTESIAN_POINT('Ctrl Pts',(0.8601080052719,-0.5034929684698,-6.02741327611));
#39585=CARTESIAN_POINT('Ctrl Pts',(0.5646307635317,-0.8904206539615,-6.061213458494));
#39586=CARTESIAN_POINT('Ctrl Pts',(-0.1501755344832,-1.043746939548,-6.11191373207));
#39587=CARTESIAN_POINT('Ctrl Pts',(-0.7927460883193,-0.6952739791533,-6.162614005646));
#39588=CARTESIAN_POINT('Ctrl Pts',(-1.054377577714,-0.01274387096732,-6.213314279222));
#39589=CARTESIAN_POINT('Ctrl Pts',(-0.8093187275974,0.6759263242647,-6.264014552798));
#39590=CARTESIAN_POINT('Ctrl Pts',(-0.1753397818274,1.03977309413,-6.314714826374));
#39591=CARTESIAN_POINT('Ctrl Pts',(0.542899761859,0.903953817237,-6.36541509995));
#39592=CARTESIAN_POINT('Ctrl Pts',(1.000246520579,0.3337355463655,-6.416115373526));
#39593=CARTESIAN_POINT('Ctrl Pts',(0.9769207671901,-0.3968606176082,-6.466815647102));
#39594=CARTESIAN_POINT('Ctrl Pts',(0.4841317554003,-0.9367438182615,-6.517515920678));
#39595=CARTESIAN_POINT('Ctrl Pts',(-0.2413087404899,-1.026470957739,-6.568216194254));
#39596=CARTESIAN_POINT('Ctrl Pts',(-0.8507873392775,-0.6229233013874,-6.61891646783));
#39597=CARTESIAN_POINT('Ctrl Pts',(-1.051416618566,0.07997268373542,-6.669616741406));
#39598=CARTESIAN_POINT('Ctrl Pts',(-0.7467833616144,0.7444374700139,-6.720317014982));
#39599=CARTESIAN_POINT('Ctrl Pts',(-0.08328032014135,1.051159799569,-6.771017288558));
#39600=CARTESIAN_POINT('Ctrl Pts',(0.6202434181993,0.8527430082558,-6.821717562134));
#39601=CARTESIAN_POINT('Ctrl Pts',(1.025706656971,0.2445370928879,-6.87241783571));
#39602=CARTESIAN_POINT('Ctrl Pts',(0.9382623861687,-0.4811821179614,-6.923118109286));
#39603=CARTESIAN_POINT('Ctrl Pts',(0.3999323061365,-0.9756673031565,-6.973818382862));
#39604=CARTESIAN_POINT('Ctrl Pts',(-0.3305868717956,-1.001291594034,-7.024518656438));
#39605=CARTESIAN_POINT('Ctrl Pts',(-0.9022411823332,-0.545741132975,-7.075218930014));
#39606=CARTESIAN_POINT('Ctrl Pts',(-1.040319821114,0.172067450248,-7.12591920359));
#39607=CARTESIAN_POINT('Ctrl Pts',(-0.6784685297463,0.8071883233295,-7.176619477166));
#39608=CARTESIAN_POINT('Ctrl Pts',(0.009423556678434,1.054411548408,-7.227319750742));
#39609=CARTESIAN_POINT('Ctrl Pts',(0.6927871851051,0.7949330608788,-7.278020024318));
#39610=CARTESIAN_POINT('Ctrl Pts',(1.043228848248,0.1534460705006,-7.328720297894));
#39611=CARTESIAN_POINT('Ctrl Pts',(0.8923436237759,-0.5617793657482,-7.37942057147));
#39612=CARTESIAN_POINT('Ctrl Pts',(0.3126353722454,-1.007042008386,-7.430120845046));
#39613=CARTESIAN_POINT('Ctrl Pts',(-0.4172973984221,-0.9683569320779,-7.480821118622));
#39614=CARTESIAN_POINT('Ctrl Pts',(-0.9467472663198,-0.4643597513654,-7.531521392198));
#39615=CARTESIAN_POINT('Ctrl Pts',(-1.021043319681,0.2629208615952,-7.582221665774));
#39616=CARTESIAN_POINT('Ctrl Pts',(-0.7439371296958,0.6632107486247,-7.616021848158));
#39617=CARTESIAN_POINT('Ctrl Pts',(-0.5564550442372,0.7945173275284,-7.63292193935));
#39618=CARTESIAN_POINT('Ctrl Pts',(0.9272843286311,-0.2846818818877,-6.063872549677));
#39619=CARTESIAN_POINT('Ctrl Pts',(0.8601080052719,-0.5034929684698,-6.080772640869));
#39620=CARTESIAN_POINT('Ctrl Pts',(0.5646307635317,-0.8904206539615,-6.114572823253));
#39621=CARTESIAN_POINT('Ctrl Pts',(-0.1501755344832,-1.043746939548,-6.165273096829));
#39622=CARTESIAN_POINT('Ctrl Pts',(-0.7927460883193,-0.6952739791533,-6.215973370405));
#39623=CARTESIAN_POINT('Ctrl Pts',(-1.054377577714,-0.01274387096732,-6.266673643981));
#39624=CARTESIAN_POINT('Ctrl Pts',(-0.8093187275974,0.6759263242647,-6.317373917557));
#39625=CARTESIAN_POINT('Ctrl Pts',(-0.1753397818274,1.03977309413,-6.368074191133));
#39626=CARTESIAN_POINT('Ctrl Pts',(0.542899761859,0.903953817237,-6.418774464709));
#39627=CARTESIAN_POINT('Ctrl Pts',(1.000246520579,0.3337355463655,-6.469474738285));
#39628=CARTESIAN_POINT('Ctrl Pts',(0.9769207671901,-0.3968606176082,-6.520175011861));
#39629=CARTESIAN_POINT('Ctrl Pts',(0.4841317554003,-0.9367438182615,-6.570875285437));
#39630=CARTESIAN_POINT('Ctrl Pts',(-0.2413087404899,-1.026470957739,-6.621575559013));
#39631=CARTESIAN_POINT('Ctrl Pts',(-0.8507873392775,-0.6229233013874,-6.672275832589));
#39632=CARTESIAN_POINT('Ctrl Pts',(-1.051416618566,0.07997268373542,-6.722976106165));
#39633=CARTESIAN_POINT('Ctrl Pts',(-0.7467833616144,0.7444374700139,-6.773676379741));
#39634=CARTESIAN_POINT('Ctrl Pts',(-0.08328032014135,1.051159799569,-6.824376653317));
#39635=CARTESIAN_POINT('Ctrl Pts',(0.6202434181993,0.8527430082558,-6.875076926893));
#39636=CARTESIAN_POINT('Ctrl Pts',(1.025706656971,0.2445370928879,-6.925777200469));
#39637=CARTESIAN_POINT('Ctrl Pts',(0.9382623861687,-0.4811821179614,-6.976477474045));
#39638=CARTESIAN_POINT('Ctrl Pts',(0.3999323061365,-0.9756673031565,-7.027177747621));
#39639=CARTESIAN_POINT('Ctrl Pts',(-0.3305868717956,-1.001291594034,-7.077878021197));
#39640=CARTESIAN_POINT('Ctrl Pts',(-0.9022411823332,-0.545741132975,-7.128578294773));
#39641=CARTESIAN_POINT('Ctrl Pts',(-1.040319821114,0.172067450248,-7.179278568349));
#39642=CARTESIAN_POINT('Ctrl Pts',(-0.6784685297463,0.8071883233295,-7.229978841925));
#39643=CARTESIAN_POINT('Ctrl Pts',(0.009423556678434,1.054411548408,-7.280679115501));
#39644=CARTESIAN_POINT('Ctrl Pts',(0.6927871851051,0.7949330608788,-7.331379389077));
#39645=CARTESIAN_POINT('Ctrl Pts',(1.043228848248,0.1534460705006,-7.382079662653));
#39646=CARTESIAN_POINT('Ctrl Pts',(0.8923436237759,-0.5617793657482,-7.432779936229));
#39647=CARTESIAN_POINT('Ctrl Pts',(0.3126353722454,-1.007042008386,-7.483480209805));
#39648=CARTESIAN_POINT('Ctrl Pts',(-0.4172973984221,-0.9683569320779,-7.534180483381));
#39649=CARTESIAN_POINT('Ctrl Pts',(-0.9467472663198,-0.4643597513654,-7.584880756957));
#39650=CARTESIAN_POINT('Ctrl Pts',(-1.021043319681,0.2629208615952,-7.635581030533));
#39651=CARTESIAN_POINT('Ctrl Pts',(-0.7439371296958,0.6632107486247,-7.669381212917));
#39652=CARTESIAN_POINT('Ctrl Pts',(-0.5564550442372,0.7945173275284,-7.686281304109));
#39653=CARTESIAN_POINT('',(-0.8397594776816,0.485493583525,-7.511700163989));
#39654=CARTESIAN_POINT('Ctrl Pts',(-0.9661995571575,0.08578120859872,-7.463802873122));
#39655=CARTESIAN_POINT('Ctrl Pts',(-0.9459577835372,0.313775113412,-7.480702964314));
#39656=CARTESIAN_POINT('Ctrl Pts',(-0.7373325155345,0.7536561561237,-7.514503146698));
#39657=CARTESIAN_POINT('Ctrl Pts',(-0.06998968740697,1.052170047392,-7.565203420274));
#39658=CARTESIAN_POINT('Ctrl Pts',(0.6309663956697,0.8448276002645,-7.61590369385));
#39659=CARTESIAN_POINT('Ctrl Pts',(1.028714521555,0.2315619048451,-7.666603967426));
#39660=CARTESIAN_POINT('Ctrl Pts',(0.932108219137,-0.4929984447149,-7.717304241002));
#39661=CARTESIAN_POINT('Ctrl Pts',(0.3875739132888,-0.9806419265493,-7.768004514578));
#39662=CARTESIAN_POINT('Ctrl Pts',(-0.3432107204247,-0.9970351330367,-7.818704788154));
#39663=CARTESIAN_POINT('Ctrl Pts',(-0.9090640168405,-0.5342987274206,-7.86940506173));
#39664=CARTESIAN_POINT('Ctrl Pts',(-1.03806290686,0.1851970209741,-7.920105335306));
#39665=CARTESIAN_POINT('Ctrl Pts',(-0.668216439086,0.81569561,-7.970805608882));
#39666=CARTESIAN_POINT('Ctrl Pts',(0.02274415819314,1.054208346859,-8.021505882458));
#39667=CARTESIAN_POINT('Ctrl Pts',(0.7027749578096,0.7861169726968,-8.072206156034));
#39668=CARTESIAN_POINT('Ctrl Pts',(1.045084390477,0.1402538866513,-8.12290642961));
#39669=CARTESIAN_POINT('Ctrl Pts',(0.8851742648668,-0.573008775467,-8.173606703186));
#39670=CARTESIAN_POINT('Ctrl Pts',(0.2998900428063,-1.010909737899,-8.224306976762));
#39671=CARTESIAN_POINT('Ctrl Pts',(-0.4295075601491,-0.9630139104517,-8.275007250338));
#39672=CARTESIAN_POINT('Ctrl Pts',(-0.9525035565898,-0.4523378279972,-8.325707523914));
#39673=CARTESIAN_POINT('Ctrl Pts',(-1.017770091349,0.275711039135,-8.37640779749));
#39674=CARTESIAN_POINT('Ctrl Pts',(-0.5939430654806,0.8712658439924,-8.427108071066));
#39675=CARTESIAN_POINT('Ctrl Pts',(0.1153057184743,1.048130300761,-8.477808344642));
#39676=CARTESIAN_POINT('Ctrl Pts',(0.7691438697144,0.7213114743296,-8.528508618218));
#39677=CARTESIAN_POINT('Ctrl Pts',(1.053366804377,0.0478634837261,-8.579208891794));
#39678=CARTESIAN_POINT('Ctrl Pts',(0.8313900288183,-0.6485855033511,-8.62990916537));
#39679=CARTESIAN_POINT('Ctrl Pts',(0.2098854061311,-1.033354069586,-8.680609438946));
#39680=CARTESIAN_POINT('Ctrl Pts',(-0.5124805616198,-0.9215401939611,-8.731309712522));
#39681=CARTESIAN_POINT('Ctrl Pts',(-0.9885716900656,-0.3668761916084,-8.782009986098));
#39682=CARTESIAN_POINT('Ctrl Pts',(-0.9896014863655,0.364090781066,-8.832710259674));
#39683=CARTESIAN_POINT('Ctrl Pts',(-0.5150712073616,0.9200957200099,-8.88341053325));
#39684=CARTESIAN_POINT('Ctrl Pts',(0.2069672452441,1.033932698984,-8.934110806826));
#39685=CARTESIAN_POINT('Ctrl Pts',(0.8295892607691,0.6509547014876,-8.984811080402));
#39686=CARTESIAN_POINT('Ctrl Pts',(1.053390111087,-0.04501237598842,-9.035511353978));
#39687=CARTESIAN_POINT('Ctrl Pts',(0.8655115137905,-0.494146506137,-9.069311536362));
#39688=CARTESIAN_POINT('Ctrl Pts',(0.7094068585195,-0.6615450922541,-9.086211627554));
#39689=CARTESIAN_POINT('Ctrl Pts',(-0.9661995571575,0.08578120859872,-7.517162237882));
#39690=CARTESIAN_POINT('Ctrl Pts',(-0.9459577835372,0.313775113412,-7.534062329074));
#39691=CARTESIAN_POINT('Ctrl Pts',(-0.7373325155345,0.7536561561237,-7.567862511458));
#39692=CARTESIAN_POINT('Ctrl Pts',(-0.06998968740697,1.052170047392,-7.618562785034));
#39693=CARTESIAN_POINT('Ctrl Pts',(0.6309663956697,0.8448276002645,-7.66926305861));
#39694=CARTESIAN_POINT('Ctrl Pts',(1.028714521555,0.2315619048451,-7.719963332186));
#39695=CARTESIAN_POINT('Ctrl Pts',(0.932108219137,-0.4929984447149,-7.770663605762));
#39696=CARTESIAN_POINT('Ctrl Pts',(0.3875739132888,-0.9806419265493,-7.821363879338));
#39697=CARTESIAN_POINT('Ctrl Pts',(-0.3432107204247,-0.9970351330367,-7.872064152914));
#39698=CARTESIAN_POINT('Ctrl Pts',(-0.9090640168405,-0.5342987274206,-7.92276442649));
#39699=CARTESIAN_POINT('Ctrl Pts',(-1.03806290686,0.1851970209741,-7.973464700066));
#39700=CARTESIAN_POINT('Ctrl Pts',(-0.668216439086,0.81569561,-8.024164973642));
#39701=CARTESIAN_POINT('Ctrl Pts',(0.02274415819314,1.054208346859,-8.074865247218));
#39702=CARTESIAN_POINT('Ctrl Pts',(0.7027749578096,0.7861169726968,-8.125565520794));
#39703=CARTESIAN_POINT('Ctrl Pts',(1.045084390477,0.1402538866513,-8.17626579437));
#39704=CARTESIAN_POINT('Ctrl Pts',(0.8851742648668,-0.573008775467,-8.226966067946));
#39705=CARTESIAN_POINT('Ctrl Pts',(0.2998900428063,-1.010909737899,-8.277666341522));
#39706=CARTESIAN_POINT('Ctrl Pts',(-0.4295075601491,-0.9630139104517,-8.328366615098));
#39707=CARTESIAN_POINT('Ctrl Pts',(-0.9525035565898,-0.4523378279972,-8.379066888674));
#39708=CARTESIAN_POINT('Ctrl Pts',(-1.017770091349,0.275711039135,-8.42976716225));
#39709=CARTESIAN_POINT('Ctrl Pts',(-0.5939430654806,0.8712658439924,-8.480467435826));
#39710=CARTESIAN_POINT('Ctrl Pts',(0.1153057184743,1.048130300761,-8.531167709402));
#39711=CARTESIAN_POINT('Ctrl Pts',(0.7691438697144,0.7213114743296,-8.581867982978));
#39712=CARTESIAN_POINT('Ctrl Pts',(1.053366804377,0.0478634837261,-8.632568256554));
#39713=CARTESIAN_POINT('Ctrl Pts',(0.8313900288183,-0.6485855033511,-8.68326853013));
#39714=CARTESIAN_POINT('Ctrl Pts',(0.2098854061311,-1.033354069586,-8.733968803706));
#39715=CARTESIAN_POINT('Ctrl Pts',(-0.5124805616198,-0.9215401939611,-8.784669077282));
#39716=CARTESIAN_POINT('Ctrl Pts',(-0.9885716900656,-0.3668761916084,-8.835369350858));
#39717=CARTESIAN_POINT('Ctrl Pts',(-0.9896014863655,0.364090781066,-8.886069624434));
#39718=CARTESIAN_POINT('Ctrl Pts',(-0.5150712073616,0.9200957200099,-8.93676989801));
#39719=CARTESIAN_POINT('Ctrl Pts',(0.2069672452441,1.033932698984,-8.987470171586));
#39720=CARTESIAN_POINT('Ctrl Pts',(0.8295892607691,0.6509547014876,-9.038170445162));
#39721=CARTESIAN_POINT('Ctrl Pts',(1.053390111087,-0.04501237598842,-9.088870718738));
#39722=CARTESIAN_POINT('Ctrl Pts',(0.8655115137905,-0.494146506137,-9.122670901122));
#39723=CARTESIAN_POINT('Ctrl Pts',(0.7094068585195,-0.6615450922541,-9.139570992314));
#39724=CARTESIAN_POINT('Ctrl Pts',(-0.9661995571575,0.08578120859872,-7.570521602641));
#39725=CARTESIAN_POINT('Ctrl Pts',(-0.9459577835372,0.313775113412,-7.587421693833));
#39726=CARTESIAN_POINT('Ctrl Pts',(-0.7373325155345,0.7536561561237,-7.621221876217));
#39727=CARTESIAN_POINT('Ctrl Pts',(-0.06998968740697,1.052170047392,-7.671922149793));
#39728=CARTESIAN_POINT('Ctrl Pts',(0.6309663956697,0.8448276002645,-7.722622423369));
#39729=CARTESIAN_POINT('Ctrl Pts',(1.028714521555,0.2315619048451,-7.773322696945));
#39730=CARTESIAN_POINT('Ctrl Pts',(0.932108219137,-0.4929984447149,-7.824022970521));
#39731=CARTESIAN_POINT('Ctrl Pts',(0.3875739132888,-0.9806419265493,-7.874723244097));
#39732=CARTESIAN_POINT('Ctrl Pts',(-0.3432107204247,-0.9970351330367,-7.925423517673));
#39733=CARTESIAN_POINT('Ctrl Pts',(-0.9090640168405,-0.5342987274206,-7.976123791249));
#39734=CARTESIAN_POINT('Ctrl Pts',(-1.03806290686,0.1851970209741,-8.026824064825));
#39735=CARTESIAN_POINT('Ctrl Pts',(-0.668216439086,0.81569561,-8.077524338401));
#39736=CARTESIAN_POINT('Ctrl Pts',(0.02274415819314,1.054208346859,-8.128224611977));
#39737=CARTESIAN_POINT('Ctrl Pts',(0.7027749578096,0.7861169726968,-8.178924885553));
#39738=CARTESIAN_POINT('Ctrl Pts',(1.045084390477,0.1402538866513,-8.229625159129));
#39739=CARTESIAN_POINT('Ctrl Pts',(0.8851742648668,-0.573008775467,-8.280325432705));
#39740=CARTESIAN_POINT('Ctrl Pts',(0.2998900428063,-1.010909737899,-8.331025706281));
#39741=CARTESIAN_POINT('Ctrl Pts',(-0.4295075601491,-0.9630139104517,-8.381725979857));
#39742=CARTESIAN_POINT('Ctrl Pts',(-0.9525035565898,-0.4523378279972,-8.432426253433));
#39743=CARTESIAN_POINT('Ctrl Pts',(-1.017770091349,0.275711039135,-8.483126527009));
#39744=CARTESIAN_POINT('Ctrl Pts',(-0.5939430654806,0.8712658439924,-8.533826800585));
#39745=CARTESIAN_POINT('Ctrl Pts',(0.1153057184743,1.048130300761,-8.584527074161));
#39746=CARTESIAN_POINT('Ctrl Pts',(0.7691438697144,0.7213114743296,-8.635227347737));
#39747=CARTESIAN_POINT('Ctrl Pts',(1.053366804377,0.0478634837261,-8.685927621313));
#39748=CARTESIAN_POINT('Ctrl Pts',(0.8313900288183,-0.6485855033511,-8.736627894889));
#39749=CARTESIAN_POINT('Ctrl Pts',(0.2098854061311,-1.033354069586,-8.787328168465));
#39750=CARTESIAN_POINT('Ctrl Pts',(-0.5124805616198,-0.9215401939611,-8.838028442041));
#39751=CARTESIAN_POINT('Ctrl Pts',(-0.9885716900656,-0.3668761916084,-8.888728715617));
#39752=CARTESIAN_POINT('Ctrl Pts',(-0.9896014863655,0.364090781066,-8.939428989193));
#39753=CARTESIAN_POINT('Ctrl Pts',(-0.5150712073616,0.9200957200099,-8.990129262769));
#39754=CARTESIAN_POINT('Ctrl Pts',(0.2069672452441,1.033932698984,-9.040829536345));
#39755=CARTESIAN_POINT('Ctrl Pts',(0.8295892607691,0.6509547014876,-9.091529809921));
#39756=CARTESIAN_POINT('Ctrl Pts',(1.053390111087,-0.04501237598842,-9.142230083497));
#39757=CARTESIAN_POINT('Ctrl Pts',(0.8655115137905,-0.494146506137,-9.176030265881));
#39758=CARTESIAN_POINT('Ctrl Pts',(0.7094068585195,-0.6615450922541,-9.192930357073));
#39759=CARTESIAN_POINT('Ctrl Pts',(-0.9661995571575,0.08578120859872,-7.6238809674));
#39760=CARTESIAN_POINT('Ctrl Pts',(-0.9459577835372,0.313775113412,-7.640781058592));
#39761=CARTESIAN_POINT('Ctrl Pts',(-0.7373325155345,0.7536561561237,-7.674581240976));
#39762=CARTESIAN_POINT('Ctrl Pts',(-0.06998968740697,1.052170047392,-7.725281514552));
#39763=CARTESIAN_POINT('Ctrl Pts',(0.6309663956697,0.8448276002645,-7.775981788128));
#39764=CARTESIAN_POINT('Ctrl Pts',(1.028714521555,0.2315619048451,-7.826682061704));
#39765=CARTESIAN_POINT('Ctrl Pts',(0.932108219137,-0.4929984447149,-7.87738233528));
#39766=CARTESIAN_POINT('Ctrl Pts',(0.3875739132888,-0.9806419265493,-7.928082608856));
#39767=CARTESIAN_POINT('Ctrl Pts',(-0.3432107204247,-0.9970351330367,-7.978782882432));
#39768=CARTESIAN_POINT('Ctrl Pts',(-0.9090640168405,-0.5342987274206,-8.029483156008));
#39769=CARTESIAN_POINT('Ctrl Pts',(-1.03806290686,0.1851970209741,-8.080183429584));
#39770=CARTESIAN_POINT('Ctrl Pts',(-0.668216439086,0.81569561,-8.13088370316));
#39771=CARTESIAN_POINT('Ctrl Pts',(0.02274415819314,1.054208346859,-8.181583976736));
#39772=CARTESIAN_POINT('Ctrl Pts',(0.7027749578096,0.7861169726968,-8.232284250312));
#39773=CARTESIAN_POINT('Ctrl Pts',(1.045084390477,0.1402538866513,-8.282984523888));
#39774=CARTESIAN_POINT('Ctrl Pts',(0.8851742648668,-0.573008775467,-8.333684797464));
#39775=CARTESIAN_POINT('Ctrl Pts',(0.2998900428063,-1.010909737899,-8.38438507104));
#39776=CARTESIAN_POINT('Ctrl Pts',(-0.4295075601491,-0.9630139104517,-8.435085344616));
#39777=CARTESIAN_POINT('Ctrl Pts',(-0.9525035565898,-0.4523378279972,-8.485785618192));
#39778=CARTESIAN_POINT('Ctrl Pts',(-1.017770091349,0.275711039135,-8.536485891768));
#39779=CARTESIAN_POINT('Ctrl Pts',(-0.5939430654806,0.8712658439924,-8.587186165344));
#39780=CARTESIAN_POINT('Ctrl Pts',(0.1153057184743,1.048130300761,-8.63788643892));
#39781=CARTESIAN_POINT('Ctrl Pts',(0.7691438697144,0.7213114743296,-8.688586712496));
#39782=CARTESIAN_POINT('Ctrl Pts',(1.053366804377,0.0478634837261,-8.739286986072));
#39783=CARTESIAN_POINT('Ctrl Pts',(0.8313900288183,-0.6485855033511,-8.789987259648));
#39784=CARTESIAN_POINT('Ctrl Pts',(0.2098854061311,-1.033354069586,-8.840687533224));
#39785=CARTESIAN_POINT('Ctrl Pts',(-0.5124805616198,-0.9215401939611,-8.8913878068));
#39786=CARTESIAN_POINT('Ctrl Pts',(-0.9885716900656,-0.3668761916084,-8.942088080376));
#39787=CARTESIAN_POINT('Ctrl Pts',(-0.9896014863655,0.364090781066,-8.992788353952));
#39788=CARTESIAN_POINT('Ctrl Pts',(-0.5150712073616,0.9200957200099,-9.043488627528));
#39789=CARTESIAN_POINT('Ctrl Pts',(0.2069672452441,1.033932698984,-9.094188901104));
#39790=CARTESIAN_POINT('Ctrl Pts',(0.8295892607691,0.6509547014876,-9.14488917468));
#39791=CARTESIAN_POINT('Ctrl Pts',(1.053390111087,-0.04501237598842,-9.195589448256));
#39792=CARTESIAN_POINT('Ctrl Pts',(0.8655115137905,-0.494146506137,-9.22938963064));
#39793=CARTESIAN_POINT('Ctrl Pts',(0.7094068585195,-0.6615450922541,-9.246289721832));
#39794=CARTESIAN_POINT('Ctrl Pts',(0.92175594885483,-0.300215476254899,
-9.07172448818857));
#39795=CARTESIAN_POINT('Ctrl Pts',(0.92175594885483,-0.300215476254899,
-9.09283316090538));
#39796=CARTESIAN_POINT('Ctrl Pts',(0.92175594885483,-0.300215476254899,
-9.11394183362219));
#39797=CARTESIAN_POINT('Ctrl Pts',(0.92175594885483,-0.300215476254899,
-9.15616978382025));
#39798=CARTESIAN_POINT('Ctrl Pts',(0.921755948854829,-0.300215476254899,
-9.17728906130151));
#39799=CARTESIAN_POINT('Ctrl Pts',(0.921755948854829,-0.300215476254899,
-9.19840833878276));
#39800=CARTESIAN_POINT('Origin',(1.188547950716,-0.3871095049826,-9.360050506339));
#39801=CARTESIAN_POINT('Origin',(-2.019557620655,-2.019557620655,-27.6432));
#39802=CARTESIAN_POINT('',(-0.5440622782918,-0.2950136037689,-10.8));
#39803=CARTESIAN_POINT('',(-0.6490486745229,-0.4,-12.));
#39804=CARTESIAN_POINT('',(-0.2950136037689,-0.5440622782918,-10.8));
#39805=CARTESIAN_POINT('Origin',(-0.545968563155165,-0.545968563155165,
-10.8));
#39806=CARTESIAN_POINT('',(-0.4,-0.6490486745229,-12.));
#39807=CARTESIAN_POINT('Origin',(-0.4,-0.4,-12.));
#39808=CARTESIAN_POINT('',(-0.995964929246,-0.2950136037689,-10.8));
#39809=CARTESIAN_POINT('',(-0.995964929246,-0.2950136037689,-10.8));
#39810=CARTESIAN_POINT('',(-0.995964929246,-0.2950136037689,-10.8));
#39811=CARTESIAN_POINT('Origin',(0.,0.,-10.8));
#39812=CARTESIAN_POINT('',(0.2950136037689,-0.5440622782918,-10.8));
#39813=CARTESIAN_POINT('',(0.2950136037689,-0.995964929246,-10.8));
#39814=CARTESIAN_POINT('',(0.2950136037689,-0.5440622782918,-10.8));
#39815=CARTESIAN_POINT('',(0.04596492924595,-1.245013603769,-10.8));
#39816=CARTESIAN_POINT('Origin',(0.0440586443834295,-0.99405864438343,-10.8));
#39817=CARTESIAN_POINT('',(-0.04596492924595,-1.245013603769,-10.8));
#39818=CARTESIAN_POINT('',(0.04596492924595,-1.245013603769,-10.8));
#39819=CARTESIAN_POINT('',(-0.2950136037689,-0.995964929246,-10.8));
#39820=CARTESIAN_POINT('Origin',(-0.0440586443826807,-0.994058644382681,
-10.8));
#39821=CARTESIAN_POINT('',(-0.2950136037689,-0.5440622782918,-10.8));
#39822=CARTESIAN_POINT('',(-1.245013603769,-0.04596492924595,-10.8));
#39823=CARTESIAN_POINT('Origin',(-0.994058644383262,-0.0440586443832619,
-10.8));
#39824=CARTESIAN_POINT('',(-1.245013603769,0.04596492924595,-10.8));
#39825=CARTESIAN_POINT('',(-1.245013603769,0.04596492924595,-10.8));
#39826=CARTESIAN_POINT('',(-0.995964929246,0.2950136037689,-10.8));
#39827=CARTESIAN_POINT('Origin',(-0.994058644383421,0.0440586443834207,
-10.8));
#39828=CARTESIAN_POINT('',(-0.5440622782918,0.2950136037689,-10.8));
#39829=CARTESIAN_POINT('',(-0.995964929246,0.2950136037689,-10.8));
#39830=CARTESIAN_POINT('',(-0.2950136037689,0.5440622782918,-10.8));
#39831=CARTESIAN_POINT('Origin',(-0.545968563155165,0.545968563155165,-10.8));
#39832=CARTESIAN_POINT('',(-0.2950136037689,0.995964929246,-10.8));
#39833=CARTESIAN_POINT('',(-0.2950136037689,0.995964929246,-10.8));
#39834=CARTESIAN_POINT('',(-0.04596492924595,1.245013603769,-10.8));
#39835=CARTESIAN_POINT('Origin',(-0.0440586443832125,0.994058644383213,
-10.8));
#39836=CARTESIAN_POINT('',(0.04596492924595,1.245013603769,-10.8));
#39837=CARTESIAN_POINT('',(-0.04596492924595,1.245013603769,-10.8));
#39838=CARTESIAN_POINT('',(0.2950136037689,0.995964929246,-10.8));
#39839=CARTESIAN_POINT('Origin',(0.0440586443829719,0.994058644382972,-10.8));
#39840=CARTESIAN_POINT('',(0.2950136037689,0.5440622782918,-10.8));
#39841=CARTESIAN_POINT('',(0.2950136037689,0.995964929246,-10.8));
#39842=CARTESIAN_POINT('',(0.5440622782918,0.2950136037689,-10.8));
#39843=CARTESIAN_POINT('Origin',(0.545968563155165,0.545968563155165,-10.8));
#39844=CARTESIAN_POINT('',(0.995964929246,0.2950136037689,-10.8));
#39845=CARTESIAN_POINT('',(0.5440622782918,0.2950136037689,-10.8));
#39846=CARTESIAN_POINT('',(1.245013603769,0.04596492924595,-10.8));
#39847=CARTESIAN_POINT('Origin',(0.994058644383084,0.0440586443830834,-10.8));
#39848=CARTESIAN_POINT('',(1.245013603769,-0.04596492924595,-10.8));
#39849=CARTESIAN_POINT('',(1.245013603769,-0.04596492924595,-10.8));
#39850=CARTESIAN_POINT('',(0.995964929246,-0.2950136037689,-10.8));
#39851=CARTESIAN_POINT('Origin',(0.994058644382849,-0.0440586443828492,
-10.8));
#39852=CARTESIAN_POINT('',(0.5440622782918,-0.2950136037689,-10.8));
#39853=CARTESIAN_POINT('',(0.995964929246,-0.2950136037689,-10.8));
#39854=CARTESIAN_POINT('Origin',(0.545968563155165,-0.545968563155165,-10.8));
#39855=CARTESIAN_POINT('Origin',(0.4,-0.4,-12.));
#39856=CARTESIAN_POINT('',(0.4,-0.6490486745229,-12.));
#39857=CARTESIAN_POINT('',(0.2950136037689,-0.995964929246,-10.8));
#39858=CARTESIAN_POINT('Origin',(2.019557620655,-2.019557620655,-27.6432));
#39859=CARTESIAN_POINT('',(0.6490486745229,-0.4,-12.));
#39860=CARTESIAN_POINT('Origin',(1.35,-0.4,-12.));
#39861=CARTESIAN_POINT('',(0.995964929246,-0.2950136037689,-10.8));
#39862=CARTESIAN_POINT('Origin',(-1.167126683436,2.117126683436,13.90246133293));
#39863=CARTESIAN_POINT('',(1.245013603769,-0.04596492924595,-10.8));
#39864=CARTESIAN_POINT('Origin',(1.35,0.4,-12.));
#39865=CARTESIAN_POINT('',(1.245013603769,0.04596492924595,-10.8));
#39866=CARTESIAN_POINT('Origin',(-1.164769817959,-2.114769817959,13.87552223726));
#39867=CARTESIAN_POINT('',(0.995964929246,0.2950136037689,-10.8));
#39868=CARTESIAN_POINT('Origin',(0.4,0.4,-12.));
#39869=CARTESIAN_POINT('',(0.6490486745229,0.4,-12.));
#39870=CARTESIAN_POINT('Origin',(2.019557620655,2.019557620655,-27.6432));
#39871=CARTESIAN_POINT('',(0.4,0.6490486745229,-12.));
#39872=CARTESIAN_POINT('Origin',(0.4,1.35,-12.));
#39873=CARTESIAN_POINT('',(0.2950136037689,0.995964929246,-10.8));
#39874=CARTESIAN_POINT('Origin',(-2.113404067612,-1.163404067612,13.85991163936));
#39875=CARTESIAN_POINT('',(0.04596492924595,1.245013603769,-10.8));
#39876=CARTESIAN_POINT('Origin',(-0.4,1.35,-12.));
#39877=CARTESIAN_POINT('',(-0.04596492924595,1.245013603769,-10.8));
#39878=CARTESIAN_POINT('Origin',(2.115813258549,-1.165813258549,13.88744881778));
#39879=CARTESIAN_POINT('',(-0.2950136037689,0.995964929246,-10.8));
#39880=CARTESIAN_POINT('Origin',(-0.4,0.4,-12.));
#39881=CARTESIAN_POINT('',(-0.4,0.6490486745229,-12.));
#39882=CARTESIAN_POINT('Origin',(-2.019557620655,2.019557620655,-27.6432));
#39883=CARTESIAN_POINT('',(-0.6490486745229,0.4,-12.));
#39884=CARTESIAN_POINT('Origin',(-1.35,0.4,-12.));
#39885=CARTESIAN_POINT('',(-0.995964929246,0.2950136037689,-10.8));
#39886=CARTESIAN_POINT('Origin',(1.229404966539,-2.179404966539,14.61430536613));
#39887=CARTESIAN_POINT('',(-1.245013603769,0.04596492924595,-10.8));
#39888=CARTESIAN_POINT('Origin',(-1.35,-0.4,-12.));
#39889=CARTESIAN_POINT('',(-1.245013603769,-0.04596492924595,-10.8));
#39890=CARTESIAN_POINT('Origin',(1.25220562464,2.20220562464,14.87491808076));
#39891=CARTESIAN_POINT('Origin',(-2.18078482228,1.23078482228,14.63007718942));
#39892=CARTESIAN_POINT('',(0.04596492924595,-1.245013603769,-10.8));
#39893=CARTESIAN_POINT('Origin',(0.4,-1.35,-12.));
#39894=CARTESIAN_POINT('',(-0.04596492924595,-1.245013603769,-10.8));
#39895=CARTESIAN_POINT('Origin',(2.202175235882,1.252175235882,14.87457073566));
#39896=CARTESIAN_POINT('',(-0.2950136037689,-0.995964929246,-10.8));
#39897=CARTESIAN_POINT('Origin',(-0.4,-1.35,-12.));
#52142=UNCERTAINTY_MEASURE_WITH_UNIT(LENGTH_MEASURE(0.01),#52165,
'DISTANCE_ACCURACY_VALUE',
'Maximum model space distance between geometric entities at asserted c
onnectivities');
#52149=UNCERTAINTY_MEASURE_WITH_UNIT(LENGTH_MEASURE(0.01),#52165,
'DISTANCE_ACCURACY_VALUE',
'Maximum model space distance between geometric entities at asserted c
onnectivities');
#52157=(
GEOMETRIC_REPRESENTATION_CONTEXT(3)
GLOBAL_UNCERTAINTY_ASSIGNED_CONTEXT((#52142))
GLOBAL_UNIT_ASSIGNED_CONTEXT((#52165,#52167,#52168))
REPRESENTATION_CONTEXT('','3D')
);
#52164=(
GEOMETRIC_REPRESENTATION_CONTEXT(3)
GLOBAL_UNCERTAINTY_ASSIGNED_CONTEXT((#52149))
GLOBAL_UNIT_ASSIGNED_CONTEXT((#52165,#52167,#52168))
REPRESENTATION_CONTEXT('','3D')
);
#52165=(
LENGTH_UNIT()
NAMED_UNIT(*)
SI_UNIT(.MILLI.,.METRE.)
);
#52167=(
NAMED_UNIT(*)
PLANE_ANGLE_UNIT()
SI_UNIT($,.RADIAN.)
);
#52168=(
NAMED_UNIT(*)
SI_UNIT($,.STERADIAN.)
SOLID_ANGLE_UNIT()
);
#52176=SHAPE_DEFINITION_REPRESENTATION(#52190,#52217);
#52190=PRODUCT_DEFINITION_SHAPE('',$,#52232);
#52217=SHAPE_REPRESENTATION('',(#9921),#52157);
#52224=PRODUCT_DEFINITION_CONTEXT('part definition',#52268,'design');
#52232=PRODUCT_DEFINITION('Countersunk Screw 2.5x12',
'Countersunk Screw 2.5x12',#52246,#52224);
#52246=PRODUCT_DEFINITION_FORMATION('',$,#52277);
#52268=APPLICATION_CONTEXT('Managed model based 3d engineering');
#52269=PRODUCT_CONTEXT('part definition',#52268,'mechanical');
#52277=PRODUCT('Countersunk Screw 2.5x12','Countersunk Screw 2.5x12',
'NOT SPECIFIED',(#52269));
#52319=COLOUR_RGB('Black',0.12,0.14,0.17);
#52320=FILL_AREA_STYLE_COLOUR('',#52319);
#52321=FILL_AREA_STYLE('',(#52320));
#52322=SURFACE_STYLE_FILL_AREA(#52321);
#52323=SURFACE_SIDE_STYLE('',(#52322));
#52324=SURFACE_STYLE_USAGE(.BOTH.,#52323);
#52325=PRESENTATION_STYLE_ASSIGNMENT((#52324));
ENDSEC;
END-ISO-10303-21;
